ISO-10303-21;
HEADER;
FILE_DESCRIPTION (('STEP AP214'),
    '1' );
FILE_NAME ('Press Handle.step',
    '2026-10-24T22:54:28',
    ( '' ),
    ( '' ),
    'SwSTEP 2.0',
    'SolidWorks 2025',
    '' );
FILE_SCHEMA (( 'AUTOMOTIVE_DESIGN' ));
ENDSEC;

DATA;
#2=CARTESIAN_POINT ( 'NONE',  ( 80.93548213101077238, 62.17232332437959030, -2.988136994358703724 ) ) ;
#14=LINE ( 'NONE', #31910, #38253 ) ;
#15=CARTESIAN_POINT ( 'NONE',  ( -64.08758708074093136, 42.07456177326923097, -2.837280263138449943 ) ) ;
#16=CARTESIAN_POINT ( 'NONE',  ( 73.82474952339838126, 59.08733682254641195, 3.476886323308218341 ) ) ;
#27=CARTESIAN_POINT ( 'NONE',  ( 81.24504193829311305, 64.75648403698987465, 3.071899782094678066 ) ) ;
#34=ADVANCED_FACE ( 'NONE', ( #40006 ), #27046, .T. ) ;
#38=AXIS2_PLACEMENT_3D ( 'NONE', #3449, #15964, #28321 ) ;
#45=CARTESIAN_POINT ( 'NONE',  ( 66.41901733680204245, 57.79934748174496661, -4.000000000000019540 ) ) ;
#56=CARTESIAN_POINT ( 'NONE',  ( 80.36293583174420974, 66.30725055998094319, -1.299258709309398130 ) ) ;
#58=CARTESIAN_POINT ( 'NONE',  ( 79.04990754624076033, 65.77731930041099417, 2.468641556982019925 ) ) ;
#61=CARTESIAN_POINT ( 'NONE',  ( 76.46949791074162306, 63.77707083977483649, -3.308002540424319626 ) ) ;
#65=CARTESIAN_POINT ( 'NONE',  ( 81.32291525751645622, 62.59435864775878144, -3.036434590848177795 ) ) ;
#66=CARTESIAN_POINT ( 'NONE',  ( 78.75717319332348154, 60.46956391627949756, 2.498359881428524609 ) ) ;
#71=CARTESIAN_POINT ( 'NONE',  ( 80.25084519670748762, 66.24728552308215512, 1.725837398062988415 ) ) ;
#79=CARTESIAN_POINT ( 'NONE',  ( -64.37872067649581709, 36.58503142451505141, 5.660009492437676037 ) ) ;
#82=ORIENTED_EDGE ( 'NONE', *, *, #9020, .T. ) ;
#94=DIRECTION ( 'NONE',  ( -0.000000000000000000, -0.000000000000000000, -1.000000000000000000 ) ) ;
#95=CARTESIAN_POINT ( 'NONE',  ( 68.04343099365841852, 58.34291608657256489, -3.996230182412897403 ) ) ;
#101=PRODUCT ( 'Press Handle', 'Press Handle', '', ( #4245 ) ) ;
#110=CARTESIAN_POINT ( 'NONE',  ( 78.59948840878007559, 65.10367658859402695, -3.015657119755322579 ) ) ;
#114=CARTESIAN_POINT ( 'NONE',  ( 81.64185025298566245, 61.96196063151609223, -2.170472567296702682 ) ) ;
#115=CARTESIAN_POINT ( 'NONE',  ( 80.76516742887832834, 61.34548671587045021, 2.174061886842027391 ) ) ;
#118=CARTESIAN_POINT ( 'NONE',  ( 82.55792188592127445, 63.20960171500894376, 1.000000000000000000 ) ) ;
#143=CARTESIAN_POINT ( 'NONE',  ( 66.81418162778464875, 58.07599004166701206, 3.996206253860483226 ) ) ;
#156=CARTESIAN_POINT ( 'NONE',  ( 80.09094484276194237, 63.40703332228277134, -3.714073935154547978 ) ) ;
#158=CARTESIAN_POINT ( 'NONE',  ( 80.96252947514877008, 61.71397308826822581, 2.561782662428527146 ) ) ;
#161=CARTESIAN_POINT ( 'NONE',  ( -56.74902312943272165, 30.60926302035622371, 3.177788716294913218 ) ) ;
#170=ADVANCED_FACE ( 'NONE', ( #3587 ), #276, .T. ) ;
#175=CARTESIAN_POINT ( 'NONE',  ( 80.63945418285952371, 64.43655742540516940, 3.486376426170536114 ) ) ;
#189=CARTESIAN_POINT ( 'NONE',  ( 81.06839910345442490, 62.80152057670051846, -3.286127602909473033 ) ) ;
#190=CARTESIAN_POINT ( 'NONE',  ( -63.71197174466732349, 35.78007194159061299, 7.175960652854955768 ) ) ;
#197=ORIENTED_EDGE ( 'NONE', *, *, #37878, .T. ) ;
#198=CARTESIAN_POINT ( 'NONE',  ( 81.07009230622234952, 61.73904331373559984, -2.506402126386314322 ) ) ;
#209=CARTESIAN_POINT ( 'NONE',  ( 69.48201546320520094, 59.78788955577742570, 3.863726395435664873 ) ) ;
#214=CARTESIAN_POINT ( 'NONE',  ( -58.99259650353461382, 28.71101865976197587, -6.736149549807849191 ) ) ;
#216=CARTESIAN_POINT ( 'NONE',  ( 81.76017987128392406, 63.49575590176132067, 2.919551171211350216 ) ) ;
#227=CYLINDRICAL_SURFACE ( 'NONE', #21754, 6.681288188914807691 ) ;
#233=EDGE_LOOP ( 'NONE', ( #32322, #27036, #31978, #32263 ) ) ;
#237=CARTESIAN_POINT ( 'NONE',  ( 66.56396446968585678, 57.85070090013417854, -3.999903336036485957 ) ) ;
#246=CARTESIAN_POINT ( 'NONE',  ( -59.00110696496997775, 28.68040728033255249, -6.999999999999999112 ) ) ;
#249=CARTESIAN_POINT ( 'NONE',  ( 82.38651420471377662, 62.84168609110417236, -1.553473047276889840 ) ) ;
#251=CARTESIAN_POINT ( 'NONE',  ( 79.70909206057019958, 64.65202245283560956, 3.503057693382588322 ) ) ;
#254=CARTESIAN_POINT ( 'NONE',  ( 76.25248298134039260, 64.19605381821561707, -2.844364419910041519 ) ) ;
#258=CARTESIAN_POINT ( 'NONE',  ( 80.74417485493692936, 64.10566034184273576, -3.509897338575004522 ) ) ;
#259=CARTESIAN_POINT ( 'NONE',  ( 79.36485406729205749, 60.67242113316877550, 2.285396881590402440 ) ) ;
#263=CARTESIAN_POINT ( 'NONE',  ( -59.00110696496997775, 28.68040728033253473, 6.999999999999999112 ) ) ;
#265=CARTESIAN_POINT ( 'NONE',  ( 81.68900298540742710, 61.66555023304469785, 1.322881339814628632 ) ) ;
#271=CARTESIAN_POINT ( 'NONE',  ( -62.77932549131172379, 36.45562188509706658, 4.736925958236329670 ) ) ;
#276=PLANE ( 'NONE',  #38056 ) ;
#278=CARTESIAN_POINT ( 'NONE',  ( 76.65113373804888397, 59.82741887089902377, -3.005488744293225878 ) ) ;
#288=CARTESIAN_POINT ( 'NONE',  ( -74.92283640148291113, 18.87330372387140187, 9.800414904976365804 ) ) ;
#289=CARTESIAN_POINT ( 'NONE',  ( 67.79930094788625183, 58.10454462619039617, -3.992148460412407118 ) ) ;
#307=CARTESIAN_POINT ( 'NONE',  ( 27.60344192425479193, 81.15229837709949834, -1.000000000000000000 ) ) ;
#310=CARTESIAN_POINT ( 'NONE',  ( 80.31443933487477693, 61.76769068803228180, -3.015657119755351889 ) ) ;
#313=CARTESIAN_POINT ( 'NONE',  ( 81.74528107327192572, 62.23958694028459604, -2.368810654844693442 ) ) ;
#314=CARTESIAN_POINT ( 'NONE',  ( 80.80164418317316688, 61.17044828488889152, 1.584170212883420081 ) ) ;
#341=CARTESIAN_POINT ( 'NONE',  ( 67.12475893546654504, 58.13278081555189658, 3.997693602769900156 ) ) ;
#359=CARTESIAN_POINT ( 'NONE',  ( 79.50008710437273862, 64.50769319364300713, -3.547878946066220340 ) ) ;
#362=CARTESIAN_POINT ( 'NONE',  ( 79.01373585440697411, 65.47072129778472060, 2.830664096605183921 ) ) ;
#367=( BOUNDED_SURFACE ( )  B_SPLINE_SURFACE ( 3, 2, ( 
 ( #9527, #37331, #24992 ),
 ( #34282, #3403, #24575 ),
 ( #28067, #3199, #6052 ),
 ( #11995, #40408, #19015 ),
 ( #21902, #34688, #15098 ),
 ( #12423, #34889, #9127 ) ),
 .UNSPECIFIED., .F., .F., .F. ) 
 B_SPLINE_SURFACE_WITH_KNOTS ( ( 4, 2, 4 ),
 ( 3, 3 ),
 ( 0.000000000000000000, 0.001067213068434984691, 0.002134426136869969383 ),
 ( 0.000000000000000000, 1.000000000000000000 ),
 .UNSPECIFIED. ) 
 GEOMETRIC_REPRESENTATION_ITEM ( )  RATIONAL_B_SPLINE_SURFACE ( (
 ( 1.000000000000000000, 0.6872206705711639829, 1.000000000000000000),
 ( 1.000000000000000000, 0.6752582546153387266, 1.000000000000000000),
 ( 1.000000000000000000, 0.6623616715684274014, 1.000000000000000000),
 ( 1.000000000000000000, 0.6342435107462650601, 1.000000000000000000),
 ( 1.000000000000000000, 0.6188407181626371933, 1.000000000000000000),
 ( 1.000000000000000000, 0.6029302108204154242, 1.000000000000000000) ) ) 
 REPRESENTATION_ITEM ( '' )  SURFACE ( )  );
#380=CARTESIAN_POINT ( 'NONE',  ( 81.32291525751649885, 62.59435864775880987, 3.036434590848157367 ) ) ;
#386=EDGE_CURVE ( 'NONE', #34099, #38151, #20947, .T. ) ;
#391=CARTESIAN_POINT ( 'NONE',  ( 25.11437021580303863, 164.7550792202006562, -1.000000000000000000 ) ) ;
#398=CARTESIAN_POINT ( 'NONE',  ( 79.64354988242321554, 65.32830775696902492, -3.122598816540614663 ) ) ;
#404=EDGE_CURVE ( 'NONE', #16945, #2799, #36230, .T. ) ;
#409=CARTESIAN_POINT ( 'NONE',  ( 78.68112288793685138, 66.00442204571392324, -1.607835478472330548 ) ) ;
#410=DIRECTION ( 'NONE',  ( 0.000000000000000000, -0.5555716052200797561, 0.8314686954258614371 ) ) ;
#412=CARTESIAN_POINT ( 'NONE',  ( 81.67793621607867749, 64.59267988934871596, -2.776691787112390397 ) ) ;
#420=CARTESIAN_POINT ( 'NONE',  ( 72.46216784064273497, 59.07243765930573431, 3.784404822033881288 ) ) ;
#428=CARTESIAN_POINT ( 'NONE',  ( 81.28907188958037011, 64.38987696229567348, 3.179853676208927116 ) ) ;
#446=VERTEX_POINT ( 'NONE', #1684 ) ;
#447=CARTESIAN_POINT ( 'NONE',  ( 66.42990020876152357, 57.76860247958598649, -4.000000000000009770 ) ) ;
#452=EDGE_CURVE ( 'NONE', #38236, #38151, #37379, .T. ) ;
#459=CARTESIAN_POINT ( 'NONE',  ( 81.58705100058459436, 65.69127060146935548, -1.444831904610020645 ) ) ;
#460=CARTESIAN_POINT ( 'NONE',  ( 81.07747211222739736, 61.58128768033702727, 2.227525437860359947 ) ) ;
#464=CARTESIAN_POINT ( 'NONE',  ( 75.27909492816711179, 60.48191808705185224, -3.786335567263138469 ) ) ;
#468=CARTESIAN_POINT ( 'NONE',  ( 79.68360889523899004, 65.64663933523164019, -2.797238656122822409 ) ) ;
#470=CARTESIAN_POINT ( 'NONE',  ( 75.74534653887745606, 63.84344576921726144, 2.970791854430534062 ) ) ;
#475=CARTESIAN_POINT ( 'NONE',  ( 82.09661666296835847, 62.69434707785895000, 2.190303691588293855 ) ) ;
#479=CIRCLE ( 'NONE', #7686, 6.329987104167475565 ) ;
#488=FACE_OUTER_BOUND ( 'NONE', #13400, .T. ) ;
#499=ORIENTED_EDGE ( 'NONE', *, *, #31706, .F. ) ;
#501=CARTESIAN_POINT ( 'NONE',  ( 68.15116243724637002, 58.05457144382717871, -3.974537232972704892 ) ) ;
#516=CARTESIAN_POINT ( 'NONE',  ( 79.64354988242320132, 65.32830775696902492, 3.122598816540617328 ) ) ;
#519=CARTESIAN_POINT ( 'NONE',  ( 79.72787136111028872, 62.61980214589642202, -3.627744115730416219 ) ) ;
#522=CARTESIAN_POINT ( 'NONE',  ( 81.36150051724392540, 64.03901721961885585, -3.243459512787965515 ) ) ;
#523=CARTESIAN_POINT ( 'NONE',  ( 78.40723131619293440, 65.41550730244513545, 2.551437666014014560 ) ) ;
#526=CARTESIAN_POINT ( 'NONE',  ( -64.08758708074093136, 42.86825253631505461, 2.416740206856579753 ) ) ;
#551=CARTESIAN_POINT ( 'NONE',  ( 66.74992980603514070, 57.79401841677491092, 3.997717836767872512 ) ) ;
#565=CARTESIAN_POINT ( 'NONE',  ( 80.74625401487976717, 62.12052764141679262, -3.052025427726072326 ) ) ;
#567=CARTESIAN_POINT ( 'NONE',  ( 81.02662073326128223, 61.25180701697230035, 1.364493914842159539 ) ) ;
#572=CARTESIAN_POINT ( 'NONE',  ( -58.88620717884589340, 28.60568668665318270, 6.105166739222743111 ) ) ;
#585=CARTESIAN_POINT ( 'NONE',  ( 79.76270496343317973, 65.40180735727545880, 3.071811904357677037 ) ) ;
#592=LINE ( 'NONE', #16805, #19092 ) ;
#595=CARTESIAN_POINT ( 'NONE',  ( 69.29807964942261833, 58.55307042757259950, 3.976370928559292750 ) ) ;
#597=CARTESIAN_POINT ( 'NONE',  ( 72.90994289418092933, 61.20204674871914818, -3.824679913472085246 ) ) ;
#603=ORIENTED_EDGE ( 'NONE', *, *, #22140, .F. ) ;
#609=CARTESIAN_POINT ( 'NONE',  ( 80.08517677095778708, 64.13476336867732641, -3.668443954219269720 ) ) ;
#617=CARTESIAN_POINT ( 'NONE',  ( -59.01448254578837549, 27.97260867553151442, -6.241456863628584095 ) ) ;
#620=CARTESIAN_POINT ( 'NONE',  ( -64.08758708074093136, 43.28737448534269561, -1.986914326913568507 ) ) ;
#621=CARTESIAN_POINT ( 'NONE',  ( 71.06822368831490166, 59.17031991972731930, 3.954977122261625233 ) ) ;
#632=CARTESIAN_POINT ( 'NONE',  ( 81.50569694085116623, 63.36683741554951865, 3.125353918848690515 ) ) ;
#647=DIRECTION ( 'NONE',  ( -1.000000000000000000, 0.000000000000000000, 0.000000000000000000 ) ) ;
#654=CARTESIAN_POINT ( 'NONE',  ( 66.42693215277256513, 57.77698748017479602, -4.000000000000012434 ) ) ;
#663=CARTESIAN_POINT ( 'NONE',  ( 81.85052347209619938, 65.46610162458726734, -1.468380750528963663 ) ) ;
#667=CARTESIAN_POINT ( 'NONE',  ( 76.46948511138614890, 60.90388096812819896, -3.723120700756775481 ) ) ;
#668=CARTESIAN_POINT ( 'NONE',  ( 9.703489126596464232, 56.50623631086179444, -4.000000000000000000 ) ) ;
#671=CARTESIAN_POINT ( 'NONE',  ( 76.39232039721480305, 61.07121484735989014, 3.784676997173924917 ) ) ;
#672=ORIENTED_EDGE ( 'NONE', *, *, #6663, .F. ) ;
#676=CARTESIAN_POINT ( 'NONE',  ( 81.92450911876647979, 64.33049094056644890, 2.665107514500538066 ) ) ;
#692=DIRECTION ( 'NONE',  ( -0.9267318687906771491, 0.3757233601570964532, -0.000000000000000000 ) ) ;
#701=CARTESIAN_POINT ( 'NONE',  ( 68.67947939959147163, 58.42312895491860303, -3.988324671431326962 ) ) ;
#711=CARTESIAN_POINT ( 'NONE',  ( 81.26572199898306792, 62.02204868734986576, 2.661900242191197474 ) ) ;
#714=CARTESIAN_POINT ( 'NONE',  ( 79.75127500915171197, 61.39906162938307688, -2.976941560848460178 ) ) ;
#717=CARTESIAN_POINT ( 'NONE',  ( 81.65590348737067927, 63.08388229442042672, -2.971291902545804664 ) ) ;
#718=CARTESIAN_POINT ( 'NONE',  ( 80.00843888008158444, 62.42993222482912330, 3.516968106976306796 ) ) ;
#720=CARTESIAN_POINT ( 'NONE',  ( 79.34209122208885390, 66.30884595491197331, 1.045691535380374182 ) ) ;
#729=CARTESIAN_POINT ( 'NONE',  ( -73.45070404594234503, 38.65432087843067421, 8.800414904976364028 ) ) ;
#736=CARTESIAN_POINT ( 'NONE',  ( -57.33218521099392717, 34.44152469268617978, 4.000000000000000000 ) ) ;
#738=CARTESIAN_POINT ( 'NONE',  ( -59.89982099243562885, 24.84364830758654463, -9.562162450795215207 ) ) ;
#747=CARTESIAN_POINT ( 'NONE',  ( 66.69989039061726999, 57.93340768760646142, 3.999416444362183576 ) ) ;
#748=CARTESIAN_POINT ( 'NONE',  ( -63.08758708074093136, 38.76906266698302517, 3.999999999999999112 ) ) ;
#750=TOROIDAL_SURFACE ( 'NONE', #1396, 82.54614097552274643, 3.000000000000000000 ) ;
#758=ORIENTED_EDGE ( 'NONE', *, *, #22196, .T. ) ;
#761=CARTESIAN_POINT ( 'NONE',  ( 80.85057025077259141, 61.36744894077061474, -2.123311106147459437 ) ) ;
#763=CARTESIAN_POINT ( 'NONE',  ( 80.09094484276241133, 63.40703332228300582, 3.714073935154433403 ) ) ;
#765=ORIENTED_EDGE ( 'NONE', *, *, #16076, .T. ) ;
#777=AXIS2_PLACEMENT_3D ( 'NONE', #21400, #36426, #4928 ) ;
#782=CARTESIAN_POINT ( 'NONE',  ( 80.84834833306135238, 63.77578157039150142, 3.533418250979425856 ) ) ;
#786=CARTESIAN_POINT ( 'NONE',  ( -64.08758708074093136, 38.76906266698303227, 3.000000000000000000 ) ) ;
#788=CARTESIAN_POINT ( 'NONE',  ( -64.95171866297675933, 36.28765213650434163, 6.629387290673633970 ) ) ;
#790=CARTESIAN_POINT ( 'NONE',  ( 35.94200923520244828, 151.3264224549853907, -1.000000000000000000 ) ) ;
#797=CARTESIAN_POINT ( 'NONE',  ( 81.21900516562017458, 61.35514353465740101, -1.483717294826000455 ) ) ;
#800=DIRECTION ( 'NONE',  ( -0.9506097019758704691, 0.3103887796125160414, 0.000000000000000000 ) ) ;
#808=CARTESIAN_POINT ( 'NONE',  ( 81.01565502672981722, 61.93906859853276359, -2.769656700700041885 ) ) ;
#822=CARTESIAN_POINT ( 'NONE',  ( -64.08758708074093136, 43.19303868977686989, -2.106422863670424306 ) ) ;
#823=CARTESIAN_POINT ( 'NONE',  ( 70.70040249450607917, 60.07892802134021792, 3.908768822720051883 ) ) ;
#831=CARTESIAN_POINT ( 'NONE',  ( 79.91673984738221748, 65.77987873796179485, 2.647945256410967563 ) ) ;
#866=CARTESIAN_POINT ( 'NONE',  ( 80.96936403957134587, 66.06451342975866226, -1.623788564014418512 ) ) ;
#869=CARTESIAN_POINT ( 'NONE',  ( 75.23821009641447688, 63.49083772021889160, -3.097219288950977312 ) ) ;
#870=FACE_OUTER_BOUND ( 'NONE', #24325, .T. ) ;
#873=CARTESIAN_POINT ( 'NONE',  ( 76.98341904138483471, 61.29654188154451333, 3.753756190332411258 ) ) ;
#875=CARTESIAN_POINT ( 'NONE',  ( -81.07947155388369254, 30.81399289130168384, -9.800414904976365804 ) ) ;
#879=CARTESIAN_POINT ( 'NONE',  ( 82.22785179944530398, 62.76084426383168591, 1.971256063808052739 ) ) ;
#896=DIRECTION ( 'NONE',  ( -0.000000000000000000, -0.000000000000000000, -1.000000000000000000 ) ) ;
#897=CARTESIAN_POINT ( 'NONE',  ( 68.47014483779531702, 58.97518246833449496, -3.964410623303926684 ) ) ;
#910=EDGE_CURVE ( 'NONE', #15868, #38802, #3918, .T. ) ;
#913=CARTESIAN_POINT ( 'NONE',  ( 78.66037426029973290, 66.03727662354840788, 1.183438861787456942 ) ) ;
#918=CARTESIAN_POINT ( 'NONE',  ( 77.99157368707381011, 64.87245838797727515, -2.976941560848442414 ) ) ;
#921=CARTESIAN_POINT ( 'NONE',  ( 79.28168835806300763, 66.11151980551120744, -1.907437723456246736 ) ) ;
#922=CARTESIAN_POINT ( 'NONE',  ( 78.69960226590261243, 64.59913094042720161, 3.401284978681007765 ) ) ;
#925=CARTESIAN_POINT ( 'NONE',  ( 82.41652906543031065, 64.58603266165646062, 1.328060019257126356 ) ) ;
#926=CARTESIAN_POINT ( 'NONE',  ( -64.08758708074093136, 43.97762867865598935, 1.773567450131052770 ) ) ;
#929=CARTESIAN_POINT ( 'NONE',  ( -64.12639773666757037, 35.29406715002951245, -4.430479139283492351 ) ) ;
#940=LINE ( 'NONE', #6709, #6812 ) ;
#945=AXIS2_PLACEMENT_3D ( 'NONE', #27776, #14403, #26973 ) ;
#951=CARTESIAN_POINT ( 'NONE',  ( 66.74110339505794798, 57.81860698948682398, 3.998609561963397674 ) ) ;
#965=ORIENTED_EDGE ( 'NONE', *, *, #8161, .F. ) ;
#966=CARTESIAN_POINT ( 'NONE',  ( 80.30026770407522463, 62.83227110018524542, -3.557377001560567020 ) ) ;
#968=CARTESIAN_POINT ( 'NONE',  ( 80.23164863169043315, 63.12273326640292481, 3.657510014241676988 ) ) ;
#978=ORIENTED_EDGE ( 'NONE', *, *, #38162, .F. ) ;
#980=ORIENTED_EDGE ( 'NONE', *, *, #4879, .T. ) ;
#987=CARTESIAN_POINT ( 'NONE',  ( 79.42405716688907091, 65.78352207363050752, 2.615128354545391165 ) ) ;
#998=CARTESIAN_POINT ( 'NONE',  ( 69.03381461298826594, 59.23726071663833181, 3.954017255840780454 ) ) ;
#1002=CARTESIAN_POINT ( 'NONE',  ( -64.08758708074094557, 43.19303869255161743, -2.106422866370387226 ) ) ;
#1003=AXIS2_PLACEMENT_3D ( 'NONE', #22810, #7149, #38030 ) ;
#1005=CARTESIAN_POINT ( 'NONE',  ( 81.11292571623972947, 62.23233742369612997, -2.923497156821700305 ) ) ;
#1011=CARTESIAN_POINT ( 'NONE',  ( -60.36144324275490902, 24.84364830758653397, -8.926047827505314558 ) ) ;
#1017=CARTESIAN_POINT ( 'NONE',  ( 80.89004220740235951, 62.15918302697183151, -3.003915454719715772 ) ) ;
#1026=CARTESIAN_POINT ( 'NONE',  ( -63.60792738000480284, 43.84705609857426367, -2.659634298586695422 ) ) ;
#1027=CARTESIAN_POINT ( 'NONE',  ( 71.74426859761079811, 60.78783288850196698, 3.823636340558493885 ) ) ;
#1033=AXIS2_PLACEMENT_3D ( 'NONE', #29881, #20807, #8445 ) ;
#1039=CARTESIAN_POINT ( 'NONE',  ( 80.78189192730862089, 64.90162691771338643, 3.235508711566409179 ) ) ;
#1052=ADVANCED_FACE ( 'NONE', ( #32716 ), #35248, .T. ) ;
#1069=CARTESIAN_POINT ( 'NONE',  ( -55.71184120586743660, 30.71742687230106839, -1.474814583819865632 ) ) ;
#1073=CARTESIAN_POINT ( 'NONE',  ( 79.98571111508536546, 66.33520038980104516, -1.398807481800599772 ) ) ;
#1076=CARTESIAN_POINT ( 'NONE',  ( 75.68633765818296411, 59.56198246982955169, -3.184487947857408408 ) ) ;
#1080=CARTESIAN_POINT ( 'NONE',  ( 75.51044298776176333, 62.93595297499960139, 3.562065002326824992 ) ) ;
#1082=CARTESIAN_POINT ( 'NONE',  ( -64.08758708074093136, 37.77454521956559574, 3.093244392761053785 ) ) ;
#1087=CARTESIAN_POINT ( 'NONE',  ( 80.30040509403158921, 65.99001427540439124, 2.270757614041262418 ) ) ;
#1095=CARTESIAN_POINT ( 'NONE',  ( 66.93722180744200045, 57.81789296588414118, 3.995856122844018810 ) ) ;
#1103=CIRCLE ( 'NONE', #32653, 67.42751648247021024 ) ;
#1106=CARTESIAN_POINT ( 'NONE',  ( -63.99293516169446150, 35.89893413629672381, 12.49999999999999645 ) ) ;
#1112=CARTESIAN_POINT ( 'NONE',  ( 67.36808046129075933, 58.37408278799862416, -3.989212576213368333 ) ) ;
#1114=VERTEX_POINT ( 'NONE', #9198 ) ;
#1117=CARTESIAN_POINT ( 'NONE',  ( -59.99245622168610481, 24.84364830758654463, 9.341017543843767257 ) ) ;
#1126=CARTESIAN_POINT ( 'NONE',  ( 79.14790672806259408, 65.85151465993942566, 2.407735119910381361 ) ) ;
#1129=CARTESIAN_POINT ( 'NONE',  ( 79.02450826907198689, 62.91033389078318550, -3.791687334209853599 ) ) ;
#1132=VECTOR ( 'NONE', #3813, 1000.000000000000000 ) ;
#1133=CARTESIAN_POINT ( 'NONE',  ( 79.91673984739684045, 65.77987873796998031, -2.647945256399896419 ) ) ;
#1134=CARTESIAN_POINT ( 'NONE',  ( 78.83212471655066622, 64.69929012837440041, 3.375657603866063727 ) ) ;
#1137=CARTESIAN_POINT ( 'NONE',  ( -1.432293644835494373, -27.47664038617742577, 1.000000000000000000 ) ) ;
#1138=CARTESIAN_POINT ( 'NONE',  ( 81.88789819931513136, 65.48572365615882518, 1.161365684106807850 ) ) ;
#1139=CARTESIAN_POINT ( 'NONE',  ( -63.70251272992033620, 44.36816940802074782, 1.449983087898546463 ) ) ;
#1141=CARTESIAN_POINT ( 'NONE',  ( -63.15778550246169232, 35.55392038829429424, -6.471101796987086985 ) ) ;
#1164=CARTESIAN_POINT ( 'NONE',  ( 66.83382626670835691, 58.02146702699413794, 3.998465113256441050 ) ) ;
#1178=CARTESIAN_POINT ( 'NONE',  ( 79.69769351933607027, 63.91149418591603393, -3.725738571856551662 ) ) ;
#1180=CARTESIAN_POINT ( 'NONE',  ( 78.73521632358557554, 65.70333808056840041, 2.340042473998457773 ) ) ;
#1186=DIRECTION ( 'NONE',  ( -1.000000000000000000, -3.905578250920211148E-15, 0.000000000000000000 ) ) ;
#1196=CARTESIAN_POINT ( 'NONE',  ( 81.31277617166799132, 62.04138461958081052, 2.639511535887547833 ) ) ;
#1209=CARTESIAN_POINT ( 'NONE',  ( 69.35860043680946774, 58.39594701590269921, 3.954017255840814649 ) ) ;
#1213=CARTESIAN_POINT ( 'NONE',  ( 80.83425215363003247, 63.04220640063321213, -3.443978770203981021 ) ) ;
#1217=CARTESIAN_POINT ( 'NONE',  ( -59.07422214908515201, 27.36241337473658319, 4.461357708502259101 ) ) ;
#1224=CARTESIAN_POINT ( 'NONE',  ( 80.93223178899225445, 61.91756539228702394, -2.804471013201356389 ) ) ;
#1226=CARTESIAN_POINT ( 'NONE',  ( 80.47318323629869496, 63.22351390842204211, 3.619557188109058021 ) ) ;
#1231=CARTESIAN_POINT ( 'NONE',  ( -58.64136512043187821, 29.17320997702626428, -5.450418868401677663 ) ) ;
#1234=CARTESIAN_POINT ( 'NONE',  ( -63.37350057586147045, 42.57076579999920796, -3.677910432553653131 ) ) ;
#1242=CARTESIAN_POINT ( 'NONE',  ( 81.48469013494974433, 61.56585122427133427, 1.622497907168700682 ) ) ;
#1245=AXIS2_PLACEMENT_3D ( 'NONE', #21698, #24156, #2774 ) ;
#1262=CARTESIAN_POINT ( 'NONE',  ( -62.89148181836064566, 37.17958841060804076, -4.327622075140624247 ) ) ;
#1264=ORIENTED_EDGE ( 'NONE', *, *, #31818, .F. ) ;
#1266=CARTESIAN_POINT ( 'NONE',  ( -58.49128007771433602, 30.53048970692593400, -5.009453334674668135 ) ) ;
#1271=CARTESIAN_POINT ( 'NONE',  ( 79.60403240858884999, 66.28972460246984610, -1.461108304022175730 ) ) ;
#1280=CARTESIAN_POINT ( 'NONE',  ( 76.54556538389320508, 62.22002718612346683, 3.872369636030853712 ) ) ;
#1286=CARTESIAN_POINT ( 'NONE',  ( -62.74545191947990475, 35.90010598104516504, 5.266623911128414548 ) ) ;
#1288=CARTESIAN_POINT ( 'NONE',  ( 81.40691186390338885, 61.43583663329575728, 1.251938014746357242 ) ) ;
#1307=CARTESIAN_POINT ( 'NONE',  ( 67.20175956769865877, 57.92120807820956685, -3.995511504169228179 ) ) ;
#1311=B_SPLINE_CURVE_WITH_KNOTS ( 'NONE', 3,
 ( #29663, #20585, #39943, #39326, #39736, #11310 ),
 .UNSPECIFIED., .F., .F.,
 ( 4, 2, 4 ),
 ( 0.000000000000000000, 0.001088541862127108796, 0.002177083724254217593 ),
 .UNSPECIFIED. ) ;
#1319=( NAMED_UNIT ( * ) SI_UNIT ( $, .STERADIAN. ) SOLID_ANGLE_UNIT ( ) );
#1321=CARTESIAN_POINT ( 'NONE',  ( 79.82117971689783076, 65.09389273565577128, 3.300462285847911570 ) ) ;
#1322=CARTESIAN_POINT ( 'NONE',  ( -63.24203369823550247, 41.86349869517832900, 3.933568017676808193 ) ) ;
#1324=CARTESIAN_POINT ( 'NONE',  ( 79.37220710802424151, 62.20501526703845485, -3.590127757398436703 ) ) ;
#1327=ADVANCED_FACE ( 'NONE', ( #20280 ), #4653, .T. ) ;
#1329=CARTESIAN_POINT ( 'NONE',  ( 81.64294641039653300, 62.46883698081568781, -2.647945256399892422 ) ) ;
#1330=CARTESIAN_POINT ( 'NONE',  ( 79.88615925706736220, 62.68050235454665398, 3.612066323963901482 ) ) ;
#1334=CARTESIAN_POINT ( 'NONE',  ( 80.37799020243589609, 66.31529150154187846, 1.204231967107850076 ) ) ;
#1336=CARTESIAN_POINT ( 'NONE',  ( -64.08758708074093136, 42.98467135419826235, 2.320054402708805696 ) ) ;
#1338=CARTESIAN_POINT ( 'NONE',  ( -64.08758708074093136, 35.87095250353018372, -3.952250494627737254 ) ) ;
#1351=EDGE_CURVE ( 'NONE', #38060, #32211, #36785, .T. ) ;
#1355=B_SPLINE_CURVE_WITH_KNOTS ( 'NONE', 3,
 ( #17928, #2115, #15258, #21240 ),
 .UNSPECIFIED., .F., .F.,
 ( 4, 4 ),
 ( 0.0002401580581033240186, 0.001136201907775618225 ),
 .UNSPECIFIED. ) ;
#1359=CARTESIAN_POINT ( 'NONE',  ( 66.42000668879826719, 57.79655248154880098, 4.000000000000015987 ) ) ;
#1360=CARTESIAN_POINT ( 'NONE',  ( 73.23371602657820745, 61.99063567959824184, -3.556895493546552878 ) ) ;
#1362=CARTESIAN_POINT ( 'NONE',  ( -64.08758708074093136, 38.13199975834322686, 3.043809435734686097 ) ) ;
#1369=CARTESIAN_POINT ( 'NONE',  ( -74.92283640148291113, 18.87330372387140187, -46.17089178453873188 ) ) ;
#1371=EDGE_CURVE ( 'NONE', #12043, #1373, #9301, .T. ) ;
#1373=VERTEX_POINT ( 'NONE', #27276 ) ;
#1374=CARTESIAN_POINT ( 'NONE',  ( 80.80054865964804378, 61.51733283104052674, -2.392122129321803126 ) ) ;
#1376=CARTESIAN_POINT ( 'NONE',  ( 78.96934220494367196, 65.43027598480411200, 2.854164747637875976 ) ) ;
#1377=DIRECTION ( 'NONE',  ( -0.4690749385695646145, -0.8831583674551010121, -3.445651357372585989E-15 ) ) ;
#1390=CARTESIAN_POINT ( 'NONE',  ( 79.37790743583137498, 65.75409067367344562, 2.639511535887585136 ) ) ;
#1393=DIRECTION ( 'NONE',  ( -0.4582725098355734938, 0.8888117386314180468, -0.000000000000000000 ) ) ;
#1396=AXIS2_PLACEMENT_3D ( 'NONE', #31980, #35078, #19006 ) ;
#1400=CARTESIAN_POINT ( 'NONE',  ( 68.43818535210665743, 59.05932329210152432, 3.950303728398547598 ) ) ;
#1403=CARTESIAN_POINT ( 'NONE',  ( 1.847632973160104664, 12.44248440543094958, 4.000000000000000000 ) ) ;
#1405=CARTESIAN_POINT ( 'NONE',  ( 78.97731087898851854, 65.91669204587326192, -2.137206601789619409 ) ) ;
#1415=CARTESIAN_POINT ( 'NONE',  ( 80.97304215327341126, 61.92799980795002313, -2.787474064117368311 ) ) ;
#1417=CARTESIAN_POINT ( 'NONE',  ( 78.88238753611518916, 65.83802744495456238, 2.215902410107951415 ) ) ;
#1428=CARTESIAN_POINT ( 'NONE',  ( -63.55798368792363107, 43.57337240874115736, -2.980826430635752367 ) ) ;
#1436=CARTESIAN_POINT ( 'NONE',  ( 81.48104477344870133, 62.99720032632000510, 3.089171411838275372 ) ) ;
#1455=CARTESIAN_POINT ( 'NONE',  ( 66.27376694609004915, 57.73522568913436004, -4.000000000000000000 ) ) ;
#1466=CARTESIAN_POINT ( 'NONE',  ( 82.11700085695680684, 62.19713100941778805, -1.465650077276901886 ) ) ;
#1469=ORIENTED_EDGE ( 'NONE', *, *, #38773, .T. ) ;
#1473=CARTESIAN_POINT ( 'NONE',  ( 75.50377651103727317, 61.49872921062497255, 3.901127667181019110 ) ) ;
#1480=CARTESIAN_POINT ( 'NONE',  ( 80.57628295459070955, 65.85481838934502719, 2.430878896394115696 ) ) ;
#1485=AXIS2_PLACEMENT_3D ( 'NONE', #33810, #5590, #30721 ) ;
#1493=CARTESIAN_POINT ( 'NONE',  ( -63.70768058868310391, 44.39675795731060504, -1.424602271588051527 ) ) ;
#1494=EDGE_CURVE ( 'NONE', #25777, #31697, #32744, .T. ) ;
#1500=CARTESIAN_POINT ( 'NONE',  ( 67.09515986712425217, 58.21407947277521089, -3.993497817183391696 ) ) ;
#1514=CARTESIAN_POINT ( 'NONE',  ( 81.12411360294466078, 61.28734817074503383, 1.205449537698832563 ) ) ;
#1515=CARTESIAN_POINT ( 'NONE',  ( -63.16614402916191295, 41.45853387640750753, 4.000000000000003553 ) ) ;
#1518=CARTESIAN_POINT ( 'NONE',  ( 79.68931684371919744, 62.31783030446535321, -3.554489553981595051 ) ) ;
#1521=CARTESIAN_POINT ( 'NONE',  ( 81.64001200211806974, 62.74592715520643793, -2.852119850606562590 ) ) ;
#1522=CARTESIAN_POINT ( 'NONE',  ( 78.56694041390316841, 64.50177951359142980, 3.424416364708430027 ) ) ;
#1524=CARTESIAN_POINT ( 'NONE',  ( 81.32357852907315987, 65.91643957835155732, 1.421283058690022916 ) ) ;
#1527=CARTESIAN_POINT ( 'NONE',  ( -64.72110749213814529, 34.74377494905899511, -6.240054254828758751 ) ) ;
#1545=ORIENTED_EDGE ( 'NONE', *, *, #25757, .F. ) ;
#1548=CARTESIAN_POINT ( 'NONE',  ( 66.42693215277247987, 57.77698748017490971, 4.000000000000009770 ) ) ;
#1550=CARTESIAN_POINT ( 'NONE',  ( 72.21306447944246543, 59.67152943164661849, -3.942504219364093121 ) ) ;
#1559=CARTESIAN_POINT ( 'NONE',  ( 25.11437021580303863, 164.7550792202006562, -1.000000000000000000 ) ) ;
#1564=CARTESIAN_POINT ( 'NONE',  ( 79.54992950373222982, 64.18601594420306355, -3.671038198312436496 ) ) ;
#1567=CARTESIAN_POINT ( 'NONE',  ( 78.51047153333163919, 65.93088068117918965, 1.448968528257593258 ) ) ;
#1575=CARTESIAN_POINT ( 'NONE',  ( 76.46955312333206223, 64.49609874770474960, -2.565500891477647816 ) ) ;
#1582=CARTESIAN_POINT ( 'NONE',  ( 80.54433603269386310, 64.00140174820366212, 3.588566286536281957 ) ) ;
#1595=CARTESIAN_POINT ( 'NONE',  ( 67.63028434841179148, 58.56128740577801750, 3.979762160777183588 ) ) ;
#1598=DIRECTION ( 'NONE',  ( -0.000000000000000000, -0.000000000000000000, -1.000000000000000000 ) ) ;
#1600=CARTESIAN_POINT ( 'NONE',  ( 80.95271419388603817, 62.75148163162413795, -3.324099845469154602 ) ) ;
#1610=CARTESIAN_POINT ( 'NONE',  ( 79.84444348018388382, 64.37461814510197655, -3.624000857162082312 ) ) ;
#1612=CARTESIAN_POINT ( 'NONE',  ( 81.08254763934547782, 61.27217476014467934, 1.284346554836957255 ) ) ;
#1629=CARTESIAN_POINT ( 'NONE',  ( 79.86705713781546478, 65.75210810415633489, 2.684801069578925947 ) ) ;
#1633=CARTESIAN_POINT ( 'NONE',  ( -66.99872204295122913, 28.48507918597134037, 9.800414904976365804 ) ) ;
#1649=EDGE_CURVE ( 'NONE', #31697, #33979, #39393, .T. ) ;
#1655=CARTESIAN_POINT ( 'NONE',  ( 66.27376694609004915, 57.73522568913436004, -4.000000000000000000 ) ) ;
#1657=ORIENTED_EDGE ( 'NONE', *, *, #38294, .F. ) ;
#1658=ORIENTED_EDGE ( 'NONE', *, *, #14390, .F. ) ;
#1666=VERTEX_POINT ( 'NONE', #17903 ) ;
#1668=CARTESIAN_POINT ( 'NONE',  ( 81.32635356316018260, 65.55379304840796806, -2.259066313178065943 ) ) ;
#1677=CARTESIAN_POINT ( 'NONE',  ( 75.52602547247359155, 59.92744485144773137, 3.494507759123859358 ) ) ;
#1680=CARTESIAN_POINT ( 'NONE',  ( -62.85296432946437051, 36.91960874151882166, 4.452026683638354854 ) ) ;
#1684=CARTESIAN_POINT ( 'NONE',  ( -63.08379346057677139, 18.80112958435941906, 9.800414904976365804 ) ) ;
#1686=CARTESIAN_POINT ( 'NONE',  ( 81.88652354500527508, 62.08144837224595847, 1.918505602738378224 ) ) ;
#1692=LINE ( 'NONE', #14225, #34172 ) ;
#1695=DIRECTION ( 'NONE',  ( -0.9267318687906771491, 0.3757233601570964532, 0.000000000000000000 ) ) ;
#1705=CARTESIAN_POINT ( 'NONE',  ( 67.13068300324758297, 58.11650739856835202, -3.998197261021420701 ) ) ;
#1706=VECTOR ( 'NONE', #19916, 1000.000000000000000 ) ;
#1718=CARTESIAN_POINT ( 'NONE',  ( 80.80454364895454944, 63.02910633771583093, 3.452358620554646151 ) ) ;
#1719=CARTESIAN_POINT ( 'NONE',  ( -63.68563422865328505, 44.27494078859859883, 1.828866361102486238 ) ) ;
#1721=CARTESIAN_POINT ( 'NONE',  ( 77.96902425052306285, 62.15836910947902538, -3.808649511194685200 ) ) ;
#1725=CARTESIAN_POINT ( 'NONE',  ( 78.68416471612006546, 66.05417514313620586, -1.083735637652206485 ) ) ;
#1727=CARTESIAN_POINT ( 'NONE',  ( 79.47877296666170821, 61.98342160143343449, 3.470679136763286099 ) ) ;
#1730=VECTOR ( 'NONE', #27504, 1000.000000000000000 ) ;
#1731=CARTESIAN_POINT ( 'NONE',  ( 80.34788146105277917, 66.29920961842019267, 1.394285451509447382 ) ) ;
#1732=CARTESIAN_POINT ( 'NONE',  ( -81.07947155388369254, 30.81399289130168384, 9.800414904976365804 ) ) ;
#1734=CARTESIAN_POINT ( 'NONE',  ( -64.08758708074091714, 36.87876644325631759, -4.900609702795900802 ) ) ;
#1745=DIRECTION ( 'NONE',  ( 0.000000000000000000, -1.000000000000000000, 0.000000000000000000 ) ) ;
#1746=DIRECTION ( 'NONE',  ( 1.000000000000000000, 0.000000000000000000, 0.000000000000000000 ) ) ;
#1747=DIRECTION ( 'NONE',  ( 0.000000000000000000, 0.000000000000000000, 1.000000000000000000 ) ) ;
#1753=ORIENTED_EDGE ( 'NONE', *, *, #35951, .F. ) ;
#1754=CARTESIAN_POINT ( 'NONE',  ( 66.27376694608996388, 57.73522568913447373, 4.000000000000000000 ) ) ;
#1755=CARTESIAN_POINT ( 'NONE',  ( 71.00148000485552302, 59.33579794997937995, -3.971832046809253391 ) ) ;
#1768=CARTESIAN_POINT ( 'NONE',  ( 79.42292528565204179, 64.10449580132841163, -3.686141857899477348 ) ) ;
#1771=CARTESIAN_POINT ( 'NONE',  ( 80.75052706852349615, 61.66721672131043874, 2.660933152496148590 ) ) ;
#1787=CARTESIAN_POINT ( 'NONE',  ( 81.26385631823474398, 62.29349618781995446, 2.861733672647093218 ) ) ;
#1793=VECTOR ( 'NONE', #32468, 1000.000000000000114 ) ;
#1800=CARTESIAN_POINT ( 'NONE',  ( 67.36808046129075933, 58.37408278799862416, 3.989212576213369221 ) ) ;
#1802=VERTEX_POINT ( 'NONE', #25532 ) ;
#1805=CARTESIAN_POINT ( 'NONE',  ( 80.71579011337402676, 63.33293116964227920, -3.563857694938807885 ) ) ;
#1809=CARTESIAN_POINT ( 'NONE',  ( -58.36416262933997245, 28.31210393328042585, 5.221062780410256288 ) ) ;
#1817=CARTESIAN_POINT ( 'NONE',  ( 79.68769792879572833, 64.63763403318208134, -3.508091314521180504 ) ) ;
#1821=CARTESIAN_POINT ( 'NONE',  ( 79.68769792879609781, 64.63763403318228029, 3.508091314521096127 ) ) ;
#1827=CARTESIAN_POINT ( 'NONE',  ( 75.27660179239936156, 61.98686977074611804, -3.846775394605563392 ) ) ;
#1837=EDGE_CURVE ( 'NONE', #21757, #26563, #23390, .T. ) ;
#1839=FACE_OUTER_BOUND ( 'NONE', #19988, .T. ) ;
#1841=CARTESIAN_POINT ( 'NONE',  ( 81.30751890104828306, 61.38951540425497200, 1.382728580145337505 ) ) ;
#1859=ORIENTED_EDGE ( 'NONE', *, *, #26010, .F. ) ;
#1867=EDGE_LOOP ( 'NONE', ( #38659, #24476, #2163, #38591 ) ) ;
#1871=CARTESIAN_POINT ( 'NONE',  ( -56.22749146662674491, 30.67773648377160001, -3.904540345294674530 ) ) ;
#1877=CARTESIAN_POINT ( 'NONE',  ( 80.49077247797903567, 66.09228938494860017, -1.971256063808603631 ) ) ;
#1879=DIRECTION ( 'NONE',  ( 0.000000000000000000, 0.000000000000000000, 1.000000000000000000 ) ) ;
#1884=CARTESIAN_POINT ( 'NONE',  ( 75.05654786057638717, 62.45444674818786268, 3.685888554891597835 ) ) ;
#1887=CARTESIAN_POINT ( 'NONE',  ( -64.08758708074093136, 37.74469198210200460, 4.273126118784214889 ) ) ;
#1893=CARTESIAN_POINT ( 'NONE',  ( -62.75245724414897808, 36.25555358314721843, 4.889260473756201542 ) ) ;
#1896=CARTESIAN_POINT ( 'NONE',  ( 81.44289297360093371, 64.86039221060747195, 2.864610283900509202 ) ) ;
#1905=CYLINDRICAL_SURFACE ( 'NONE', #1033, 5.000000000000000000 ) ;
#1912=CARTESIAN_POINT ( 'NONE',  ( -64.08758708074091714, 38.34299140179737719, -3.014629887201876635 ) ) ;
#1913=CARTESIAN_POINT ( 'NONE',  ( 67.62039053056824400, 58.58799842263783120, -3.976226663256291260 ) ) ;
#1919=CARTESIAN_POINT ( 'NONE',  ( 76.98045162513071205, 64.85275298426677182, 2.378822723470982670 ) ) ;
#1925=CARTESIAN_POINT ( 'NONE',  ( 81.16955088369260807, 61.30397035488353197, -1.005837412005794906 ) ) ;
#1926=CARTESIAN_POINT ( 'NONE',  ( 80.09489858828513320, 64.52483703883090982, 3.563857694938804777 ) ) ;
#1930=CARTESIAN_POINT ( 'NONE',  ( 79.26553226962353449, 61.67928659302132388, -3.361664161258277161 ) ) ;
#1935=CARTESIAN_POINT ( 'NONE',  ( 81.13122672739170582, 64.30755116178544029, -3.292658836668130640 ) ) ;
#1936=CARTESIAN_POINT ( 'NONE',  ( 77.83481221125374816, 64.51125116100621426, 3.218236826935550798 ) ) ;
#1941=CARTESIAN_POINT ( 'NONE',  ( 81.46190421581952990, 61.46294189193149293, 1.114595100209201162 ) ) ;
#1947=ORIENTED_EDGE ( 'NONE', *, *, #5919, .T. ) ;
#1952=LINE ( 'NONE', #5630, #5998 ) ;
#1957=CARTESIAN_POINT ( 'NONE',  ( -11.81496944966682960, -21.25669541281728669, 4.000000000000000000 ) ) ;
#1965=ORIENTED_EDGE ( 'NONE', *, *, #36863, .T. ) ;
#1967=CARTESIAN_POINT ( 'NONE',  ( 66.41703863280932296, 57.80493748213761762, 4.000000000000019540 ) ) ;
#1968=CARTESIAN_POINT ( 'NONE',  ( 73.73614897715009420, 59.29615633563123822, -3.619654763491260585 ) ) ;
#1974=EDGE_LOOP ( 'NONE', ( #15030, #13071, #3505, #26512, #37227 ) ) ;
#1981=CARTESIAN_POINT ( 'NONE',  ( 79.60839748543872929, 63.85977214187242623, -3.734652355492745102 ) ) ;
#1983=CARTESIAN_POINT ( 'NONE',  ( 80.42678074443124103, 62.56544727678166140, 3.449595662144092412 ) ) ;
#1988=CARTESIAN_POINT ( 'NONE',  ( -105.6213936588467135, -59.15536422891795354, 9.800414904976365804 ) ) ;
#1998=CARTESIAN_POINT ( 'NONE',  ( 79.68007496026341130, 65.35156779369863500, 3.108243619504650113 ) ) ;
#1999=CARTESIAN_POINT ( 'NONE',  ( -69.08758708074093136, 35.93730870640389696, -8.800414904976364028 ) ) ;
#2000=CARTESIAN_POINT ( 'NONE',  ( -63.08758708074094557, 43.61223004741321319, -1.000000000000000000 ) ) ;
#2003=CARTESIAN_POINT ( 'NONE',  ( -64.24852075262772644, 34.84521132811198640, 5.064982173168631086 ) ) ;
#2007=CARTESIAN_POINT ( 'NONE',  ( 67.37599051809213790, 58.35250968650521486, 3.990882853436548139 ) ) ;
#2022=CARTESIAN_POINT ( 'NONE',  ( 80.81138441778081472, 62.13752223189714385, -3.030715982579941681 ) ) ;
#2024=CARTESIAN_POINT ( 'NONE',  ( 79.49051211673885575, 64.87125159350641468, 3.403428918328328834 ) ) ;
#2029=CARTESIAN_POINT ( 'NONE',  ( 74.43259725886051115, 60.83706718145764114, -3.924711207976804950 ) ) ;
#2030=CARTESIAN_POINT ( 'NONE',  ( -81.07947155388369254, 30.81399289130168384, 12.49999999999999645 ) ) ;
#2044=CARTESIAN_POINT ( 'NONE',  ( 81.58232553938692888, 62.71761900942991730, 2.892908819267544729 ) ) ;
#2061=ORIENTED_EDGE ( 'NONE', *, *, #9157, .T. ) ;
#2062=VERTEX_POINT ( 'NONE', #10800 ) ;
#2069=CYLINDRICAL_SURFACE ( 'NONE', #777, 2.500000000000002220 ) ;
#2077=CARTESIAN_POINT ( 'NONE',  ( 79.19089293128583051, 65.62284279856319813, -2.735335646780913788 ) ) ;
#2078=CARTESIAN_POINT ( 'NONE',  ( -58.91453996558632156, 28.99622802882459638, -6.206785453512805972 ) ) ;
#2083=CARTESIAN_POINT ( 'NONE',  ( 81.66247121191628366, 61.65231731326586839, -1.378120381825870266 ) ) ;
#2089=CARTESIAN_POINT ( 'NONE',  ( 76.25423822322979106, 59.84407948384421161, 3.204585025132129950 ) ) ;
#2092=DIRECTION ( 'NONE',  ( -1.000000000000000000, 0.000000000000000000, 0.000000000000000000 ) ) ;
#2093=CARTESIAN_POINT ( 'NONE',  ( -66.22295697853020613, 35.49170696305580464, 7.967283012326582536 ) ) ;
#2094=CARTESIAN_POINT ( 'NONE',  ( 81.00802433895704269, 65.38516391083565793, 2.726953404243151802 ) ) ;
#2097=DIRECTION ( 'NONE',  ( 1.000000000000000000, 0.000000000000000000, 0.000000000000000000 ) ) ;
#2113=CARTESIAN_POINT ( 'NONE',  ( 66.98823442903206171, 58.05250069757015297, -3.998791315154375692 ) ) ;
#2115=CARTESIAN_POINT ( 'NONE',  ( -58.99872204295123623, 28.26327478256400383, -6.631997745857265869 ) ) ;
#2126=CARTESIAN_POINT ( 'NONE',  ( 82.44648106056945380, 62.87232481290443076, -1.233992409460997308 ) ) ;
#2127=CARTESIAN_POINT ( 'NONE',  ( 81.02087009143654939, 62.46468763289096415, 3.155412080370043615 ) ) ;
#2130=CARTESIAN_POINT ( 'NONE',  ( 79.17274970258590372, 61.87635977960857758, -3.505091495581010630 ) ) ;
#2133=CARTESIAN_POINT ( 'NONE',  ( 81.15996319168233697, 61.30045982539696325, -1.094381639753446045 ) ) ;
#2134=CARTESIAN_POINT ( 'NONE',  ( 79.37220710802424151, 62.20501526703846906, 3.590127757398436259 ) ) ;
#2138=CARTESIAN_POINT ( 'NONE',  ( 82.33093480182121482, 62.53300266214105108, 1.299258709308648729 ) ) ;
#2139=CARTESIAN_POINT ( 'NONE',  ( -75.45330471031414277, 33.71485196875532608, -8.800414904976364028 ) ) ;
#2143=DIRECTION ( 'NONE',  ( 0.000000000000000000, 0.000000000000000000, 1.000000000000000000 ) ) ;
#2158=CYLINDRICAL_SURFACE ( 'NONE', #40412, 7.999999999999986677 ) ;
#2163=ORIENTED_EDGE ( 'NONE', *, *, #8162, .T. ) ;
#2164=CARTESIAN_POINT ( 'NONE',  ( 66.27376694608996388, 57.73522568913447373, 4.000000000000000000 ) ) ;
#2165=CARTESIAN_POINT ( 'NONE',  ( 69.13527637438681950, 58.97494527044376866, -3.984982412582154687 ) ) ;
#2172=CARTESIAN_POINT ( 'NONE',  ( 17.97454669799173033, 51.66243977840390045, 1.000000000000000000 ) ) ;
#2174=( BOUNDED_SURFACE ( )  B_SPLINE_SURFACE ( 3, 2, ( 
 ( #12198, #3187, #22309 ),
 ( #15905, #28464, #271 ),
 ( #25383, #15493, #25177 ),
 ( #37315, #12811, #21688 ),
 ( #24559, #19201, #9309 ),
 ( #28253, #34266, #18373 ),
 ( #6037, #79, #34876 ),
 ( #37923, #31767, #15083 ),
 ( #27644, #28053, #37708 ),
 ( #40200, #11981, #37113 ),
 ( #18572, #8899, #2974 ),
 ( #31158, #21887, #37514 ),
 ( #21482, #40602, #34465 ),
 ( #12610, #9517, #22098 ),
 ( #34060, #30960, #2765 ),
 ( #20199, #35075, #3581 ) ),
 .UNSPECIFIED., .F., .F., .F. ) 
 B_SPLINE_SURFACE_WITH_KNOTS ( ( 4, 2, 2, 2, 2, 2, 2, 4 ),
 ( 3, 3 ),
 ( 7.589415207398531038E-18, 0.0009755768803159603443, 0.001463365320473936776, 0.001951153760631913099, 0.002438942200789889422, 0.002926730640947865746, 0.003414519081105842069, 0.003902307521263818826 ),
 ( 0.000000000000000000, 1.000000000000000000 ),
 .UNSPECIFIED. ) 
 GEOMETRIC_REPRESENTATION_ITEM ( )  RATIONAL_B_SPLINE_SURFACE ( (
 ( 1.000000000000000000, 0.6029302108204158683, 1.000000000000000000),
 ( 1.000000000000000000, 0.5783298881757151788, 1.000000000000000000),
 ( 1.000000000000000000, 0.5522465926628815636, 1.000000000000000000),
 ( 1.000000000000000000, 0.5169885426013864915, 1.000000000000000000),
 ( 1.000000000000000000, 0.5061025709684146001, 1.000000000000000000),
 ( 1.000000000000000000, 0.4881721342722146750, 1.000000000000000000),
 ( 1.000000000000000000, 0.4810711757772043184, 1.000000000000000000),
 ( 1.000000000000000000, 0.4726640060677125832, 1.000000000000000000),
 ( 1.000000000000000000, 0.4715283203431503423, 1.000000000000000000),
 ( 1.000000000000000000, 0.4761415489114605992, 1.000000000000000000),
 ( 1.000000000000000000, 0.4818043763597624762, 1.000000000000000000),
 ( 1.000000000000000000, 0.4989518560459819119, 1.000000000000000000),
 ( 1.000000000000000000, 0.5102645520264953438, 1.000000000000000000),
 ( 1.000000000000000000, 0.5358562791028443906, 1.000000000000000000),
 ( 1.000000000000000000, 0.5501980292661390326, 1.000000000000000000),
 ( 1.000000000000000000, 0.5652620711642688534, 1.000000000000000000) ) ) 
 REPRESENTATION_ITEM ( '' )  SURFACE ( )  );
#2178=CARTESIAN_POINT ( 'NONE',  ( -69.08758708074093136, 24.84364830758653397, -3.800414904976364028 ) ) ;
#2180=CARTESIAN_POINT ( 'NONE',  ( 79.46360196572365453, 64.13050462409741215, -3.681573067026198576 ) ) ;
#2182=CARTESIAN_POINT ( 'NONE',  ( 81.80618415539481703, 63.87961589575506594, -2.903340743335492302 ) ) ;
#2183=CARTESIAN_POINT ( 'NONE',  ( 80.80786883982545987, 61.35646782832052537, 2.148686496494744080 ) ) ;
#2189=ORIENTED_EDGE ( 'NONE', *, *, #29979, .F. ) ;
#2201=CIRCLE ( 'NONE', #35737, 6.681288188914807691 ) ;
#2206=CARTESIAN_POINT ( 'NONE',  ( 68.05544300132015678, 58.31078564718745127, 3.995571880668738363 ) ) ;
#2215=CARTESIAN_POINT ( 'NONE',  ( -63.08379346057677139, 18.80112958435941906, -9.800414904976365804 ) ) ;
#2221=CARTESIAN_POINT ( 'NONE',  ( 80.48752863069321961, 62.90068369996134834, -3.525318766974259166 ) ) ;
#2223=CARTESIAN_POINT ( 'NONE',  ( 79.17340063025110908, 65.28954359503943294, 3.030715982579951451 ) ) ;
#2229=CARTESIAN_POINT ( 'NONE',  ( 73.86803306573551708, 62.08347648694399368, -3.642458757454824614 ) ) ;
#2230=VECTOR ( 'NONE', #34040, 1000.000000000000000 ) ;
#2235=CARTESIAN_POINT ( 'NONE',  ( -69.08758708074093136, 36.88538962427716683, 8.800414904976364028 ) ) ;
#2242=CARTESIAN_POINT ( 'NONE',  ( 28.52663967383706023, 50.14399159706750453, 1.000000000000000000 ) ) ;
#2244=CARTESIAN_POINT ( 'NONE',  ( 81.40528610411782040, 61.52959015154564071, 1.692865493182717840 ) ) ;
#2252=CARTESIAN_POINT ( 'NONE',  ( -63.99293516169446150, 35.89893413629673091, -7.506047544094580637 ) ) ;
#2261=CARTESIAN_POINT ( 'NONE',  ( 81.29039616289740877, 62.30485139745669443, -2.850064543546689588 ) ) ;
#2268=CARTESIAN_POINT ( 'NONE',  ( -69.08758708074093136, 24.84364830758653397, 8.800414904976364028 ) ) ;
#2273=CARTESIAN_POINT ( 'NONE',  ( 80.99158576241018181, 62.18982880056436358, -2.968223699503256263 ) ) ;
#2274=CARTESIAN_POINT ( 'NONE',  ( 27.60344192425479193, 81.15229837709949834, 1.000000000000000000 ) ) ;
#2279=CARTESIAN_POINT ( 'NONE',  ( 82.23158145857209433, 63.37565065107707341, -2.326649614738084182 ) ) ;
#2286=CARTESIAN_POINT ( 'NONE',  ( 75.65523814419378823, 61.17064132828575396, 3.882889210543257974 ) ) ;
#2292=ORIENTED_EDGE ( 'NONE', *, *, #7895, .T. ) ;
#2294=CARTESIAN_POINT ( 'NONE',  ( 82.01382571621898876, 63.62535219989236168, 2.645340681430091045 ) ) ;
#2315=CARTESIAN_POINT ( 'NONE',  ( 66.83382626670835691, 58.02146702699413794, -3.998465113256441938 ) ) ;
#2320=AXIS2_PLACEMENT_3D ( 'NONE', #2000, #26494, #7745 ) ;
#2331=CARTESIAN_POINT ( 'NONE',  ( 81.96779975749585390, 61.96402392828839822, -1.065376284871803581 ) ) ;
#2332=CARTESIAN_POINT ( 'NONE',  ( 79.09180288389933366, 65.81009211479097587, 2.442092683901131434 ) ) ;
#2335=ORIENTED_EDGE ( 'NONE', *, *, #10534, .T. ) ;
#2336=CARTESIAN_POINT ( 'NONE',  ( 78.44508438210819179, 62.63916802445879028, -3.816136337383043919 ) ) ;
#2339=CARTESIAN_POINT ( 'NONE',  ( 80.95699988732381769, 64.21667718577664630, -3.402511877377342842 ) ) ;
#2341=CARTESIAN_POINT ( 'NONE',  ( 80.20105671851041507, 61.18620973470589064, 2.431999527814463935 ) ) ;
#2347=CARTESIAN_POINT ( 'NONE',  ( 81.73112818161185089, 61.68666564161353705, 1.174937739208268050 ) ) ;
#2359=FACE_OUTER_BOUND ( 'NONE', #18590, .T. ) ;
#2377=CARTESIAN_POINT ( 'NONE',  ( 69.97231107847817100, 58.54512925548123548, -3.931953536312680964 ) ) ;
#2385=CARTESIAN_POINT ( 'NONE',  ( -60.81661347076554591, 25.20155461598436375, -9.800414904976365804 ) ) ;
#2392=CARTESIAN_POINT ( 'NONE',  ( 80.15282788578683437, 62.77883523856217352, -3.578491385641961120 ) ) ;
#2394=CARTESIAN_POINT ( 'NONE',  ( 81.62235710223383478, 64.17388774702364174, -3.017922835037758489 ) ) ;
#2395=CARTESIAN_POINT ( 'NONE',  ( 78.57218090866955151, 65.76747258267620566, 2.123311106147464322 ) ) ;
#2396=EDGE_CURVE ( 'NONE', #39470, #16748, #16094, .T. ) ;
#2400=B_SPLINE_CURVE_WITH_KNOTS ( 'NONE', 3,
 ( #35693, #20221, #17122, #4783, #29896, #14241, #11145, #23714, #17514, #30110, #1919, #14845, #30729, #39769, #15464, #2534, #36679, #11745, #8461, #9281, #24114, #33617, #33817, #30933, #2947, #30514, #6213, #24530 ),
 .UNSPECIFIED., .F., .F.,
 ( 4, 2, 2, 2, 2, 2, 2, 2, 2, 2, 2, 2, 2, 4 ),
 ( 2.168404344971008868E-19, 0.0002510493512354818220, 0.0005020987024709634271, 0.001004197404941950707, 0.002008394809883904883, 0.003012592214825858192, 0.004016789619767812368, 0.006025184429651660872, 0.008033579239535510244, 0.01205036885930323327, 0.01405876366918711907, 0.01506296107412906024, 0.01556505977660003169, 0.01606715847907100314 ),
 .UNSPECIFIED. ) ;
#2416=DIRECTION ( 'NONE',  ( 0.000000000000000000, 0.000000000000000000, 1.000000000000000000 ) ) ;
#2424=CARTESIAN_POINT ( 'NONE',  ( 67.83896914621323049, 57.99724189137371155, 3.982857479566772607 ) ) ;
#2434=CARTESIAN_POINT ( 'NONE',  ( -69.08758708074093136, 24.84364830758653397, 3.800414904976363140 ) ) ;
#2439=EDGE_LOOP ( 'NONE', ( #15197, #32066, #23804, #27519 ) ) ;
#2440=CARTESIAN_POINT ( 'NONE',  ( 79.20065834867790500, 65.31285345095534467, -3.018898740118490576 ) ) ;
#2442=CARTESIAN_POINT ( 'NONE',  ( 78.70885197775000108, 65.89012877898849752, 1.994058748902171940 ) ) ;
#2444=CARTESIAN_POINT ( 'NONE',  ( -68.71186372058383540, 37.81212149306784909, 9.800414904976364028 ) ) ;
#2446=CARTESIAN_POINT ( 'NONE',  ( 73.92749824250802249, 61.95374747488791201, -3.708893976703420137 ) ) ;
#2456=CIRCLE ( 'NONE', #12296, 95.38357402481355507 ) ;
#2462=CARTESIAN_POINT ( 'NONE',  ( 79.48860182481728032, 65.82309781974731777, 2.578835243349295148 ) ) ;
#2477=CARTESIAN_POINT ( 'NONE',  ( 79.73516162904324744, 65.38506083608318420, -3.083955809406671467 ) ) ;
#2489=CARTESIAN_POINT ( 'NONE',  ( 80.51591231855056208, 63.60920045316173344, -3.640670270625564253 ) ) ;
#2490=CARTESIAN_POINT ( 'NONE',  ( -58.69259491913187787, 29.82092612118092489, -5.479210374447095688 ) ) ;
#2494=CARTESIAN_POINT ( 'NONE',  ( 81.93064166251112113, 62.10341262211372992, -1.859759604986998882 ) ) ;
#2500=CARTESIAN_POINT ( 'NONE',  ( 73.18282872914367942, 62.10277071170013841, 3.478821770299028948 ) ) ;
#2509=CARTESIAN_POINT ( 'NONE',  ( 81.16598293928451824, 61.30266375757629049, 1.057717897339646163 ) ) ;
#2519=FACE_OUTER_BOUND ( 'NONE', #33487, .T. ) ;
#2520=DIRECTION ( 'NONE',  ( 0.000000000000000000, 0.000000000000000000, 1.000000000000000000 ) ) ;
#2525=CARTESIAN_POINT ( 'NONE',  ( -11.81496944966682960, -21.25669541281728669, -1.000000000000000000 ) ) ;
#2527=CARTESIAN_POINT ( 'NONE',  ( 67.00300875778714271, 58.01168839481970707, -3.999354069328931782 ) ) ;
#2530=AXIS2_PLACEMENT_3D ( 'NONE', #10971, #23551, #33449 ) ;
#2534=CARTESIAN_POINT ( 'NONE',  ( 73.85944157702037671, 62.69931772841422202, 3.253003066526747755 ) ) ;
#2539=CARTESIAN_POINT ( 'NONE',  ( 79.68852728668518637, 66.33522678087791746, -1.065376284871803803 ) ) ;
#2541=CARTESIAN_POINT ( 'NONE',  ( 80.56654867478538051, 63.26449302893301052, 3.600689860192759717 ) ) ;
#2544=CARTESIAN_POINT ( 'NONE',  ( 78.51266523469813308, 61.01400193535545213, -3.220231295875733757 ) ) ;
#2547=CARTESIAN_POINT ( 'NONE',  ( 81.47459903045408680, 62.11139297693658534, -2.556731990913030828 ) ) ;
#2549=CARTESIAN_POINT ( 'NONE',  ( 79.57681890279650361, 60.99726435378330081, 2.643019404357117352 ) ) ;
#2554=CARTESIAN_POINT ( 'NONE',  ( 81.46991160412491695, 61.46693516840312554, 1.070820504726896827 ) ) ;
#2566=CARTESIAN_POINT ( 'NONE',  ( 80.01459546602684725, 60.89228396117896835, 2.037903991281934335 ) ) ;
#2570=DIRECTION ( 'NONE',  ( 0.000000000000000000, 0.000000000000000000, 1.000000000000000000 ) ) ;
#2581=VERTEX_POINT ( 'NONE', #12796 ) ;
#2583=CARTESIAN_POINT ( 'NONE',  ( 69.48201546320520094, 59.78788955577742570, -3.863726395435664873 ) ) ;
#2588=CARTESIAN_POINT ( 'NONE',  ( 70.04419837359742473, 58.36171959603688464, 3.883859131414874710 ) ) ;
#2594=CARTESIAN_POINT ( 'NONE',  ( -75.45330471031414277, 33.71485196875532608, -46.17089178453873188 ) ) ;
#2602=CARTESIAN_POINT ( 'NONE',  ( 80.39157904934594967, 62.27158585385627987, -3.322373183921394801 ) ) ;
#2604=CARTESIAN_POINT ( 'NONE',  ( 81.86163085503896752, 62.85586669281862982, -2.670779692148389728 ) ) ;
#2605=CARTESIAN_POINT ( 'NONE',  ( 79.79522905248630593, 63.61080392591205168, 3.730195463674649492 ) ) ;
#2610=ORIENTED_EDGE ( 'NONE', *, *, #24418, .T. ) ;
#2613=CARTESIAN_POINT ( 'NONE',  ( -69.08758708074093136, 37.96445039004638033, -9.800414904976365804 ) ) ;
#2620=CARTESIAN_POINT ( 'NONE',  ( -67.52519766902113929, 36.12526529565825939, -8.800414904976360475 ) ) ;
#2626=ORIENTED_EDGE ( 'NONE', *, *, #34903, .T. ) ;
#2627=CARTESIAN_POINT ( 'NONE',  ( 67.08333554474984339, 58.24655189615426565, 3.990981480864018938 ) ) ;
#2642=EDGE_LOOP ( 'NONE', ( #34392, #28768, #2335, #15418, #11291, #197, #25108 ) ) ;
#2644=AXIS2_PLACEMENT_3D ( 'NONE', #36252, #14213, #20586 ) ;
#2646=CARTESIAN_POINT ( 'NONE',  ( 79.76446817951413948, 64.32424044856641387, -3.638935937159315515 ) ) ;
#2648=CARTESIAN_POINT ( 'NONE',  ( 80.89004220740271478, 62.15918302697193099, 3.003915454719618960 ) ) ;
#2651=CARTESIAN_POINT ( 'NONE',  ( 74.86006972221214539, 59.87270642427902345, -3.642458757454620777 ) ) ;
#2664=CARTESIAN_POINT ( 'NONE',  ( 80.26863108949500258, 64.98620546077047777, 3.307636073424107703 ) ) ;
#2666=( BOUNDED_CURVE ( )  B_SPLINE_CURVE ( 3, ( #16614, #29198, #1011, #13545 ),
 .UNSPECIFIED., .F., .T. ) 
 B_SPLINE_CURVE_WITH_KNOTS ( ( 4, 4 ),
 ( 1.570796326794896558, 2.438744940551181184 ),
 .UNSPECIFIED. ) 
 CURVE ( )  GEOMETRIC_REPRESENTATION_ITEM ( )  RATIONAL_B_SPLINE_CURVE ( ( 1.000000000000000000, 0.9382012019593851671, 0.9382012019593851671, 1.000000000000000000 ) ) 
 REPRESENTATION_ITEM ( '' )  );
#2682=CARTESIAN_POINT ( 'NONE',  ( 79.37790743583136077, 65.75409067367344562, -2.639511535887587801 ) ) ;
#2688=EDGE_CURVE ( 'NONE', #30686, #3289, #9189, .T. ) ;
#2689=ORIENTED_EDGE ( 'NONE', *, *, #24932, .T. ) ;
#2690=CIRCLE ( 'NONE', #3347, 6.681288188914807691 ) ;
#2696=CARTESIAN_POINT ( 'NONE',  ( 81.09687786842310686, 61.96238702813622723, -2.735335646780895580 ) ) ;
#2697=CARTESIAN_POINT ( 'NONE',  ( -58.36416262933996535, 28.31210393328041519, -5.221062780410251847 ) ) ;
#2701=ORIENTED_EDGE ( 'NONE', *, *, #24022, .T. ) ;
#2702=CARTESIAN_POINT ( 'NONE',  ( 82.08208307362210121, 62.96685751817972232, -2.430878896394279121 ) ) ;
#2703=LINE ( 'NONE', #40134, #23291 ) ;
#2707=CARTESIAN_POINT ( 'NONE',  ( -64.08758708074093136, 42.21690229090457791, -2.785273623167488388 ) ) ;
#2708=CARTESIAN_POINT ( 'NONE',  ( 74.14280505202560789, 59.94172787350157705, 3.795548882712136418 ) ) ;
#2715=CARTESIAN_POINT ( 'NONE',  ( 80.35914242818654429, 65.73759417665652904, 2.670779692148245399 ) ) ;
#2721=CARTESIAN_POINT ( 'NONE',  ( -58.99872204295123623, 28.48507918597066180, 6.834244957304007606 ) ) ;
#2732=CARTESIAN_POINT ( 'NONE',  ( 66.82989622468531365, 58.03237508814455481, -3.998112125426342978 ) ) ;
#2738=EDGE_CURVE ( 'NONE', #7186, #30246, #32234, .T. ) ;
#2742=DIRECTION ( 'NONE',  ( -1.000000000000000000, 0.000000000000000000, 0.000000000000000000 ) ) ;
#2745=CARTESIAN_POINT ( 'NONE',  ( 81.74784679736075077, 61.69507302169112251, -1.045691535380373960 ) ) ;
#2746=CARTESIAN_POINT ( 'NONE',  ( 81.14230761098953337, 61.33243076862672183, 1.577285172236835287 ) ) ;
#2749=CARTESIAN_POINT ( 'NONE',  ( 77.74497067125915351, 61.15868661831865438, -3.539370024157715733 ) ) ;
#2753=CARTESIAN_POINT ( 'NONE',  ( 81.34501369141619875, 61.50378551383992942, -1.741375869723593706 ) ) ;
#2754=CARTESIAN_POINT ( 'NONE',  ( 77.88532341798187986, 63.74564772441265603, 3.640295653904954243 ) ) ;
#2758=CARTESIAN_POINT ( 'NONE',  ( 79.96508732583362189, 66.32411498806379768, 1.465650077276458241 ) ) ;
#2759=CARTESIAN_POINT ( 'NONE',  ( -64.08758708074093136, 42.22117905496008916, 2.795515496173683889 ) ) ;
#2765=CARTESIAN_POINT ( 'NONE',  ( -63.48867051204930334, 35.67471974816369595, 6.899503081314800390 ) ) ;
#2773=CARTESIAN_POINT ( 'NONE',  ( 78.50958624606134606, 60.39254520314257491, -2.557033454456006272 ) ) ;
#2774=DIRECTION ( 'NONE',  ( 1.000000000000000000, 0.000000000000000000, 0.000000000000000000 ) ) ;
#2780=EDGE_CURVE ( 'NONE', #28971, #27835, #28277, .T. ) ;
#2786=CARTESIAN_POINT ( 'NONE',  ( 69.21678231378241719, 58.76388891306111617, -3.990151341881419622 ) ) ;
#2790=FACE_OUTER_BOUND ( 'NONE', #30369, .T. ) ;
#2796=EDGE_LOOP ( 'NONE', ( #7777, #31240, #26410, #29295, #758, #37196, #31718, #10409, #9214, #8538 ) ) ;
#2799=VERTEX_POINT ( 'NONE', #4042 ) ;
#2800=CARTESIAN_POINT ( 'NONE',  ( 80.21769632236902225, 61.97993766192919196, -3.195657361810719799 ) ) ;
#2802=CARTESIAN_POINT ( 'NONE',  ( 78.90307038293785524, 66.16006992971016132, -1.301239782962685609 ) ) ;
#2803=CARTESIAN_POINT ( 'NONE',  ( 79.46360196572364032, 64.13050462409741215, 3.681573067026199464 ) ) ;
#2830=ORIENTED_EDGE ( 'NONE', *, *, #18925, .T. ) ;
#2831=CARTESIAN_POINT ( 'NONE',  ( 67.02270721038308920, 57.95726884087558517, 3.999016414675010900 ) ) ;
#2847=CARTESIAN_POINT ( 'NONE',  ( 79.25608414939210888, 65.04333590781634200, -3.260928702718599581 ) ) ;
#2849=CARTESIAN_POINT ( 'NONE',  ( 80.21880177947251411, 63.46656020078421534, 3.697630003121159525 ) ) ;
#2850=AXIS2_PLACEMENT_3D ( 'NONE', #2385, #39204, #18198 ) ;
#2852=ORIENTED_EDGE ( 'NONE', *, *, #22531, .T. ) ;
#2854=CARTESIAN_POINT ( 'NONE',  ( -58.95285064334387215, 28.35919974994700965, 6.323895744698114996 ) ) ;
#2858=CARTESIAN_POINT ( 'NONE',  ( -63.08758708074093136, 38.76906266698303227, 4.000000000000000000 ) ) ;
#2860=ORIENTED_EDGE ( 'NONE', *, *, #3948, .F. ) ;
#2866=DIRECTION ( 'NONE',  ( 0.6751708784618154491, -0.7376613619250370624, 0.000000000000000000 ) ) ;
#2867=CARTESIAN_POINT ( 'NONE',  ( 80.52090910898030529, 64.76150916408880676, 3.396356880840907699 ) ) ;
#2869=CARTESIAN_POINT ( 'NONE',  ( -105.6213936588467135, -59.15536422891795354, -9.800414904976365804 ) ) ;
#2871=CARTESIAN_POINT ( 'NONE',  ( -60.75950795826495465, 23.17721540975219696, -46.17089178453873188 ) ) ;
#2883=CARTESIAN_POINT ( 'NONE',  ( 80.69089980977658172, 64.07786826041910899, -3.533418250979443620 ) ) ;
#2895=CARTESIAN_POINT ( 'NONE',  ( 79.82480777417542583, 64.72726844050399109, -3.473545878414593613 ) ) ;
#2896=CARTESIAN_POINT ( 'NONE',  ( -59.65099889957328116, 26.74201272916461747, -6.661192808835155965 ) ) ;
#2901=CARTESIAN_POINT ( 'NONE',  ( 81.51784234612458135, 64.89972252180021428, -2.776691787112390397 ) ) ;
#2908=CARTESIAN_POINT ( 'NONE',  ( 72.70998213798715426, 61.65396340192921798, 3.619654763610430592 ) ) ;
#2918=CARTESIAN_POINT ( 'NONE',  ( 81.88543442889059065, 63.19940289366435593, 2.771525467261982456 ) ) ;
#2920=EDGE_LOOP ( 'NONE', ( #22448, #11812, #22923, #24483, #26225 ) ) ;
#2925=AXIS2_PLACEMENT_3D ( 'NONE', #16486, #12390, #9496 ) ;
#2931=CARTESIAN_POINT ( 'NONE',  ( -68.98442902999595105, 21.93515443114010210, -46.17089178453873188 ) ) ;
#2941=CARTESIAN_POINT ( 'NONE',  ( 66.82596693864583415, 58.04328079001189877, -3.997688572870336188 ) ) ;
#2945=CARTESIAN_POINT ( 'NONE',  ( -55.57018072619605675, 31.35870463729802538, 3.952748674019340935 ) ) ;
#2947=CARTESIAN_POINT ( 'NONE',  ( 66.82540811322722618, 58.08308925668564626, 3.996046963204149094 ) ) ;
#2953=CARTESIAN_POINT ( 'NONE',  ( 80.99740051111608352, 66.07939114927816604, -1.509105202935689061 ) ) ;
#2955=CARTESIAN_POINT ( 'NONE',  ( 79.14683388637743633, 65.58698894143067548, 2.758686562281585264 ) ) ;
#2958=CARTESIAN_POINT ( 'NONE',  ( 75.81058488580238475, 63.71552251304081693, -3.121245466998380902 ) ) ;
#2962=CARTESIAN_POINT ( 'NONE',  ( 79.12689763788452524, 66.01933680498308377, -2.028924249969750182 ) ) ;
#2963=CARTESIAN_POINT ( 'NONE',  ( 76.72614680668753806, 63.26816225425361040, 3.643081266322642175 ) ) ;
#2967=DIRECTION ( 'NONE',  ( 0.000000000000000000, -1.000000000000000000, -0.000000000000000000 ) ) ;
#2968=CARTESIAN_POINT ( 'NONE',  ( 80.18989135007177538, 66.21456565649060622, 1.848245342697199645 ) ) ;
#2974=CARTESIAN_POINT ( 'NONE',  ( -63.02437332573799011, 35.53684452423013340, 6.244480380086192994 ) ) ;
#2985=CARTESIAN_POINT ( 'NONE',  ( 80.01441196509479425, 60.89222036820343220, -2.037985562400662420 ) ) ;
#2996=EDGE_LOOP ( 'NONE', ( #19757, #16021, #33769, #26644 ) ) ;
#2999=CARTESIAN_POINT ( 'NONE',  ( 70.60245471852235255, 60.31942058782808402, -3.837797619696055929 ) ) ;
#3012=CARTESIAN_POINT ( 'NONE',  ( 80.00843888008158444, 62.42993222482911619, -3.516968106976306796 ) ) ;
#3014=CARTESIAN_POINT ( 'NONE',  ( 81.30277405988975659, 64.78683171160533050, -3.017922835037759377 ) ) ;
#3015=CARTESIAN_POINT ( 'NONE',  ( 80.39157904934594967, 62.27158585385627987, 3.322373183921395245 ) ) ;
#3029=LINE ( 'NONE', #32031, #40065 ) ;
#3043=CARTESIAN_POINT ( 'NONE',  ( 66.99808371854801692, 58.02529356684345885, 3.999241514195644331 ) ) ;
#3047=FACE_OUTER_BOUND ( 'NONE', #40193, .T. ) ;
#3057=DIRECTION ( 'NONE',  ( -1.000000000000000000, 0.000000000000000000, 0.000000000000000000 ) ) ;
#3063=CARTESIAN_POINT ( 'NONE',  ( 80.68879072954297271, 62.10584950744627974, -3.070011659370638579 ) ) ;
#3066=CARTESIAN_POINT ( 'NONE',  ( 79.73288524454797255, 64.30401648905856860, 3.644176963625960664 ) ) ;
#3070=CARTESIAN_POINT ( 'NONE',  ( -59.00631990433781482, 28.04920808151690181, 6.320701908730214313 ) ) ;
#3080=CARTESIAN_POINT ( 'NONE',  ( 81.47459903045201202, 62.11139297693598849, 2.556731990914077546 ) ) ;
#3085=DIRECTION ( 'NONE',  ( -0.3757233601570931225, -0.9267318687906784813, 0.000000000000000000 ) ) ;
#3086=AXIS2_PLACEMENT_3D ( 'NONE', #1559, #23578, #33051 ) ;
#3098=CARTESIAN_POINT ( 'NONE',  ( 81.16399599188275715, 62.84525499041613017, -3.248659383495559272 ) ) ;
#3100=DIRECTION ( 'NONE',  ( -1.000000000000000000, 0.000000000000000000, 0.000000000000000000 ) ) ;
#3106=CARTESIAN_POINT ( 'NONE',  ( 79.89218238839933406, 64.40427343574535257, -3.614403801066810473 ) ) ;
#3118=CARTESIAN_POINT ( 'NONE',  ( 81.76287911024830635, 64.24668757703146582, -2.864610283900680621 ) ) ;
#3125=CARTESIAN_POINT ( 'NONE',  ( 73.33958664722344167, 61.75625940721956653, 3.692213121420756305 ) ) ;
#3133=CARTESIAN_POINT ( 'NONE',  ( 79.13116897371948255, 66.19293011460084131, 1.571309534768041694 ) ) ;
#3151=CARTESIAN_POINT ( 'NONE',  ( 66.43088956075783358, 57.76580747938971427, -4.000000000000008882 ) ) ;
#3154=EDGE_LOOP ( 'NONE', ( #19142, #36431, #6585, #38308 ) ) ;
#3158=( BOUNDED_CURVE ( )  B_SPLINE_CURVE ( 3, ( #40285, #3470, #38015, #28143 ),
 .UNSPECIFIED., .F., .T. ) 
 B_SPLINE_CURVE_WITH_KNOTS ( ( 4, 4 ),
 ( 4.712388980384689674, 5.617490880575807921 ),
 .UNSPECIFIED. ) 
 CURVE ( )  GEOMETRIC_REPRESENTATION_ITEM ( )  RATIONAL_B_SPLINE_CURVE ( ( 1.000000000000000000, 0.9328897322841716022, 0.9328897322841716022, 1.000000000000000000 ) ) 
 REPRESENTATION_ITEM ( '' )  );
#3164=CARTESIAN_POINT ( 'NONE',  ( 81.16949749213439702, 61.30395080096879212, -1.008685033153519983 ) ) ;
#3166=CARTESIAN_POINT ( 'NONE',  ( 79.76203521409539121, 64.68678814937342736, 3.489836119548952009 ) ) ;
#3170=CARTESIAN_POINT ( 'NONE',  ( 76.74823446354515966, 60.29158698200773614, -3.346357594037797423 ) ) ;
#3175=CARTESIAN_POINT ( 'NONE',  ( 81.09339258687016638, 63.16289930221478954, -3.352621494407070024 ) ) ;
#3176=CARTESIAN_POINT ( 'NONE',  ( 77.55533639035668614, 62.99992453720928864, 3.808649511194677650 ) ) ;
#3177=TOROIDAL_SURFACE ( 'NONE', #25503, 10.99999999999998579, 3.000000000000000000 ) ;
#3181=CARTESIAN_POINT ( 'NONE',  ( 81.67240355425563791, 65.37253450681799904, 2.134985007309429861 ) ) ;
#3187=CARTESIAN_POINT ( 'NONE',  ( -64.08758708074091714, 36.87876644325631759, 4.900609702795900802 ) ) ;
#3188=DIRECTION ( 'NONE',  ( -1.000000000000000000, 0.000000000000000000, -0.000000000000000000 ) ) ;
#3194=DIRECTION ( 'NONE',  ( 0.000000000000000000, 0.000000000000000000, 1.000000000000000000 ) ) ;
#3198=B_SPLINE_CURVE_WITH_KNOTS ( 'NONE', 3,
 ( #246, #12784, #33822, #28226 ),
 .UNSPECIFIED., .F., .F.,
 ( 4, 4 ),
 ( -1.385643128159646227E-05, 0.0002401580581033240457 ),
 .UNSPECIFIED. ) ;
#3199=CARTESIAN_POINT ( 'NONE',  ( -64.08758708074093136, 37.74469198210380227, -4.273126118783022065 ) ) ;
#3204=CARTESIAN_POINT ( 'NONE',  ( 68.55047844998404116, 58.76352648041117277, -3.988324671431286106 ) ) ;
#3208=CARTESIAN_POINT ( 'NONE',  ( -11.81496944966682960, -21.25669541281728669, -1.000000000000000000 ) ) ;
#3220=ORIENTED_EDGE ( 'NONE', *, *, #22577, .F. ) ;
#3221=CARTESIAN_POINT ( 'NONE',  ( 78.35540530300707474, 65.82096406625564100, -1.612955153530279739 ) ) ;
#3225=CARTESIAN_POINT ( 'NONE',  ( 79.60170308687696661, 66.12598108333446589, -2.076176908533889698 ) ) ;
#3226=CARTESIAN_POINT ( 'NONE',  ( 80.34542504610526237, 62.25824679691980634, 3.331801170923413213 ) ) ;
#3227=CARTESIAN_POINT ( 'NONE',  ( 82.56222392620333039, 63.90769089702598649, 1.000000000000000000 ) ) ;
#3235=AXIS2_PLACEMENT_3D ( 'NONE', #7498, #1745, #26450 ) ;
#3249=CLOSED_SHELL ( 'NONE', ( #31808, #4835, #38901, #19241, #34, #170, #3534, #4397, #23902, #38393, #36869, #25308, #14226, #22297, #26408, #11362, #10317, #4872, #23394, #33780, #28320, #28838, #21359, #19161, #37285, #13937, #4285, #28559, #33246, #15901, #34295, #13889, #28837, #29190, #21592, #9071, #7757, #26997, #7122, #39813, #37440, #21489, #3571, #4345, #18597, #7169, #4571, #26471, #24956, #18628, #17638, #36175, #15823, #26445, #20171, #12910, #9380, #8391, #20723, #30445, #20956, #20536, #12698, #37317, #31515, #20151, #37641, #1052, #3452, #37971, #33505, #6672, #28022, #35316, #34160, #31971, #9060, #27872, #20168, #7872, #24310, #35138, #1327, #23124 ) ) ;
#3252=CARTESIAN_POINT ( 'NONE',  ( 67.05715689120697220, 57.86208461462646113, 3.995640437668404044 ) ) ;
#3259=FACE_OUTER_BOUND ( 'NONE', #13167, .T. ) ;
#3264=EDGE_CURVE ( 'NONE', #29308, #8770, #34652, .T. ) ;
#3265=EDGE_LOOP ( 'NONE', ( #16864, #16195, #34493, #16904 ) ) ;
#3266=CARTESIAN_POINT ( 'NONE',  ( 79.97265554092989248, 63.70311272660515556, -3.710743084827438754 ) ) ;
#3268=CARTESIAN_POINT ( 'NONE',  ( 79.40192692649263506, 64.80415203875446650, 3.426353657592664526 ) ) ;
#3273=CARTESIAN_POINT ( 'NONE',  ( -58.94223801633730631, 28.40373775090870012, 6.290611457194089873 ) ) ;
#3276=CARTESIAN_POINT ( 'NONE',  ( -64.08758708074093136, 38.13199975834724142, -3.043809435734133206 ) ) ;
#3283=CARTESIAN_POINT ( 'NONE',  ( -68.71186372058384961, 37.81212149306785619, 8.800414904976364028 ) ) ;
#3286=CARTESIAN_POINT ( 'NONE',  ( 79.68360889523903268, 65.64663933523165440, 2.797238656122799760 ) ) ;
#3289=VERTEX_POINT ( 'NONE', #26599 ) ;
#3304=CARTESIAN_POINT ( 'NONE',  ( 80.87203728266233327, 63.05930952086730201, -3.432259906339282463 ) ) ;
#3306=CARTESIAN_POINT ( 'NONE',  ( -66.99872204295122913, 28.48507918597134037, 4.000000000000000000 ) ) ;
#3314=CARTESIAN_POINT ( 'NONE',  ( 79.02959213847954345, 65.76024385718582721, -2.482170738714647218 ) ) ;
#3320=CARTESIAN_POINT ( 'NONE',  ( 82.03499260127743753, 62.66326407617577132, -2.270757614041408079 ) ) ;
#3326=CARTESIAN_POINT ( 'NONE',  ( 74.91450450041774900, 59.74817859300106448, 3.564124015814033264 ) ) ;
#3329=EDGE_LOOP ( 'NONE', ( #28001, #25555, #17461, #13984 ) ) ;
#3334=DIRECTION ( 'NONE',  ( 0.5171480877355281169, -0.2439873919671817493, 0.8203828422831251910 ) ) ;
#3335=CARTESIAN_POINT ( 'NONE',  ( 78.88661621011570446, 66.15061626711309373, 1.323744132979558286 ) ) ;
#3347=AXIS2_PLACEMENT_3D ( 'NONE', #8799, #33959, #30865 ) ;
#3349=FACE_OUTER_BOUND ( 'NONE', #11070, .T. ) ;
#3355=CARTESIAN_POINT ( 'NONE',  ( 66.41308122482412557, 57.81611748292259279, -4.000000000000024869 ) ) ;
#3357=CARTESIAN_POINT ( 'NONE',  ( -55.72565997008030081, 31.19966888624958301, 3.920894724096667172 ) ) ;
#3365=DIRECTION ( 'NONE',  ( -0.000000000000000000, -0.000000000000000000, -1.000000000000000000 ) ) ;
#3367=CARTESIAN_POINT ( 'NONE',  ( 82.29396208789050604, 62.51418980721555840, -1.483157530539361391 ) ) ;
#3368=CARTESIAN_POINT ( 'NONE',  ( 79.89218238839933406, 64.40427343574535257, 3.614403801066811361 ) ) ;
#3371=CARTESIAN_POINT ( 'NONE',  ( 77.14378789031545125, 60.95143994403622401, -3.590981437852774238 ) ) ;
#3375=CARTESIAN_POINT ( 'NONE',  ( 80.45887431248497990, 64.72775385883045374, -3.425340496581089855 ) ) ;
#3376=CARTESIAN_POINT ( 'NONE',  ( 77.35226663217760290, 63.40502609692227765, 3.687756614093542940 ) ) ;
#3381=CARTESIAN_POINT ( 'NONE',  ( 81.94850308769548519, 64.73378216408571006, 2.360008641314786715 ) ) ;
#3392=EDGE_CURVE ( 'NONE', #22494, #28100, #32917, .T. ) ;
#3393=AXIS2_PLACEMENT_3D ( 'NONE', #12523, #25097, #19318 ) ;
#3403=CARTESIAN_POINT ( 'NONE',  ( -64.08758708074093136, 38.00013147421994830, -4.165003120434588091 ) ) ;
#3408=CARTESIAN_POINT ( 'NONE',  ( 68.45414103466679023, 59.01732383939346249, -3.957896739784463325 ) ) ;
#3422=CARTESIAN_POINT ( 'NONE',  ( 79.52562300987042931, 63.81209149333333386, -3.741985197832885746 ) ) ;
#3425=CARTESIAN_POINT ( 'NONE',  ( 78.87111998578919270, 66.14166623576272741, -1.344573736155070698 ) ) ;
#3426=CARTESIAN_POINT ( 'NONE',  ( 78.32432613507506858, 65.79895565947732905, 1.640065189519638755 ) ) ;
#3428=CARTESIAN_POINT ( 'NONE',  ( 79.00097698949592484, 66.21430696267364624, 1.000000000000000000 ) ) ;
#3433=ORIENTED_EDGE ( 'NONE', *, *, #18925, .F. ) ;
#3443=DIRECTION ( 'NONE',  ( -1.000000000000000000, 0.000000000000000000, 0.000000000000000000 ) ) ;
#3449=CARTESIAN_POINT ( 'NONE',  ( -57.16504416091206053, 33.41445838748276742, -1.000000000000000000 ) ) ;
#3452=ADVANCED_FACE ( 'NONE', ( #2519 ), #11942, .T. ) ;
#3455=CARTESIAN_POINT ( 'NONE',  ( 67.20175956769865877, 57.92120807820956685, 3.995511504169227290 ) ) ;
#3463=ORIENTED_EDGE ( 'NONE', *, *, #19206, .F. ) ;
#3464=CARTESIAN_POINT ( 'NONE',  ( 79.94486516293694933, 63.68863865526427759, -3.714073935154548423 ) ) ;
#3465=LINE ( 'NONE', #15792, #21382 ) ;
#3466=CARTESIAN_POINT ( 'NONE',  ( 78.57794565308397239, 65.91709162046863923, 1.743126864185328806 ) ) ;
#3468=CARTESIAN_POINT ( 'NONE',  ( -59.01947560891952804, 27.90920910948504385, 6.147301388271928957 ) ) ;
#3470=CARTESIAN_POINT ( 'NONE',  ( -66.83699642652008777, 37.05199716444892744, -9.800414904976365804 ) ) ;
#3471=CARTESIAN_POINT ( 'NONE',  ( -55.16612787639756732, 31.23053227951973199, 1.484562114140385747 ) ) ;
#3483=CARTESIAN_POINT ( 'NONE',  ( 81.24880315266035780, 62.88501018724376479, 3.211742283750890437 ) ) ;
#3488=DIRECTION ( 'NONE',  ( -0.9267318687906784813, 0.3757233601570931225, 0.000000000000000000 ) ) ;
#3499=CARTESIAN_POINT ( 'NONE',  ( 78.66788830423078593, 66.04261347698268025, -1.159471704397126102 ) ) ;
#3505=ORIENTED_EDGE ( 'NONE', *, *, #6051, .T. ) ;
#3507=VERTEX_POINT ( 'NONE', #34632 ) ;
#3508=CARTESIAN_POINT ( 'NONE',  ( 81.13710691025120525, 61.43629694585947476, -1.911132874451710650 ) ) ;
#3510=CARTESIAN_POINT ( 'NONE',  ( -63.08758708074093136, 36.14363715547679590, -3.800414904976364472 ) ) ;
#3516=CARTESIAN_POINT ( 'NONE',  ( 80.07729437284001506, 66.15382583937143579, -2.040045296073660808 ) ) ;
#3520=CARTESIAN_POINT ( 'NONE',  ( -63.33907144938095968, 42.38509300232142607, -3.755920398012963624 ) ) ;
#3521=CARTESIAN_POINT ( 'NONE',  ( 69.60281991352538000, 59.48300438377392396, 3.944663542062654571 ) ) ;
#3522=EDGE_LOOP ( 'NONE', ( #10649, #29613, #27923, #18259, #9021, #12100 ) ) ;
#3529=CARTESIAN_POINT ( 'NONE',  ( 81.76814852625392405, 62.80907675923856459, 2.758880570191250658 ) ) ;
#3534=ADVANCED_FACE ( 'NONE', ( #16066 ), #227, .T. ) ;
#3539=DIRECTION ( 'NONE',  ( 0.000000000000000000, 0.000000000000000000, -1.000000000000000000 ) ) ;
#3542=CIRCLE ( 'NONE', #2925, 31.02204673211315011 ) ;
#3548=CARTESIAN_POINT ( 'NONE',  ( 66.56200747226770886, 57.85618981312373421, -3.999874661883399352 ) ) ;
#3549=VERTEX_POINT ( 'NONE', #28836 ) ;
#3550=CARTESIAN_POINT ( 'NONE',  ( -57.76433750236255804, 32.39122475941741186, 4.160719226838292428 ) ) ;
#3553=DIRECTION ( 'NONE',  ( 1.000000000000000000, 0.000000000000000000, 0.000000000000000000 ) ) ;
#3558=CARTESIAN_POINT ( 'NONE',  ( 79.68325118717125122, 66.33239387230217687, -1.129532193886523261 ) ) ;
#3559=CARTESIAN_POINT ( 'NONE',  ( 80.91173626137351960, 62.16536564854140323, 2.996423812020193367 ) ) ;
#3562=CARTESIAN_POINT ( 'NONE',  ( 75.65523814419378823, 61.17064132828575396, -3.882889210543257974 ) ) ;
#3566=EDGE_CURVE ( 'NONE', #2799, #10884, #18442, .T. ) ;
#3567=CARTESIAN_POINT ( 'NONE',  ( 79.87861596566074240, 65.47018085071597682, -3.015642068896328798 ) ) ;
#3568=CARTESIAN_POINT ( 'NONE',  ( 75.66308047697211236, 62.61957414976296121, 3.723120700747973633 ) ) ;
#3571=ADVANCED_FACE ( 'NONE', ( #12151 ), #9216, .T. ) ;
#3576=CARTESIAN_POINT ( 'NONE',  ( 82.11700085695696316, 62.19713100941785200, 1.465650077276457131 ) ) ;
#3581=CARTESIAN_POINT ( 'NONE',  ( -63.58520484588291311, 35.72026407271198423, 6.999999999999986677 ) ) ;
#3584=ORIENTED_EDGE ( 'NONE', *, *, #25760, .T. ) ;
#3587=FACE_OUTER_BOUND ( 'NONE', #7625, .T. ) ;
#3600=CARTESIAN_POINT ( 'NONE',  ( 68.61500287773905882, 58.59333675578601230, -3.993768376023893563 ) ) ;
#3603=AXIS2_PLACEMENT_3D ( 'NONE', #15289, #14464, #24558 ) ;
#3612=CARTESIAN_POINT ( 'NONE',  ( 81.27646189173411528, 61.63998710316791829, 2.098997056522959426 ) ) ;
#3614=DIRECTION ( 'NONE',  ( -1.000000000000000000, 0.000000000000000000, 0.000000000000000000 ) ) ;
#3616=CARTESIAN_POINT ( 'NONE',  ( 80.55759259636404579, 61.16327383424329156, -2.033355767895908883 ) ) ;
#3620=CARTESIAN_POINT ( 'NONE',  ( 81.28907188958018537, 64.38987696229560243, -3.179853676209052793 ) ) ;
#3621=CARTESIAN_POINT ( 'NONE',  ( 78.62541471602109766, 65.39282990155331277, 2.732428818688203087 ) ) ;
#3623=EDGE_CURVE ( 'NONE', #33723, #7222, #28297, .T. ) ;
#3624=B_SPLINE_SURFACE_WITH_KNOTS ( 'NONE', 3, 3, ( 
 ( #36799, #3428, #6280, #34505, #15539, #28298, #22550, #19043, #33730, #18052, #31199, #40646, #12449, #25018, #37555, #3227, #15745, #118, #19242, #31605, #25224, #37752, #25422, #3625, #22351 ),
 ( #6694, #29321, #720, #35319, #38364, #38568, #35711, #7691, #7086, #10966, #1138, #19447, #39168, #10161, #20238, #17143, #38964, #6891, #32822, #19651, #7487, #16735, #13670, #3826, #4613 ),
 ( #14058, #28917, #10569, #22752, #13459, #1334, #35113, #29122, #32626, #32222, #4024, #26438, #20046, #925, #26240, #16542, #29523, #26034, #32020, #10763, #10374, #16943, #26634, #29715, #22950 ),
 ( #38774, #4421, #16344, #13261, #13871, #25827, #35513, #23340, #1524, #35912, #7284, #19847, #32417, #4215, #23143, #11563, #36908, #23733, #27438, #2138, #14657, #26833, #27636, #2554, #24139 ),
 ( #36700, #14866, #17747, #23930, #8483, #1731, #27228, #21065, #33639, #21268, #39994, #39372, #18159, #39794, #5414, #20439, #36303, #17952, #30126, #8076, #30536, #30753, #2347, #11764, #24345 ),
 ( #8689, #15077, #5210, #30332, #27033, #23546, #33841, #5619, #39578, #40194, #36110, #7888, #33019, #11163, #4807, #17336, #11363, #29913, #14262, #20639, #33221, #5007, #17538, #1941, #14460 ),
 ( #36502, #8274, #20848, #33440, #2758, #11974, #40390, #12192, #24761, #24552, #8892, #37915, #24971, #18367, #37106, #6646, #9105, #15695, #22092, #21475, #3576, #34667, #15284, #37309, #12604 ),
 ( #16103, #25170, #34053, #5826, #30954, #71, #25376, #21682, #15897, #31355, #3181, #27836, #28669, #31760, #37702, #37508, #12805, #34260, #28458, #12403, #6031, #31558, #265, #18565, #9722 ),
 ( #22303, #31152, #19197, #28247, #9510, #2968, #15486, #6445, #28045, #40596, #18997, #9303, #3381, #34870, #21880, #34458, #6234, #18778, #879, #10520, #9924, #38318, #16895, #25782, #22900 ),
 ( #13015, #25577, #22506, #16301, #32374, #26193, #29073, #4373, #35667, #13825, #31972, #19803, #32779, #26394, #13216, #35866, #6842, #22703, #38122, #38725, #19996, #32578, #35070, #13618, #4568 ),
 ( #23295, #7644, #38924, #23100, #10115, #13411, #19400, #10716, #25986, #3777, #35271, #28869, #20193, #676, #16688, #7038, #19606, #7435, #475, #32180, #29475, #3977, #16496, #1288, #17095 ),
 ( #38518, #10322, #35468, #7240, #4172, #29275, #1087, #1480, #39125, #4758, #20800, #14610, #17488, #33593, #24088, #2294, #20391, #8229, #21219, #14820, #1686, #24298, #36064, #11120, #26586 ),
 ( #32973, #29668, #17292, #7843, #39330, #30081, #11723, #36859, #27386, #2094, #14216, #1896, #10922, #39947, #14418, #29870, #23689, #26791, #8644, #23498, #5165, #36255, #8032, #36656, #14014 ),
 ( #23880, #20590, #26986, #8435, #33790, #5570, #33175, #30279, #4962, #39532, #11314, #36454, #33393, #17701, #27182, #39742, #11521, #21017, #5368, #17906, #30488, #9673, #28197, #8845, #5778 ),
 ( #31311, #22258, #3133, #40147, #15033, #27594, #6187, #31511, #18316, #22044, #37461, #9257, #21430, #34826, #37869, #18731, #2918, #18946, #27789, #34622, #18522, #18109, #37657, #6395, #30907 ),
 ( #15851, #3335, #34004, #12756, #34414, #21837, #11929, #2715, #15651, #24714, #15236, #27, #25334, #12555, #28409, #216, #9459, #40344, #30703, #31106, #25127, #24505, #12138, #37057, #2509 ),
 ( #37262, #21632, #9055, #34213, #5983, #15438, #12353, #27998, #40542, #24925, #4325, #13778, #428, #7194, #6797, #19351, #6602, #3529, #32525, #19561, #12968, #19147, #1242, #3731, #10275 ),
 ( #19754, #16053, #19946, #29028, #10072, #16846, #25534, #38276, #3937, #32332, #22656, #13362, #38078, #28826, #7392, #4128, #26346, #38471, #35620, #10670, #38878, #25937, #22853, #35425, #16641 ),
 ( #6996, #23251, #26143, #29428, #31922, #31713, #831, #16255, #29226, #35224, #1039, #9880, #28622, #22454, #35023, #632, #13173, #25733, #32137, #13571, #38677, #16454, #10474, #23055, #20962 ),
 ( #5113, #4523, #32921, #11468, #20342, #17436, #1629, #14168, #20539, #30026, #30230, #33543, #36405, #39072, #14364, #13969, #32727, #2044, #17043, #33338, #36204, #23637, #4712, #1841, #14765 ),
 ( #20748, #27133, #39684, #29622, #8176, #39897, #10871, #8385, #17853, #24036, #7595, #5319, #7790, #17649, #26932, #39477, #1436, #30434, #20147, #7983, #27337, #36607, #2244, #36012, #11671 ),
 ( #23447, #35817, #11264, #23828, #26537, #17245, #26740, #39279, #11067, #33124, #4904, #15390, #40705, #28151, #15599, #37009, #34572, #24659, #34366, #33737, #21373, #12506, #8791, #5932, #18265 ),
 ( #36809, #5517, #40096, #27946, #9208, #12085, #25081, #18677, #37611, #14983, #2867, #15808, #9407, #33952, #18896, #30650, #5727, #21172, #21788, #3080, #21995, #18059, #37412, #28362, #27543 ),
 ( #6346, #31463, #6136, #30857, #37211, #2462, #3286, #9004, #11877, #2664, #24452, #175, #15183, #40488, #27742, #40295, #31263, #24245, #21584, #8594, #34166, #18471, #31056, #12300, #24873 ),
 ( #13312, #12916, #25482, #12711, #9621, #38632, #25683, #19098, #25285, #7342, #9830, #16404, #22808, #22208, #4272, #35378, #3483, #380, #25885, #10431, #38424, #16795, #10225, #34775, #6553 ),
 ( #34976, #13523, #7147, #32474, #3889, #987, #29376, #19901, #32084, #19509, #28978, #19707, #4082, #782, #29178, #16596, #26094, #38028, #23006, #13124, #32282, #31667, #22406, #35573, #6751 ),
 ( #37816, #16008, #28573, #19301, #31872, #3683, #16207, #585, #28778, #38226, #10023, #22606, #35174, #6947, #36362, #29574, #33283, #35769, #26492, #26296, #20492, #14316, #26886, #10622, #33074 ),
 ( #20291, #5064, #17597, #23783, #4858, #1390, #32874, #38828, #8129, #4664, #7543, #39017, #20098, #30177, #23197, #23597, #32675, #10821, #1787, #1196, #23397, #17391, #13921, #4476, #39427 ),
 ( #26692, #35962, #11217, #7743, #13733, #14516, #39227, #1998, #16998, #17200, #20700, #29767, #1582, #14113, #11016, #36161, #29972, #7940, #19639, #711, #10556, #3612, #28905, #35304, #22939 ),
 ( #34908, #26022, #23132, #38154, #1126, #16531, #29109, #516, #1321, #16934, #38553, #22740, #38763, #6881, #13659, #38354, #29511, #16723, #26228, #9958, #35700, #32213, #19434, #10363, #13248 ),
 ( #913, #6682, #22540, #35501, #3814, #35102, #13449, #32613, #7473, #25817, #7274, #20032, #10151, #7075, #19837, #19231, #4409, #4014, #32409, #13860, #16141, #4203, #29310, #37952, #9759 ),
 ( #32009, #22339, #31797, #28702, #13047, #25610, #16331, #33626, #4996, #33211, #1926, #27020, #17730, #20625, #26821, #14449, #4601, #17521, #39566, #36492, #24123, #30317, #29703, #21054, #11350 ),
 ( #8470, #5401, #20427, #36690, #2332, #38955, #30117, #20833, #27217, #17324, #29904, #11552, #17941, #8064, #23914, #1718, #26426, #2127, #30522, #14248, #10749, #23330, #35899, #7677, #1514 ),
 ( #14047, #8262, #17129, #20229, #33429, #32812, #5198, #39360, #11152, #36100, #14644, #26622, #39779, #39157, #10952, #23535, #7877, #33005, #4794, #23722, #36288, #37688, #9493, #28231, #28032 ),
 ( #15471, #37296, #9093, #24332, #58, #39982, #21666, #21255, #15065, #18148, #18352, #40578, #12587, #27623, #31545, #34245, #11754, #40372, #9289, #25154, #22080, #8674, #12389, #40180, #11961 ),
 ( #34654, #27820, #33826, #6425, #18983, #5609, #24957, #24537, #37092, #14853, #36896, #27421, #12177, #30736, #2541, #8881, #21463, #18552, #37492, #34039, #5812, #21866, #30940, #2746, #34443 ),
 ( #15269, #24747, #6220, #6016, #31136, #2955, #18766, #15682, #31340, #3166, #35797, #32904, #7967, #11048, #23231, #10652, #20128, #4505, #35993, #38861, #4306, #32710, #22288, #7575, #17027 ),
 ( #12998, #29602, #7371, #1417, #34857, #20518, #26720, #23623, #38107, #14147, #3368, #15884, #13953, #39052, #4694, #35055, #19928, #29800, #36187, #26324, #26519, #32506, #28443, #7774, #1612 ),
 ( #22491, #29412, #10851, #23428, #39257, #20322, #6634, #17226, #19181, #251, #12788, #25364, #37901, #16828, #1226, #25563, #9708, #31746, #3559, #16087, #28653, #460, #9911, #13760, #11245 ),
 ( #5708, #15165, #36993, #4887, #18250, #5094, #33719, #14745, #27316, #1821, #30838, #17418, #39876, #39456, #33314, #36385, #36590, #5498, #2648, #17627, #8984, #11653, #30003, #17833, #27529 ),
 ( #14343, #24228, #23809, #30207, #8157, #8367, #18041, #27723, #2024, #33102, #36789, #26914, #30416, #40081, #40278, #12064, #20729, #30634, #14540, #27114, #39664, #11448, #24643, #5296, #24014 ),
 ( #20939, #8574, #2442, #33525, #37194, #14964, #2223, #21153, #11859, #24435, #8773, #21360, #33934, #2849, #18456, #31042, #9604, #34956, #21768, #25464, #158, #12691, #24857, #25664, #567 ),
 ( #22391, #31245, #38009, #21977, #13105, #362, #9811, #34351, #6733, #15793, #3066, #22187, #25061, #37800, #40472, #38206, #3665, #28757, #15582, #31850, #21570, #34148, #25267, #15984, #19283 ),
 ( #6121, #16192, #34554, #31650, #15370, #18656, #5916, #28137, #3268, #40689, #12494, #6326, #28344, #28551, #27928, #34761, #37398, #6535, #12281, #9193, #12899, #37595, #19082, #18874, #9392 ),
 ( #31446, #3466, #6929, #35750, #29556, #1376, #3870, #23180, #14097, #13294, #23379, #32861, #13907, #22589, #35947, #22789, #10607, #32455, #4255, #16386, #7524, #10207, #35357, #10006, #19491 ),
 ( #1567, #7729, #26077, #1180, #4650, #10414, #7325, #20085, #28960, #20276, #16780, #13505, #17183, #763, #968, #29360, #32663, #38610, #13714, #25867, #32265, #10801, #4462, #29752, #26280 ),
 ( #26676, #35157, #38814, #35557, #38406, #19689, #26475, #22990, #7129, #39003, #4063, #16578, #29159, #16984, #8113, #39841, #1983, #14701, #17376, #15124, #21316, #5668, #33267, #8733, #39211 ),
 ( #30379, #14920, #2395, #30588, #11205, #33888, #39624, #8531, #7927, #36345, #27488, #23769, #20896, #5050, #17581, #23970, #33483, #33681, #24395, #11610, #1771, #17793, #29957, #36147, #5461 ),
 ( #30797, #11811, #20682, #18205, #4845, #30163, #20476, #24189, #18002, #40038, #33058, #36745, #2605, #14300, #36953, #10999, #23583, #26868, #39414, #14503, #21113, #5253, #2183, #27079, #11404 ),
 ( #36545, #8322, #27270, #31000, #6075, #34713, #27680, #21723, #25221, #27882, #2803, #19041, #12647, #34306, #21928, #19240, #25420, #3015, #18825, #9767, #28092, #25013, #115, #37151, #314 ),
 ( #12851, #5874, #18608, #37552, #37751, #31196, #34502, #21525, #9147, #28502, #9556, #6692, #31397, #15937, #31806, #34917, #6277, #3226, #15742, #28294, #31603, #22141, #40643, #6489, #18412 ),
 ( #3426, #37961, #22347, #15328, #3621, #40237, #12020, #24597, #40427, #8940, #15535, #12238, #24812, #37353, #12446, #9347, #20040, #7483, #28913, #26435, #16539, #26238, #25618, #13256, #32621 ),
 ( #32219, #10758, #28711, #523, #38161, #32017, #7281, #1134, #4022, #4417, #10566, #29519, #6888, #35509, #7687, #1330, #718, #23337, #22548, #38361, #13057, #13666, #35708, #16941, #9967 ),
 ( #25825, #29116, #38962, #35906, #13867, #29317, #10158, #922, #35110, #20236, #13457, #19442, #22747, #3824, #32819, #16341, #32416, #35314, #7082, #23140, #16148, #19649, #38770, #26029, #38561 ),
 ( #10371, #22947, #19846, #16732, #4211, #4802, #4608, #1522, #30531, #17948, #17333, #39990, #10960, #26828, #14055, #30326, #24133, #36697, #26631, #17738, #8681, #7885, #2341, #27431, #8478 ),
 ( #29911, #5004, #39164, #14862, #17530, #23543, #39369, #36108, #24340, #20434, #20842, #33015, #23730, #11559, #17139, #11159, #2134, #1727, #14257, #21061, #14652, #36297, #39573, #8073, #39789 ),
 ( #29712, #20633, #11761, #30124, #33219, #1936, #36904, #14457, #8270, #27224, #27029, #21263, #33633, #11357, #23925, #5207, #36499, #5409, #33436, #6229, #15074, #30747, #2549, #21875, #6436 ),
 ( #12398, #24967, #37102, #37910, #12799, #34453, #18560, #34663, #2754, #9505, #34253, #25372, #12597, #22088, #34048, #18992, #28041, #15278, #18774, #37304, #9297, #11970, #9716, #15892, #259 ),
 ( #5822, #31348, #28452, #37502, #31553, #37697, #25163, #18361, #3376, #6026, #3176, #27631, #30949, #33836, #27829, #15479, #40381, #12187, #31145, #40590, #28241, #5616, #15690, #8889, #66 ),
 ( #18156, #24545, #40188, #21471, #24756, #9100, #21677, #2963, #22892, #22500, #35063, #22295, #19189, #7429, #35264, #28664, #34866, #16887, #19394, #25980, #32368, #31755, #13816, #4164, #13009 ),
 ( #35659, #470, #13208, #19601, #7234, #25776, #29066, #16097, #3769, #23094, #35462, #1280, #13406, #10514, #26385, #29468, #873, #38513, #10315, #19795, #13612, #16492, #22698, #16681, #25572 ),
 ( #29268, #19987, #26185, #38116, #38916, #1080, #38718, #3568, #6837, #32571, #28864, #31967, #4367, #6642, #9919, #16294, #671, #38313, #10110, #7032, #32174, #3973, #20186, #7834, #27173 ),
 ( #26782, #5361, #23287, #35856, #32771, #26577, #1884, #36446, #39320, #14601, #5156, #24080, #1473, #30072, #2286, #36649, #23489, #17899, #17086, #32963, #7635, #8221, #30273, #2089, #4560 ),
 ( #20384, #11110, #33584, #30480, #8428, #23870, #36056, #23681, #29660, #21006, #36247, #14006, #4750, #39117, #14810, #10913, #26978, #17284, #29863, #17693, #10708, #1677, #20792, #14208, #8024 ),
 ( #33166, #20580, #4953, #17480, #14409, #39730, #27378, #11305, #39523, #33387, #11513, #36852, #34407, #21212, #37452, #40336, #27782, #8836, #21624, #18937, #15428, #3326, #15844, #30693, #39941 ),
 ( #11714, #2500, #12547, #22035, #3125, #24290, #25118, #11920, #40535, #34204, #5972, #8635, #37648, #33784, #18513, #5561, #40139, #15024, #2708, #12343, #9452, #24495, #18102, #31098, #27587 ),
 ( #24916, #33994, #2908, #37050, #6179, #21420, #5769, #15641, #18308, #21826, #31503, #34612, #15228, #27988, #6389, #12128, #37255, #9249, #30898, #24707, #18721, #9046, #31303, #28189, #16 ),
 ( #9664, #25327, #37860, #16443, #1027, #28613, #32320, #6986, #19552, #31705, #32516, #7380, #29019, #13164, #29217, #38069, #4119, #28818, #19938, #7184, #16632, #420, #13561, #22648, #9871 ),
 ( #23045, #3928, #32128, #22250, #12959, #823, #35014, #25524, #13354, #35610, #25928, #26134, #38666, #19745, #22446, #10465, #621, #38461, #34816, #6788, #4315, #19342, #25725, #6594, #28402 ),
 ( #209, #12750, #35214, #19139, #31912, #3521, #3723, #10264, #16044, #16247, #38267, #22844, #10062, #35417, #27669, #12006, #8720, #33875, #40224, #5654, #18192, #21299, #30784, #2588, #15110 ),
 ( #22819, #35584, #29584, #7158, #998, #19913, #28788, #32688, #13534, #10239, #4487, #13135, #38433, #7355, #4283, #35388, #29390, #595, #13321, #7553, #1209, #26502, #13743, #17009, #10832 ),
 ( #32294, #1400, #16417, #23212, #19720, #39033, #26307, #13931, #6959, #23408, #38840, #25898, #10635, #19313, #31885, #25693, #3696, #10036, #22618, #35186, #19518, #32098, #3902, #27098, #30401 ),
 ( #27297, #7952, #5483, #36369, #5278, #4675, #33082, #11634, #20500, #17609, #29984, #14325, #20709, #30186, #2206, #21137, #36567, #39237, #14527, #14125, #32888, #14727, #17210, #33507, #8140 ),
 ( #30615, #1595, #17401, #29777, #20923, #39863, #24211, #26703, #8347, #40061, #11026, #8556, #18026, #36772, #7755, #20302, #23606, #36171, #39648, #17818, #23795, #33703, #2424, #14944, #4867 ),
 ( #33295, #5078, #1800, #2007, #27510, #11432, #11842, #35975, #26894, #39437, #11228, #23996, #34128, #12263, #6518, #19065, #37779, #37578, #8962, #24835, #33912, #9587, #37383, #30821, #5897 ),
 ( #2627, #24623, #27706, #27909, #25046, #22169, #37176, #341, #18638, #8757, #9176, #18855, #34740, #31629, #18232, #9374, #21551, #18435, #24420, #21340, #3455, #21748, #15146, #36976, #15969 ),
 ( #34331, #6101, #21959, #5691, #28533, #31224, #40452, #40260, #12044, #15353, #3043, #34533, #15563, #28119, #31023, #2831, #25249, #6306, #40671, #12475, #12673, #31428, #3252, #15771, #28327 ),
 ( #143, #29342, #13281, #4443, #32440, #1164, #13087, #26264, #7113, #22572, #13486, #16372, #29145, #31835, #29543, #35734, #20070, #6914, #23166, #12882, #25447, #4049, #7311, #13695, #3854 ),
 ( #32646, #35343, #19676, #28943, #37992, #16762, #10591, #747, #7507, #9794, #26061, #16970, #16172, #38796, #22374, #34940, #6718, #19269, #25647, #38593, #16563, #951, #3648, #28740, #551 ),
 ( #38191, #10399, #9993, #32047, #19869, #35141, #19472, #22975, #25854, #38387, #4237, #35539, #10192, #22776, #26659, #36528, #10986, #17979, #17772, #20460, #23951, #33662, #39822, #17359, #33248 ),
 ( #11386, #10786, #5439, #8301, #32846, #29734, #1967, #27253, #14485, #1359, #27058, #23364, #38987, #35932, #30149, #14685, #1548, #5235, #20664, #5033, #4635, #13894, #21091, #39604, #26854 ),
 ( #30359, #1754, #26457, #20877, #2164, #14080, #11590, #36327, #23566, #33467, #4829, #17563, #20260, #7711, #24170, #8511, #36130, #36727, #17165, #39193, #7911, #33039, #29937, #14284, #39395 ) ),
 .UNSPECIFIED., .F., .F., .F.,
 ( 4, 3, 3, 3, 3, 3, 3, 3, 3, 3, 3, 3, 3, 3, 3, 3, 3, 3, 3, 3, 3, 3, 3, 3, 3, 3, 3, 4 ),
 ( 4, 3, 3, 3, 3, 3, 3, 3, 4 ),
 ( -2.505502282154539045E-17, 9.220626685347035532E-07, 1.844125337094462129E-06, 3.688250674213979493E-06, 5.532376011333496433E-06, 7.376501348453014221E-06, 1.106475202269204810E-05, 1.475300269693108368E-05, 2.212950404540915483E-05, 2.950600539388722259E-05, 4.425900809084336150E-05, 5.901201078779949702E-05, 8.851801618171178162E-05, 0.0001180240215756240527, 0.0001770360323634486083, 0.0002360480431512731504, 0.0003540720647269222617, 0.0004720960863025713459, 0.0009441921726051677368, 0.001888384345210360627, 0.003776768690420746408, 0.005665153035631132622, 0.007553537380841517969, 0.01133030607126228953, 0.01321869041647267401, 0.01416288258907786798, 0.01463497867538046324, 0.01510707476168306022 ),
 ( 0.000000000000000000, 0.1250000000000000000, 0.2500000000000000000, 0.3750000000000000000, 0.5000000000000000000, 0.6250000000000000000, 0.7500000000000000000, 0.8750000000000000000, 1.000000000000000000 ),
 .UNSPECIFIED. ) ;
#3625=CARTESIAN_POINT ( 'NONE',  ( 81.47505553675506462, 61.46950381087522430, 1.000000000000000000 ) ) ;
#3626=CARTESIAN_POINT ( 'NONE',  ( -64.08758708074093136, 42.22117905423280604, 2.795515491199095148 ) ) ;
#3629=EDGE_LOOP ( 'NONE', ( #35747, #24009, #39614, #18985 ) ) ;
#3638=CYLINDRICAL_SURFACE ( 'NONE', #18982, 6.329987104167475565 ) ;
#3640=DIRECTION ( 'NONE',  ( -0.000000000000000000, -0.000000000000000000, -1.000000000000000000 ) ) ;
#3648=CARTESIAN_POINT ( 'NONE',  ( 66.74404603967394678, 57.81040951471371159, 3.998354769210576976 ) ) ;
#3649=CARTESIAN_POINT ( 'NONE',  ( -64.08758708074093136, 38.43534281692316767, 4.049547700704724029 ) ) ;
#3659=VECTOR ( 'NONE', #11289, 1000.000000000000000 ) ;
#3662=CARTESIAN_POINT ( 'NONE',  ( 78.77165107407959965, 65.73683965358550552, -2.311104455577570160 ) ) ;
#3665=CARTESIAN_POINT ( 'NONE',  ( 80.57935153413077956, 62.61414007970553541, 3.419027627190931451 ) ) ;
#3666=DIRECTION ( 'NONE',  ( 0.000000000000000000, 0.000000000000000000, -1.000000000000000000 ) ) ;
#3671=CARTESIAN_POINT ( 'NONE',  ( -56.90680744419238124, 30.56621156453423183, 3.329292219611507342 ) ) ;
#3683=CARTESIAN_POINT ( 'NONE',  ( 79.39921707337094858, 65.76781561079134519, 2.628317182735757651 ) ) ;
#3692=CARTESIAN_POINT ( 'NONE',  ( -66.99872204295122913, 28.48507918597134037, -6.999999999999999112 ) ) ;
#3696=CARTESIAN_POINT ( 'NONE',  ( 68.67947939959147163, 58.42312895491860303, 3.988324671431328738 ) ) ;
#3702=CARTESIAN_POINT ( 'NONE',  ( 81.23333979799274118, 62.00977392264719157, -2.676159939830913270 ) ) ;
#3705=EDGE_LOOP ( 'NONE', ( #21612, #33997, #7666, #28503 ) ) ;
#3711=CARTESIAN_POINT ( 'NONE',  ( 81.08254763934547782, 61.27217476014467934, -1.284346554836955256 ) ) ;
#3723=CARTESIAN_POINT ( 'NONE',  ( 69.62738871241069205, 59.42086865771531023, 3.954846139149833739 ) ) ;
#3725=ORIENTED_EDGE ( 'NONE', *, *, #22930, .T. ) ;
#3726=CIRCLE ( 'NONE', #4358, 2.999999999999998668 ) ;
#3730=CARTESIAN_POINT ( 'NONE',  ( -54.85217575791900657, 31.46625607997153296, -1.118209565749431533 ) ) ;
#3731=CARTESIAN_POINT ( 'NONE',  ( 81.34095870999074407, 61.40448684960413317, 1.344573736155039390 ) ) ;
#3751=CARTESIAN_POINT ( 'NONE',  ( 66.58940539569050543, 57.77934511969053943, -3.999344142514784650 ) ) ;
#3760=CARTESIAN_POINT ( 'NONE',  ( 81.46661790917876544, 61.46529165999840671, -1.093381982072927361 ) ) ;
#3764=CARTESIAN_POINT ( 'NONE',  ( 75.18153624412200031, 63.60369824193131194, -2.950589020697163889 ) ) ;
#3768=CARTESIAN_POINT ( 'NONE',  ( 79.48860182481722347, 65.82309781974730356, -2.578835243349315576 ) ) ;
#3769=CARTESIAN_POINT ( 'NONE',  ( 76.28050337382492785, 62.76811984040510595, 3.753756190325763242 ) ) ;
#3777=CARTESIAN_POINT ( 'NONE',  ( 81.15665777833334005, 65.46403653819207591, 2.541832380858825235 ) ) ;
#3784=TOROIDAL_SURFACE ( 'NONE', #33365, 114.6618724293813898, 3.000000000000000000 ) ;
#3786=CARTESIAN_POINT ( 'NONE',  ( 66.44405367406183416, 57.75571810119279093, 3.999999999999982681 ) ) ;
#3789=CYLINDRICAL_SURFACE ( 'NONE', #31887, 0.9999999999999998890 ) ;
#3799=CARTESIAN_POINT ( 'NONE',  ( 67.80923286766689273, 58.07768331974902765, -3.990378031984521012 ) ) ;
#3804=CARTESIAN_POINT ( 'NONE',  ( -64.08758708074094557, 36.76569972833094369, 3.434863364315535961 ) ) ;
#3813=DIRECTION ( 'NONE',  ( 0.000000000000000000, 0.000000000000000000, 1.000000000000000000 ) ) ;
#3814=CARTESIAN_POINT ( 'NONE',  ( 79.12779906683435627, 65.83686883797783196, 2.419967184825693174 ) ) ;
#3817=EDGE_CURVE ( 'NONE', #2799, #23657, #25223, .T. ) ;
#3820=CARTESIAN_POINT ( 'NONE',  ( 77.95070745440513349, 65.53481705947537250, -1.908681007153592235 ) ) ;
#3823=CARTESIAN_POINT ( 'NONE',  ( 81.16506502659913735, 61.30232764367859488, -1.065084354002960865 ) ) ;
#3824=CARTESIAN_POINT ( 'NONE',  ( 79.47890774847340367, 63.12292952392867562, 3.765547211956734586 ) ) ;
#3826=CARTESIAN_POINT ( 'NONE',  ( 81.47505553675506462, 61.46950381087522430, 1.024355359505926266 ) ) ;
#3837=CIRCLE ( 'NONE', #2530, 7.999999999999992895 ) ;
#3854=CARTESIAN_POINT ( 'NONE',  ( 66.90849722842033032, 57.81418058710544727, 3.996206253853811674 ) ) ;
#3868=CARTESIAN_POINT ( 'NONE',  ( 80.72570547868197366, 61.86964107431867177, -2.884918531047269141 ) ) ;
#3870=CARTESIAN_POINT ( 'NONE',  ( 79.10075812992909050, 65.22691190166821684, 3.061371641637242735 ) ) ;
#3884=DIRECTION ( 'NONE',  ( 0.000000000000000000, -1.000000000000000000, 0.000000000000000000 ) ) ;
#3889=CARTESIAN_POINT ( 'NONE',  ( 79.24523542244190821, 65.91691524828226534, 2.349509806045092297 ) ) ;
#3902=CARTESIAN_POINT ( 'NONE',  ( 68.77554901931263487, 58.16923054873410592, 3.957896739784568574 ) ) ;
#3905=EDGE_CURVE ( 'NONE', #21757, #36812, #21108, .T. ) ;
#3910=CARTESIAN_POINT ( 'NONE',  ( 81.26572199898306792, 62.02204868734987286, -2.661900242191199695 ) ) ;
#3917=ORIENTED_EDGE ( 'NONE', *, *, #33230, .T. ) ;
#3918=CIRCLE ( 'NONE', #19672, 6.681288188914807691 ) ;
#3919=CARTESIAN_POINT ( 'NONE',  ( 81.12024331894986062, 61.43208913379081793, -1.925402693829568745 ) ) ;
#3925=CARTESIAN_POINT ( 'NONE',  ( -58.71358459458718926, 29.03749951736172719, -5.614777500241355135 ) ) ;
#3928=CARTESIAN_POINT ( 'NONE',  ( 70.57032280423491954, 60.39816359117256184, 3.808711916423200616 ) ) ;
#3935=ORIENTED_EDGE ( 'NONE', *, *, #20944, .T. ) ;
#3937=CARTESIAN_POINT ( 'NONE',  ( 80.42837321982344179, 65.43835520822057106, 2.971291902561977949 ) ) ;
#3948=EDGE_CURVE ( 'NONE', #6853, #33723, #19780, .T. ) ;
#3955=CARTESIAN_POINT ( 'NONE',  ( 66.41703863280939402, 57.80493748213750393, -4.000000000000021316 ) ) ;
#3966=CARTESIAN_POINT ( 'NONE',  ( 81.41819469040422064, 65.60226997055944764, -2.078018481493678404 ) ) ;
#3969=CARTESIAN_POINT ( 'NONE',  ( 75.80265905884337485, 60.84868533121094458, -3.810661578667723148 ) ) ;
#3973=CARTESIAN_POINT ( 'NONE',  ( 76.74823446354523071, 60.29158698200765798, 3.346357594037719707 ) ) ;
#3977=CARTESIAN_POINT ( 'NONE',  ( 81.77194423968626324, 61.86568514665832907, 1.662695954554601840 ) ) ;
#3986=CARTESIAN_POINT ( 'NONE',  ( 66.27376694608931018, 57.73522568913554665, 4.000000000000000000 ) ) ;
#3990=( BOUNDED_SURFACE ( )  B_SPLINE_SURFACE ( 3, 2, ( 
 ( #32094, #788, #9838 ),
 ( #29385, #38035, #22814 ),
 ( #29184, #12926, #10233 ),
 ( #34983, #7350, #7154 ) ),
 .UNSPECIFIED., .F., .F., .T. ) 
 B_SPLINE_SURFACE_WITH_KNOTS ( ( 4, 4 ),
 ( 3, 3 ),
 ( 0.000000000000000000, 0.0006385966863609145649 ),
 ( 0.000000000000000000, 1.000000000000000000 ),
 .UNSPECIFIED. ) 
 GEOMETRIC_REPRESENTATION_ITEM ( )  RATIONAL_B_SPLINE_SURFACE ( (
 ( 1.000000000000000000, 0.5935057080259643625, 1.000000000000000000),
 ( 1.000000000000000000, 0.5840949208454031538, 1.000000000000000000),
 ( 1.000000000000000000, 0.5746205253747198594, 1.000000000000000000),
 ( 1.000000000000000000, 0.5652620711642702966, 1.000000000000000000) ) ) 
 REPRESENTATION_ITEM ( '' )  SURFACE ( )  );
#4001=CARTESIAN_POINT ( 'NONE',  ( 68.12732179974642577, 58.11841597887141120, -3.982418445723222789 ) ) ;
#4014=CARTESIAN_POINT ( 'NONE',  ( 81.08176929032271119, 62.48897713179231772, 3.134554000843276178 ) ) ;
#4017=CARTESIAN_POINT ( 'NONE',  ( 78.78025785238997969, 63.39248666165328672, -3.791687334209850935 ) ) ;
#4020=CARTESIAN_POINT ( 'NONE',  ( 79.73441168749667440, 65.96538777704688528, -2.410848004503907127 ) ) ;
#4022=CARTESIAN_POINT ( 'NONE',  ( 78.95999731999182814, 64.46943033386045840, 3.516968106976288588 ) ) ;
#4024=CARTESIAN_POINT ( 'NONE',  ( 81.87444285025611634, 65.47866087958064440, 1.319711737399753781 ) ) ;
#4025=CARTESIAN_POINT ( 'NONE',  ( -63.66774038485660725, 44.17617058018847587, 2.092190587516514100 ) ) ;
#4027=CARTESIAN_POINT ( 'NONE',  ( -64.66796849410253856, 36.23110552202055601, -6.165526157072429569 ) ) ;
#4037=LINE ( 'NONE', #20251, #29259 ) ;
#4042=CARTESIAN_POINT ( 'NONE',  ( -63.58520484588292732, 35.72026407271187765, 6.999999999999999112 ) ) ;
#4049=CARTESIAN_POINT ( 'NONE',  ( 66.89671537544454338, 57.84689108302589489, 3.997688572865332635 ) ) ;
#4050=CARTESIAN_POINT ( 'NONE',  ( -63.05048152672938500, 38.43432252562566731, 4.010992198732391323 ) ) ;
#4057=CARTESIAN_POINT ( 'NONE',  ( -58.99872204295123623, 28.48507918597136523, -6.834244957304557389 ) ) ;
#4062=CARTESIAN_POINT ( 'NONE',  ( 80.91727723835752784, 61.27046310099965609, -1.796258654643025476 ) ) ;
#4063=CARTESIAN_POINT ( 'NONE',  ( 79.59524243168506530, 64.21532580903964060, 3.665158340976913287 ) ) ;
#4068=CARTESIAN_POINT ( 'NONE',  ( 10.50357756723356140, 59.39757829809867928, -1.000000000000000000 ) ) ;
#4069=EDGE_CURVE ( 'NONE', #4188, #7364, #36876, .T. ) ;
#4082=CARTESIAN_POINT ( 'NONE',  ( 80.69089980977662435, 64.07786826041912320, 3.533418250979425412 ) ) ;
#4084=DIRECTION ( 'NONE',  ( 0.000000000000000000, 0.000000000000000000, 1.000000000000000000 ) ) ;
#4096=CARTESIAN_POINT ( 'NONE',  ( 80.84084779726516956, 63.39242392479005161, -3.526329879082124030 ) ) ;
#4098=DIRECTION ( 'NONE',  ( -0.3103887796125159859, -0.9506097019758703581, 0.000000000000000000 ) ) ;
#4106=CARTESIAN_POINT ( 'NONE',  ( 81.03127633846453648, 61.72971393008351981, -2.526545245021137198 ) ) ;
#4111=ORIENTED_EDGE ( 'NONE', *, *, #40113, .F. ) ;
#4119=CARTESIAN_POINT ( 'NONE',  ( 72.25564410411975302, 59.56945073910184618, 3.929231508797896399 ) ) ;
#4128=CARTESIAN_POINT ( 'NONE',  ( 81.57183863168549465, 63.40013557970607394, 3.079343812564428351 ) ) ;
#4141=DIRECTION ( 'NONE',  ( 0.000000000000000000, -0.000000000000000000, -1.000000000000000000 ) ) ;
#4156=CARTESIAN_POINT ( 'NONE',  ( 82.43319509988585025, 63.84109541104518115, -1.838010297257801851 ) ) ;
#4160=CARTESIAN_POINT ( 'NONE',  ( 75.82377327986996818, 62.28299708301697279, -3.825872951952260959 ) ) ;
#4164=CARTESIAN_POINT ( 'NONE',  ( 78.09760114435867706, 60.38799743245716911, 2.844364419925230258 ) ) ;
#4172=CARTESIAN_POINT ( 'NONE',  ( 79.73837173991839222, 66.20136991484933731, 1.918505602738378446 ) ) ;
#4185=CARTESIAN_POINT ( 'NONE',  ( -63.57019645983813660, 43.64021813969844743, -2.910064772521099741 ) ) ;
#4188=VERTEX_POINT ( 'NONE', #11171 ) ;
#4191=CARTESIAN_POINT ( 'NONE',  ( 67.15438370417800229, 58.05139456359000150, -3.999036733496184048 ) ) ;
#4203=CARTESIAN_POINT ( 'NONE',  ( 81.23507808130547403, 61.62583295638711434, 2.125034277891707291 ) ) ;
#4207=CARTESIAN_POINT ( 'NONE',  ( 80.20105671851041507, 61.18620973470589774, -2.431999527814464379 ) ) ;
#4210=CARTESIAN_POINT ( 'NONE',  ( 81.59312859631556591, 63.05267747590616523, -3.015199126117770412 ) ) ;
#4211=CARTESIAN_POINT ( 'NONE',  ( 78.24346468842466606, 65.07400588416957987, 2.889371261047450457 ) ) ;
#4212=EDGE_CURVE ( 'NONE', #33614, #29368, #1952, .T. ) ;
#4215=CARTESIAN_POINT ( 'NONE',  ( 82.39191784114052552, 64.57324092874044652, 1.480606629405690544 ) ) ;
#4217=CARTESIAN_POINT ( 'NONE',  ( -64.08758708074093136, 43.28886537931755640, 1.984762278319444961 ) ) ;
#4219=CARTESIAN_POINT ( 'NONE',  ( -64.14095127866889356, 35.19432717188715287, -4.537732464557278966 ) ) ;
#4236=ORIENTED_EDGE ( 'NONE', *, *, #11636, .T. ) ;
#4237=CARTESIAN_POINT ( 'NONE',  ( 66.56396446968585678, 57.85070090013417854, 3.999903336036485069 ) ) ;
#4239=CARTESIAN_POINT ( 'NONE',  ( -64.08758708074093136, 38.76906266698302517, 3.999999999999998668 ) ) ;
#4245=PRODUCT_CONTEXT ( 'NONE', #14482, 'mechanical' ) ;
#4253=CARTESIAN_POINT ( 'NONE',  ( 78.52976371562807856, 65.87711177338782420, -1.796258654643035912 ) ) ;
#4255=CARTESIAN_POINT ( 'NONE',  ( 80.71678001510488798, 62.11300466482759219, 3.061371641637220087 ) ) ;
#4264=CARTESIAN_POINT ( 'NONE',  ( 77.97558924392689050, 65.55221975275186708, -1.909876039719648588 ) ) ;
#4272=CARTESIAN_POINT ( 'NONE',  ( 81.03825699591070020, 63.48946937969523674, 3.448515284080272192 ) ) ;
#4278=DIRECTION ( 'NONE',  ( -0.000000000000000000, -0.000000000000000000, -1.000000000000000000 ) ) ;
#4282=B_SPLINE_CURVE_WITH_KNOTS ( 'NONE', 3,
 ( #23041, #34812, #617, #35607, #35010, #9868, #4311, #16832, #25721, #10261, #10059, #10657, #29417, #3925, #1231, #26332, #13764, #38866, #19135, #22442, #6784, #31908, #14753, #33320, #13957, #10855 ),
 .UNSPECIFIED., .F., .F.,
 ( 4, 2, 2, 2, 2, 2, 2, 2, 2, 2, 2, 2, 4 ),
 ( 0.000000000000000000, 0.0001695542964127800731, 0.0003391085928255601462, 0.0005086628892383401922, 0.0006782171856511202924, 0.001017325778476677999, 0.001356434371302235814, 0.002034651556953352095, 0.002712868742604468593, 0.003391085928255584223, 0.004069303113906699854, 0.004747520299557816785, 0.005425737485208931982 ),
 .UNSPECIFIED. ) ;
#4283=CARTESIAN_POINT ( 'NONE',  ( 69.23715119732055712, 58.71109548446294468, 3.988427515945585089 ) ) ;
#4285=ADVANCED_FACE ( 'NONE', ( #2359 ), #8084, .T. ) ;
#4289=CARTESIAN_POINT ( 'NONE',  ( 79.39927235112092774, 65.46614203786572261, -2.932725070486261743 ) ) ;
#4295=CARTESIAN_POINT ( 'NONE',  ( -59.65099889957326695, 26.74201272916463878, 6.661192808835134649 ) ) ;
#4304=CARTESIAN_POINT ( 'NONE',  ( 80.80704226153129355, 62.39036624599364700, -3.220356845322062789 ) ) ;
#4306=CARTESIAN_POINT ( 'NONE',  ( 81.09335400879911049, 61.74513338965306275, 2.494286432550478771 ) ) ;
#4311=CARTESIAN_POINT ( 'NONE',  ( -58.97292984558871609, 28.26388549929947303, -6.370425507473826521 ) ) ;
#4314=CARTESIAN_POINT ( 'NONE',  ( -64.08758708074196875, 43.90637424960519297, -1.960639441496169200 ) ) ;
#4315=CARTESIAN_POINT ( 'NONE',  ( 71.19973236181560594, 58.84349373463830091, 3.887826097256417590 ) ) ;
#4319=VERTEX_POINT ( 'NONE', #39804 ) ;
#4325=CARTESIAN_POINT ( 'NONE',  ( 80.93493477626120125, 64.98323193449216717, 3.125232205748817549 ) ) ;
#4345=ADVANCED_FACE ( 'NONE', ( #37517 ), #750, .T. ) ;
#4347=CARTESIAN_POINT ( 'NONE',  ( 66.27376694609004915, 57.73522568913436004, -4.000000000000000000 ) ) ;
#4354=CARTESIAN_POINT ( 'NONE',  ( -57.68674048389793541, 29.08812126441105406, -4.503248736989433176 ) ) ;
#4358=AXIS2_PLACEMENT_3D ( 'NONE', #9720, #18776, #27634 ) ;
#4359=CARTESIAN_POINT ( 'NONE',  ( 82.39984057372335258, 63.46184634947035619, -2.021051955677194201 ) ) ;
#4363=CARTESIAN_POINT ( 'NONE',  ( 74.67253486855700828, 63.25418332940030552, -3.074209570828856819 ) ) ;
#4367=CARTESIAN_POINT ( 'NONE',  ( 76.06955384389382857, 61.76325957217472506, 3.887901781368110488 ) ) ;
#4373=CARTESIAN_POINT ( 'NONE',  ( 80.71833143474502492, 65.93084270547805659, 2.217414436011085677 ) ) ;
#4381=CARTESIAN_POINT ( 'NONE',  ( 74.75340671132555315, 59.31352934624568718, 3.344778443633103837 ) ) ;
#4396=CARTESIAN_POINT ( 'NONE',  ( 67.43143073044585378, 58.20127550988744503, -3.998123450764769604 ) ) ;
#4397=ADVANCED_FACE ( 'NONE', ( #18575 ), #34270, .T. ) ;
#4398=CARTESIAN_POINT ( 'NONE',  ( -65.15514661499977933, 34.97220226750606997, -6.888442104241536690 ) ) ;
#4409=CARTESIAN_POINT ( 'NONE',  ( 80.98905497205693393, 62.76708948751929995, 3.312281065658538193 ) ) ;
#4412=CARTESIAN_POINT ( 'NONE',  ( 78.68856915541800845, 64.27844437337117256, -3.554489553981586170 ) ) ;
#4416=CARTESIAN_POINT ( 'NONE',  ( 80.04208101465897585, 65.56312698749695755, -2.920975158733597699 ) ) ;
#4417=CARTESIAN_POINT ( 'NONE',  ( 79.09261123048416664, 64.22416776617161815, 3.612066323963887715 ) ) ;
#4421=CARTESIAN_POINT ( 'NONE',  ( 78.99593020234610208, 66.21156118037409044, 1.070820504726896605 ) ) ;
#4424=CARTESIAN_POINT ( 'NONE',  ( -64.46937875527684980, 36.54399046018806985, -5.728582434991689176 ) ) ;
#4443=CARTESIAN_POINT ( 'NONE',  ( 66.82596693864583415, 58.04328079001189877, 3.997688572870336188 ) ) ;
#4445=CARTESIAN_POINT ( 'NONE',  ( 73.06729433089581960, 60.84378783247667144, -3.914122288852232678 ) ) ;
#4459=CARTESIAN_POINT ( 'NONE',  ( 79.88928440695104882, 63.65969051258252165, -3.720735635808768205 ) ) ;
#4460=( BOUNDED_SURFACE ( )  B_SPLINE_SURFACE ( 3, 2, ( 
 ( #19448, #16345, #19652 ),
 ( #7088, #32223, #28918 ),
 ( #32418, #20047, #1139 ),
 ( #28714, #926, #25828 ),
 ( #6892, #19243, #4025 ),
 ( #4217, #38775, #16151 ),
 ( #9769, #13061, #16543 ),
 ( #1336, #29123, #29524 ),
 ( #526, #25423, #25623 ),
 ( #35114, #13262, #16736 ),
 ( #3626, #6695, #9971 ),
 ( #13460, #26035, #38365 ),
 ( #22352, #32021, #31811 ),
 ( #7488, #38167, #38569 ) ),
 .UNSPECIFIED., .F., .F., .T. ) 
 B_SPLINE_SURFACE_WITH_KNOTS ( ( 4, 2, 2, 2, 2, 2, 4 ),
 ( 3, 3 ),
 ( 0.000000000000000000, 0.0004485899915298040600, 0.0008971799830596081200, 0.001345769974589412126, 0.001794359966119216240, 0.002691539949178824252, 0.003588719932238432480 ),
 ( 0.000000000000000000, 1.000000000000000000 ),
 .UNSPECIFIED. ) 
 GEOMETRIC_REPRESENTATION_ITEM ( )  RATIONAL_B_SPLINE_SURFACE ( (
 ( 1.000000000000000000, 0.9000259740535757613, 1.000000000000000000),
 ( 1.000000000000000000, 0.9000175163599423156, 1.000000000000000000),
 ( 1.000000000000000000, 0.8985936556292808408, 1.000000000000000000),
 ( 1.000000000000000000, 0.8930319130234418701, 1.000000000000000000),
 ( 1.000000000000000000, 0.8888779410518012902, 1.000000000000000000),
 ( 1.000000000000000000, 0.8784198174355972721, 1.000000000000000000),
 ( 1.000000000000000000, 0.8719969190870759945, 1.000000000000000000),
 ( 1.000000000000000000, 0.8575109182637734584, 1.000000000000000000),
 ( 1.000000000000000000, 0.8493613801775528049, 1.000000000000000000),
 ( 1.000000000000000000, 0.8227151417012925627, 1.000000000000000000),
 ( 1.000000000000000000, 0.8025165990303427810, 1.000000000000000000),
 ( 1.000000000000000000, 0.7574223494978716831, 1.000000000000000000),
 ( 1.000000000000000000, 0.7332909362864591385, 1.000000000000000000),
 ( 1.000000000000000000, 0.7071067811865473507, 1.000000000000000000) ) ) 
 REPRESENTATION_ITEM ( '' )  SURFACE ( )  );
#4462=CARTESIAN_POINT ( 'NONE',  ( 80.93996669421811418, 61.38942684853007847, 2.064111563736219956 ) ) ;
#4470=CARTESIAN_POINT ( 'NONE',  ( 78.60787044352795760, 65.99999220767536201, -1.312857279933637766 ) ) ;
#4476=CARTESIAN_POINT ( 'NONE',  ( 81.23287006775859709, 61.35999619221078660, 1.467306180864043075 ) ) ;
#4487=CARTESIAN_POINT ( 'NONE',  ( 69.15563817390996348, 58.92225492517195562, 3.988427515945577095 ) ) ;
#4493=CARTESIAN_POINT ( 'NONE',  ( 80.41878079785792011, 63.93588341273047604, -3.625945587094182354 ) ) ;
#4496=CARTESIAN_POINT ( 'NONE',  ( -58.97877168559173100, 27.59157091290065367, 6.753965997777578778 ) ) ;
#4503=CARTESIAN_POINT ( 'NONE',  ( 79.79930721375663438, 64.34646279424465831, -3.632888195267881315 ) ) ;
#4505=CARTESIAN_POINT ( 'NONE',  ( 80.88543547514460386, 62.41573260227067976, 3.197674131580384493 ) ) ;
#4520=CARTESIAN_POINT ( 'NONE',  ( -64.36865852185155745, 34.97220226750606997, 7.506047544094573531 ) ) ;
#4523=CARTESIAN_POINT ( 'NONE',  ( 78.83984420990493902, 66.12288285737184879, 1.382728580145343278 ) ) ;
#4544=CARTESIAN_POINT ( 'NONE',  ( -75.45330471031414277, 33.71485196875532608, 9.800414904976365804 ) ) ;
#4545=FACE_OUTER_BOUND ( 'NONE', #28914, .T. ) ;
#4547=DIRECTION ( 'NONE',  ( -0.000000000000000000, -0.000000000000000000, -1.000000000000000000 ) ) ;
#4548=CARTESIAN_POINT ( 'NONE',  ( -55.16208421294561504, 31.22611435454061990, -1.446432346866528995 ) ) ;
#4553=CARTESIAN_POINT ( 'NONE',  ( 82.13040900219759521, 64.82864533757665981, -1.905332024691357429 ) ) ;
#4560=CARTESIAN_POINT ( 'NONE',  ( 76.30453859000765249, 59.72919098693703432, 3.074209570828593918 ) ) ;
#4568=CARTESIAN_POINT ( 'NONE',  ( 81.16843721835843439, 61.30356250071481128, 1.032522165606394315 ) ) ;
#4571=ADVANCED_FACE ( 'NONE', ( #23304 ), #4697, .T. ) ;
#4577=CARTESIAN_POINT ( 'NONE',  ( 35.94200923520244828, 151.3264224549853907, 1.000000000000000000 ) ) ;
#4582=CARTESIAN_POINT ( 'NONE',  ( -63.68920958294118151, 44.29446941693485229, -1.843112653903773657 ) ) ;
#4588=CARTESIAN_POINT ( 'NONE',  ( 67.14253272251396254, 58.08395421452478757, -3.998868826385352460 ) ) ;
#4596=CARTESIAN_POINT ( 'NONE',  ( 35.94200923520244828, 151.3264224549853907, 1.000000000000000000 ) ) ;
#4601=CARTESIAN_POINT ( 'NONE',  ( 80.95271419388603817, 62.75148163162413795, 3.324099845469156378 ) ) ;
#4604=CARTESIAN_POINT ( 'NONE',  ( 79.34756916856697728, 63.37933396398980079, -3.765547211956733697 ) ) ;
#4607=CARTESIAN_POINT ( 'NONE',  ( 81.34875679480646227, 63.64560584541077759, -3.283621700554755218 ) ) ;
#4608=CARTESIAN_POINT ( 'NONE',  ( 78.45565513354563336, 64.70068626995113448, 3.258123098320686140 ) ) ;
#4609=EDGE_CURVE ( 'NONE', #18695, #20708, #17913, .T. ) ;
#4613=CARTESIAN_POINT ( 'NONE',  ( 81.16957891225079891, 61.30398062001319914, 1.002944004955704127 ) ) ;
#4616=CARTESIAN_POINT ( 'NONE',  ( -64.78745217040265914, 34.77601383833022197, -6.355070236020407215 ) ) ;
#4635=CARTESIAN_POINT ( 'NONE',  ( 66.43088956075774831, 57.76580747938982796, 4.000000000000006217 ) ) ;
#4636=CARTESIAN_POINT ( 'NONE',  ( 72.54144496250529528, 58.88102433069186503, -3.699617110138616383 ) ) ;
#4648=CARTESIAN_POINT ( 'NONE',  ( 78.51047153333161077, 65.93088068117907596, -1.448968528258141486 ) ) ;
#4650=CARTESIAN_POINT ( 'NONE',  ( 78.83205648568262802, 65.58035453618819588, 2.615973384260660950 ) ) ;
#4653=CYLINDRICAL_SURFACE ( 'NONE', #12459, 1.000000000000003997 ) ;
#4656=CARTESIAN_POINT ( 'NONE',  ( 78.31607304441834572, 65.79307132853784879, -1.652946521066924745 ) ) ;
#4664=CARTESIAN_POINT ( 'NONE',  ( 80.10206815703588745, 64.89240018571257451, 3.380792992375215356 ) ) ;
#4675=CARTESIAN_POINT ( 'NONE',  ( 67.94738262351316394, 58.59965392607728063, 3.985705108533788010 ) ) ;
#4678=CARTESIAN_POINT ( 'NONE',  ( -64.08758708074093136, 41.04287353446839859, -3.000000000000000000 ) ) ;
#4680=CARTESIAN_POINT ( 'NONE',  ( 81.20006484400859392, 61.61449114502521951, -2.147349935851008862 ) ) ;
#4681=DIRECTION ( 'NONE',  ( 0.8888117386314196011, 0.4582725098355703852, 0.000000000000000000 ) ) ;
#4691=CARTESIAN_POINT ( 'NONE',  ( 80.69932603693776230, 62.65430898200600751, -3.392181771880276919 ) ) ;
#4694=CARTESIAN_POINT ( 'NONE',  ( 80.50045704793726031, 63.23530725187647050, 3.614403801066808697 ) ) ;
#4697=TOROIDAL_SURFACE ( 'NONE', #22468, 98.38357402481355507, 3.000000000000000000 ) ;
#4700=DIRECTION ( 'NONE',  ( -1.000000000000000000, 0.000000000000000000, 0.000000000000000000 ) ) ;
#4702=CARTESIAN_POINT ( 'NONE',  ( -81.07947155388369254, 30.81399289130168384, -46.17089178453873188 ) ) ;
#4712=CARTESIAN_POINT ( 'NONE',  ( 81.42106526723539162, 61.53660244640637700, 1.679744683813965578 ) ) ;
#4738=ORIENTED_EDGE ( 'NONE', *, *, #14908, .F. ) ;
#4739=CARTESIAN_POINT ( 'NONE',  ( -57.16504416091206053, 33.41445838748276742, -3.999999999999999112 ) ) ;
#4741=ORIENTED_EDGE ( 'NONE', *, *, #37378, .T. ) ;
#4743=CARTESIAN_POINT ( 'NONE',  ( 81.16905975791091521, 61.30379048835199995, -1.022614849746412924 ) ) ;
#4750=CARTESIAN_POINT ( 'NONE',  ( 74.93610893867889899, 61.23939191379614755, 3.912919437578919357 ) ) ;
#4752=CARTESIAN_POINT ( 'NONE',  ( -64.08758708074093136, 37.05642372032221488, 4.717683440829013364 ) ) ;
#4758=CARTESIAN_POINT ( 'NONE',  ( 81.07711124303949646, 65.42186869171266039, 2.645340681430091490 ) ) ;
#4768=FACE_OUTER_BOUND ( 'NONE', #14978, .T. ) ;
#4769=CARTESIAN_POINT ( 'NONE',  ( -63.99293516169446150, 35.89893413629672381, 12.49999999999999645 ) ) ;
#4777=CARTESIAN_POINT ( 'NONE',  ( 67.48690106321139126, 58.04989387035797677, -3.996173465816880377 ) ) ;
#4783=CARTESIAN_POINT ( 'NONE',  ( 78.60788762842503274, 66.00000440856842943, 1.312824883943342513 ) ) ;
#4786=EDGE_CURVE ( 'NONE', #20345, #33155, #18498, .T. ) ;
#4789=DIRECTION ( 'NONE',  ( -1.000000000000000000, 0.000000000000000000, 0.000000000000000000 ) ) ;
#4794=CARTESIAN_POINT ( 'NONE',  ( 81.06670574969137988, 62.21556664890213284, 2.940771700540082634 ) ) ;
#4797=CARTESIAN_POINT ( 'NONE',  ( 79.06939945841564565, 62.09164075111537073, -3.616565173810662337 ) ) ;
#4798=( BOUNDED_CURVE ( )  B_SPLINE_CURVE ( 3, ( #12143, #18525, #8648, #33794 ),
 .UNSPECIFIED., .F., .T. ) 
 B_SPLINE_CURVE_WITH_KNOTS ( ( 4, 4 ),
 ( 4.564251139902668619, 4.712388980384691450 ),
 .UNSPECIFIED. ) 
 CURVE ( )  GEOMETRIC_REPRESENTATION_ITEM ( )  RATIONAL_B_SPLINE_CURVE ( ( 1.000000000000000000, 0.9981721009331390171, 0.9981721009331390171, 1.000000000000000000 ) ) 
 REPRESENTATION_ITEM ( '' )  );
#4801=CARTESIAN_POINT ( 'NONE',  ( 81.16101395366625582, 61.30084446962304412, -1.089225060638851161 ) ) ;
#4802=CARTESIAN_POINT ( 'NONE',  ( 78.34436985318809832, 64.89959302631085336, 3.091829831932942252 ) ) ;
#4807=CARTESIAN_POINT ( 'NONE',  ( 82.43454424851958606, 64.20405324974034045, 1.755995906647955795 ) ) ;
#4811=CARTESIAN_POINT ( 'NONE',  ( -62.78278205347345420, 35.70412497698336551, -5.569918731383365795 ) ) ;
#4821=CARTESIAN_POINT ( 'NONE',  ( -66.99872204295122913, 28.48507918597134037, 12.49999999999999645 ) ) ;
#4829=CARTESIAN_POINT ( 'NONE',  ( 66.27376694608996388, 57.73522568913447373, 4.000000000000000000 ) ) ;
#4830=CARTESIAN_POINT ( 'NONE',  ( 73.59222858082205221, 59.63291812028631966, -3.785151435545463183 ) ) ;
#4835=ADVANCED_FACE ( 'NONE', ( #4545 ), #39098, .F. ) ;
#4843=CARTESIAN_POINT ( 'NONE',  ( 79.84618440311783161, 63.29375160576378079, -3.738478073092017517 ) ) ;
#4845=CARTESIAN_POINT ( 'NONE',  ( 78.72519613238203817, 65.48187369539458302, 2.679976076788566530 ) ) ;
#4855=CIRCLE ( 'NONE', #34485, 64.42751648247021024 ) ;
#4858=CARTESIAN_POINT ( 'NONE',  ( 79.20700709577714349, 65.89182355360533450, 2.372413575842139188 ) ) ;
#4859=DIRECTION ( 'NONE',  ( 0.000000000000000000, 0.000000000000000000, 1.000000000000000000 ) ) ;
#4864=CARTESIAN_POINT ( 'NONE',  ( -64.85784325972055342, 34.81586596186931359, 6.466735817496056526 ) ) ;
#4867=CARTESIAN_POINT ( 'NONE',  ( 67.85873555399604129, 57.94375731920307260, 3.976226663256418714 ) ) ;
#4872=ADVANCED_FACE ( 'NONE', ( #11899 ), #2069, .F. ) ;
#4873=CARTESIAN_POINT ( 'NONE',  ( 80.68504733838216225, 63.31860838049917106, -3.572022490087447988 ) ) ;
#4876=CARTESIAN_POINT ( 'NONE',  ( -59.64698295252581772, 26.74637988513383391, 7.056669117542213598 ) ) ;
#4879=EDGE_CURVE ( 'NONE', #38151, #1666, #7971, .T. ) ;
#4885=CARTESIAN_POINT ( 'NONE',  ( 81.06091538032714539, 61.57736434115989965, -2.238287240292677449 ) ) ;
#4887=CARTESIAN_POINT ( 'NONE',  ( 78.85680892556288768, 65.81502797165208563, 2.238287240292551772 ) ) ;
#4895=CARTESIAN_POINT ( 'NONE',  ( -63.84790524989457339, 35.84013490037983729, -7.344445564913361757 ) ) ;
#4903=LINE ( 'NONE', #17435, #13645 ) ;
#4904=CARTESIAN_POINT ( 'NONE',  ( 80.61314501154876666, 64.81116531652718038, 3.343039074470575578 ) ) ;
#4928=DIRECTION ( 'NONE',  ( 1.000000000000000000, 0.000000000000000000, 0.000000000000000000 ) ) ;
#4933=ORIENTED_EDGE ( 'NONE', *, *, #14864, .T. ) ;
#4939=CARTESIAN_POINT ( 'NONE',  ( -56.64002613362055882, 29.83241628681515323, -1.779850828381725814 ) ) ;
#4945=CARTESIAN_POINT ( 'NONE',  ( 79.28422506984790630, 66.27750502035057423, -1.322881339814841573 ) ) ;
#4953=CARTESIAN_POINT ( 'NONE',  ( 73.75428705932469597, 62.33035115498114465, 3.485789274173696661 ) ) ;
#4956=CARTESIAN_POINT ( 'NONE',  ( -64.08758708074093136, 36.76354445449373998, 3.435823087746894267 ) ) ;
#4958=DIRECTION ( 'NONE',  ( 0.9637806624122927657, -0.2666961468790326473, 1.731454049777543614E-15 ) ) ;
#4962=CARTESIAN_POINT ( 'NONE',  ( 80.71114116412925910, 65.59088185864123943, 2.713791510777070037 ) ) ;
#4982=CARTESIAN_POINT ( 'NONE',  ( 67.39181666045010388, 58.30934502646129403, -3.993945454764282310 ) ) ;
#4995=CARTESIAN_POINT ( 'NONE',  ( 81.74417899799368570, 61.69322615925144504, -1.090531591958677327 ) ) ;
#4996=CARTESIAN_POINT ( 'NONE',  ( 79.75420125634298074, 65.05222905597021565, 3.324099845469147052 ) ) ;
#4999=CARTESIAN_POINT ( 'NONE',  ( 78.65108613080990096, 60.71083206350689210, -2.889099817377091650 ) ) ;
#5003=CARTESIAN_POINT ( 'NONE',  ( 81.29424054903955721, 63.61798189665201875, -3.316380171282754308 ) ) ;
#5004=CARTESIAN_POINT ( 'NONE',  ( 77.75442706423145012, 65.27774734742538953, 2.313798345564205494 ) ) ;
#5006=CARTESIAN_POINT ( 'NONE',  ( -63.08379346057677139, 18.80112958435941906, 12.49999999999999645 ) ) ;
#5007=CARTESIAN_POINT ( 'NONE',  ( 81.92984576605168456, 61.94483778347748881, 1.306649493516907290 ) ) ;
#5031=ORIENTED_EDGE ( 'NONE', *, *, #11598, .F. ) ;
#5033=CARTESIAN_POINT ( 'NONE',  ( 66.42990020876143831, 57.76860247958609307, 4.000000000000007105 ) ) ;
#5034=CARTESIAN_POINT ( 'NONE',  ( 72.61754431144450450, 61.86111285056382059, -3.476886323448412419 ) ) ;
#5044=DIRECTION ( 'NONE',  ( 1.000000000000000000, 0.000000000000000000, 0.000000000000000000 ) ) ;
#5045=FACE_OUTER_BOUND ( 'NONE', #26119, .T. ) ;
#5048=CARTESIAN_POINT ( 'NONE',  ( 80.48656635915796187, 62.05344631111049836, -3.128253119413326289 ) ) ;
#5050=CARTESIAN_POINT ( 'NONE',  ( 79.98443850338786376, 63.35773072451035404, 3.725738571856552106 ) ) ;
#5064=CARTESIAN_POINT ( 'NONE',  ( 78.77361741396555317, 66.07891176884449180, 1.467306180864091703 ) ) ;
#5071=AXIS2_PLACEMENT_3D ( 'NONE', #2172, #39827, #4098 ) ;
#5078=CARTESIAN_POINT ( 'NONE',  ( 67.36017643331848603, 58.39563743223260417, 3.987264345885670025 ) ) ;
#5085=CARTESIAN_POINT ( 'NONE',  ( -58.33732831438487665, 31.01206039140789983, 4.738023936417821602 ) ) ;
#5087=ORIENTED_EDGE ( 'NONE', *, *, #16076, .F. ) ;
#5091=CARTESIAN_POINT ( 'NONE',  ( 78.61081429290072720, 65.94468767047428059, -1.703597047176659940 ) ) ;
#5094=CARTESIAN_POINT ( 'NONE',  ( 79.09343976728347059, 65.54176476638913584, 2.787474064117257733 ) ) ;
#5100=CARTESIAN_POINT ( 'NONE',  ( 74.30211141138923381, 59.57442121254392475, -3.624554307378899054 ) ) ;
#5107=ORIENTED_EDGE ( 'NONE', *, *, #23300, .T. ) ;
#5113=CARTESIAN_POINT ( 'NONE',  ( 78.68416471612012231, 66.05417514313617744, 1.083735637653860495 ) ) ;
#5115=CARTESIAN_POINT ( 'NONE',  ( -75.45330471031414277, 33.71485196875532608, -9.800414904976365804 ) ) ;
#5116=ORIENTED_EDGE ( 'NONE', *, *, #12561, .F. ) ;
#5138=FACE_OUTER_BOUND ( 'NONE', #3265, .T. ) ;
#5142=CARTESIAN_POINT ( 'NONE',  ( 81.14259283377289478, 61.75830469257449806, -2.468641556981999496 ) ) ;
#5149=CARTESIAN_POINT ( 'NONE',  ( 79.53094818655489462, 66.25005786596102553, -1.601045042264588325 ) ) ;
#5156=CARTESIAN_POINT ( 'NONE',  ( 75.35164290873603932, 61.82650661013094862, 3.882889210543307268 ) ) ;
#5157=VERTEX_POINT ( 'NONE', #9427 ) ;
#5164=CARTESIAN_POINT ( 'NONE',  ( -65.27430759792673598, 36.41843883184812114, 8.800656633793924044 ) ) ;
#5165=CARTESIAN_POINT ( 'NONE',  ( 81.84810375386635428, 62.06244373962204008, 1.965143080302226508 ) ) ;
#5168=DIRECTION ( 'NONE',  ( 0.000000000000000000, 0.000000000000000000, 1.000000000000000000 ) ) ;
#5185=CARTESIAN_POINT ( 'NONE',  ( 66.84954949145740954, 57.97782447864501165, -3.999382933223863734 ) ) ;
#5197=CARTESIAN_POINT ( 'NONE',  ( 80.38645948019593845, 66.31981033314001195, -1.103079483641125069 ) ) ;
#5198=CARTESIAN_POINT ( 'NONE',  ( 79.38068533922456993, 65.45287079212486958, 2.940771700540096401 ) ) ;
#5202=CARTESIAN_POINT ( 'NONE',  ( 77.83481221125377658, 64.51125116100624268, -3.218236826935536588 ) ) ;
#5205=CARTESIAN_POINT ( 'NONE',  ( 81.25398435008909814, 63.24110186484434593, -3.279590910092189393 ) ) ;
#5207=CARTESIAN_POINT ( 'NONE',  ( 78.95981124517781780, 62.31610944509175454, 3.691425412862327171 ) ) ;
#5210=CARTESIAN_POINT ( 'NONE',  ( 79.31644831670718077, 66.29498274501730748, 1.214491505233689983 ) ) ;
#5212=CARTESIAN_POINT ( 'NONE',  ( 10.50357756723356140, 59.39757829809867928, 4.000000000000000000 ) ) ;
#5216=EDGE_LOOP ( 'NONE', ( #17746, #27735, #38508, #30579 ) ) ;
#5220=DIRECTION ( 'NONE',  ( -0.000000000000000000, -0.000000000000000000, -1.000000000000000000 ) ) ;
#5230=DIRECTION ( 'NONE',  ( 0.000000000000000000, 0.000000000000000000, 1.000000000000000000 ) ) ;
#5235=CARTESIAN_POINT ( 'NONE',  ( 66.42792150476880408, 57.77419247997864460, 4.000000000000008882 ) ) ;
#5236=CARTESIAN_POINT ( 'NONE',  ( 72.66268786488812736, 61.76016136843576021, -3.552420216958366517 ) ) ;
#5239=CARTESIAN_POINT ( 'NONE',  ( -63.08758708074093136, 36.14363715547679590, 3.800414904976364472 ) ) ;
#5250=CARTESIAN_POINT ( 'NONE',  ( 79.70629046221083058, 63.56464109829104814, -3.738478073092015297 ) ) ;
#5252=CARTESIAN_POINT ( 'NONE',  ( 81.24504193829289989, 64.75648403698978939, -3.071899782094857478 ) ) ;
#5253=CARTESIAN_POINT ( 'NONE',  ( 80.75607764207482830, 61.50646045904602488, 2.414331286641654195 ) ) ;
#5254=DIRECTION ( 'NONE',  ( -1.000000000000000000, 0.000000000000000000, 0.000000000000000000 ) ) ;
#5272=CARTESIAN_POINT ( 'NONE',  ( -64.58659014339545479, 34.69724588627169481, 5.982304021381975367 ) ) ;
#5274=FACE_OUTER_BOUND ( 'NONE', #27150, .T. ) ;
#5278=CARTESIAN_POINT ( 'NONE',  ( 67.93540907064681278, 58.63163702635943508, 3.982418445723137967 ) ) ;
#5290=ORIENTED_EDGE ( 'NONE', *, *, #21307, .T. ) ;
#5292=CARTESIAN_POINT ( 'NONE',  ( 80.45282402617027628, 62.88786617374236698, -3.531602295408444281 ) ) ;
#5296=CARTESIAN_POINT ( 'NONE',  ( 81.06761308752996342, 61.31222891353765192, 1.660510093083209737 ) ) ;
#5302=CARTESIAN_POINT ( 'NONE',  ( 74.23991766213896426, 61.26593220986219279, -3.911020515999897640 ) ) ;
#5319=CARTESIAN_POINT ( 'NONE',  ( 80.84588251005118309, 64.54609234697676357, 3.375310687858769310 ) ) ;
#5322=ORIENTED_EDGE ( 'NONE', *, *, #4069, .T. ) ;
#5323=DIRECTION ( 'NONE',  ( -0.000000000000000000, 0.000000000000000000, 1.000000000000000000 ) ) ;
#5326=DIRECTION ( 'NONE',  ( -0.000000000000000000, -0.000000000000000000, -1.000000000000000000 ) ) ;
#5336=CARTESIAN_POINT ( 'NONE',  ( 78.78605531729427014, 66.08782950793384714, -1.450104216466339802 ) ) ;
#5340=DIRECTION ( 'NONE',  ( -1.000000000000000000, 0.000000000000000000, 0.000000000000000000 ) ) ;
#5348=CARTESIAN_POINT ( 'NONE',  ( 80.60461247708464327, 63.28149962716670984, -3.592474444481850604 ) ) ;
#5349=CARTESIAN_POINT ( 'NONE',  ( -58.98400447371446376, 28.74159977738611715, -6.613141227606677219 ) ) ;
#5355=CARTESIAN_POINT ( 'NONE',  ( 82.04158296082394486, 62.38656886254256051, -2.040045296073659920 ) ) ;
#5361=CARTESIAN_POINT ( 'NONE',  ( 74.72764284544139457, 63.14151651683601330, 3.204585025132375975 ) ) ;
#5368=CARTESIAN_POINT ( 'NONE',  ( 81.92776049059212085, 62.60942412355771580, 2.397965335136732712 ) ) ;
#5380=CARTESIAN_POINT ( 'NONE',  ( -72.95330471031414277, 33.71485196875532608, -46.17089178453873188 ) ) ;
#5386=CARTESIAN_POINT ( 'NONE',  ( 66.88099813915303571, 57.89052526007606758, -3.999029912548879739 ) ) ;
#5400=CARTESIAN_POINT ( 'NONE',  ( 81.60972716517450465, 65.70321483603501633, -1.303631908149876617 ) ) ;
#5401=CARTESIAN_POINT ( 'NONE',  ( 78.73074668855629454, 66.04592173387707987, 1.531260274641973895 ) ) ;
#5405=CARTESIAN_POINT ( 'NONE',  ( 78.38159772055732333, 63.47233311668937006, -3.766285651913922283 ) ) ;
#5408=CARTESIAN_POINT ( 'NONE',  ( 81.39159673219582203, 61.52361671445444102, -1.704083397383978626 ) ) ;
#5409=CARTESIAN_POINT ( 'NONE',  ( 79.17274970258583267, 61.87635977960864153, 3.505091495581067029 ) ) ;
#5414=CARTESIAN_POINT ( 'NONE',  ( 82.46885687451873537, 64.22182207139040599, 1.617049763655828531 ) ) ;
#5424=DIRECTION ( 'NONE',  ( -0.9267318687906771491, 0.3757233601570964532, 0.000000000000000000 ) ) ;
#5429=DIRECTION ( 'NONE',  ( -1.000000000000000000, -3.568978458213368244E-15, 0.000000000000000000 ) ) ;
#5432=FACE_OUTER_BOUND ( 'NONE', #36298, .T. ) ;
#5439=CARTESIAN_POINT ( 'NONE',  ( 66.41308122482404031, 57.81611748292269937, 4.000000000000022204 ) ) ;
#5440=CARTESIAN_POINT ( 'NONE',  ( 68.97355662219305827, 59.39279559060015146, -3.921432738910643589 ) ) ;
#5457=EDGE_LOOP ( 'NONE', ( #36330, #27625, #20881, #33478 ) ) ;
#5458=CARTESIAN_POINT ( 'NONE',  ( 79.56639652130381535, 63.83553059081831549, -3.738478073092013076 ) ) ;
#5460=CARTESIAN_POINT ( 'NONE',  ( 81.35720881915658254, 61.41209416231795615, -1.323744132979588928 ) ) ;
#5461=CARTESIAN_POINT ( 'NONE',  ( 80.87678155331657592, 61.19751495238255501, 1.521414672925271772 ) ) ;
#5470=FACE_OUTER_BOUND ( 'NONE', #35342, .T. ) ;
#5478=CARTESIAN_POINT ( 'NONE',  ( -56.59682361629209879, 30.63869417066593925, -3.015094993620159425 ) ) ;
#5483=CARTESIAN_POINT ( 'NONE',  ( 67.91151009994659660, 58.69545974841741298, 3.974537232972598755 ) ) ;
#5485=AXIS2_PLACEMENT_3D ( 'NONE', #5239, #29941, #8102 ) ;
#5492=VERTEX_POINT ( 'NONE', #35012 ) ;
#5494=EDGE_CURVE ( 'NONE', #32500, #35091, #14, .T. ) ;
#5496=CARTESIAN_POINT ( 'NONE',  ( 79.61178798950636804, 64.58589821993882651, -3.525318766974264051 ) ) ;
#5498=CARTESIAN_POINT ( 'NONE',  ( 80.80704226153167724, 62.39036624599375358, 3.220356845321973083 ) ) ;
#5500=CARTESIAN_POINT ( 'NONE',  ( -58.99948754145753327, 28.61410076184086293, 6.947368380125157117 ) ) ;
#5501=ORIENTED_EDGE ( 'NONE', *, *, #33705, .F. ) ;
#5503=CARTESIAN_POINT ( 'NONE',  ( 74.17630236427460488, 61.40657735673663353, -3.883841728571264529 ) ) ;
#5505=CARTESIAN_POINT ( 'NONE',  ( -63.99293516169446150, 35.89893413629672381, -46.17089178453873188 ) ) ;
#5507=CARTESIAN_POINT ( 'NONE',  ( -63.99293516169446150, 35.89893413629672381, -7.506047544094577084 ) ) ;
#5511=ORIENTED_EDGE ( 'NONE', *, *, #20944, .F. ) ;
#5517=CARTESIAN_POINT ( 'NONE',  ( 78.81184074671354267, 66.10527324714757924, 1.416821487223875131 ) ) ;
#5519=( BOUNDED_CURVE ( )  B_SPLINE_CURVE ( 3, ( #8046, #10342, #22915, #29682 ),
 .UNSPECIFIED., .F., .T. ) 
 B_SPLINE_CURVE_WITH_KNOTS ( ( 4, 4 ),
 ( 1.422658486313809423, 1.570796326794892561 ),
 .UNSPECIFIED. ) 
 CURVE ( )  GEOMETRIC_REPRESENTATION_ITEM ( )  RATIONAL_B_SPLINE_CURVE ( ( 1.000000000000000000, 0.9981721009331622207, 0.9981721009331622207, 1.000000000000000000 ) ) 
 REPRESENTATION_ITEM ( '' )  );
#5535=VECTOR ( 'NONE', #9973, 1000.000000000000000 ) ;
#5539=CARTESIAN_POINT ( 'NONE',  ( 80.28274408427735409, 64.63090917800610669, -3.500437194783550421 ) ) ;
#5550=CARTESIAN_POINT ( 'NONE',  ( 80.42360172120015704, 63.56407742133696104, -3.661914029440274998 ) ) ;
#5556=CARTESIAN_POINT ( 'NONE',  ( 82.03714350014146817, 63.99860240201132910, -2.622983904469594396 ) ) ;
#5558=CARTESIAN_POINT ( 'NONE',  ( -69.08758708074093136, 36.88538962427716683, -9.800414904976365804 ) ) ;
#5561=CARTESIAN_POINT ( 'NONE',  ( 73.97359482965943300, 60.32890003735500528, 3.899931323540654748 ) ) ;
#5565=AXIS2_PLACEMENT_3D ( 'NONE', #5115, #7792, #11267 ) ;
#5568=ORIENTED_EDGE ( 'NONE', *, *, #16410, .F. ) ;
#5570=CARTESIAN_POINT ( 'NONE',  ( 79.93288853953367834, 66.07525097314720597, 2.222430037835993133 ) ) ;
#5572=DIRECTION ( 'NONE',  ( 0.000000000000000000, 0.000000000000000000, 1.000000000000000000 ) ) ;
#5590=DIRECTION ( 'NONE',  ( 0.000000000000000000, 0.000000000000000000, 1.000000000000000000 ) ) ;
#5591=CARTESIAN_POINT ( 'NONE',  ( 66.95378024648879034, 58.14766406364808660, -3.994852852620100592 ) ) ;
#5602=AXIS2_PLACEMENT_3D ( 'NONE', #29730, #5230, #14074 ) ;
#5608=CARTESIAN_POINT ( 'NONE',  ( 82.56222392620334460, 63.90769089702597228, -1.000000000000000000 ) ) ;
#5609=CARTESIAN_POINT ( 'NONE',  ( 79.16740428156646203, 65.60392721301286656, 2.747716423863120649 ) ) ;
#5612=CARTESIAN_POINT ( 'NONE',  ( 77.40632518803428752, 64.64540924511489095, -2.913524936156950851 ) ) ;
#5615=CARTESIAN_POINT ( 'NONE',  ( 81.42004705249084395, 62.63944267392457022, -2.989933650881958727 ) ) ;
#5616=CARTESIAN_POINT ( 'NONE',  ( 78.58187568275398860, 60.86241699943124672, 3.054665556626515510 ) ) ;
#5619=CARTESIAN_POINT ( 'NONE',  ( 80.96936403957158745, 66.06451342975873331, 1.623788564013679547 ) ) ;
#5629=AXIS2_PLACEMENT_3D ( 'NONE', #37575, #30818, #19062 ) ;
#5630=CARTESIAN_POINT ( 'NONE',  ( -63.99293516169446150, 35.89893413629672381, -12.49999999999999645 ) ) ;
#5632=CARTESIAN_POINT ( 'NONE',  ( 81.01439173330787469, 61.24733602610728411, 1.383572655854213185 ) ) ;
#5650=CARTESIAN_POINT ( 'NONE',  ( 70.96793116520528599, 59.41887718710786714, -3.976054184260645386 ) ) ;
#5654=CARTESIAN_POINT ( 'NONE',  ( 69.94804423520642445, 58.60696991578217308, 3.944663542062682993 ) ) ;
#5665=CARTESIAN_POINT ( 'NONE',  ( 78.41749725426429052, 65.86496093260605278, -1.552792442904348036 ) ) ;
#5667=CARTESIAN_POINT ( 'NONE',  ( 81.51618470504202207, 61.58087653888391344, -1.588372325568315535 ) ) ;
#5668=CARTESIAN_POINT ( 'NONE',  ( 80.84620594802116500, 61.52815374075451871, 2.368006059520743722 ) ) ;
#5691=CARTESIAN_POINT ( 'NONE',  ( 66.96362040430034313, 58.12048686563063882, 3.996315564296190725 ) ) ;
#5706=CARTESIAN_POINT ( 'NONE',  ( 81.02333598550073646, 61.30014629029354722, -1.703597047176645507 ) ) ;
#5708=CARTESIAN_POINT ( 'NONE',  ( 78.60310727342863402, 65.99661392892443246, 1.312782405654750129 ) ) ;
#5711=CARTESIAN_POINT ( 'NONE',  ( 74.40173173411091057, 59.34324565254589601, -3.478821770173325501 ) ) ;
#5715=CARTESIAN_POINT ( 'NONE',  ( -64.08758708074091714, 38.43534281692514298, -4.049547700704213327 ) ) ;
#5723=VECTOR ( 'NONE', #34985, 1000.000000000000000 ) ;
#5727=CARTESIAN_POINT ( 'NONE',  ( 81.35401977072818624, 62.93507997573772883, 3.162824939346248865 ) ) ;
#5736=CARTESIAN_POINT ( 'NONE',  ( -67.91293329751151475, 37.48821246048833444, -8.742028012083927990 ) ) ;
#5743=CARTESIAN_POINT ( 'NONE',  ( 81.14684024915200666, 61.29565758240214279, -1.145133111591833286 ) ) ;
#5746=CIRCLE ( 'NONE', #22833, 3.000000000000003109 ) ;
#5756=CARTESIAN_POINT ( 'NONE',  ( 79.07783777134646641, 65.79916784333097723, -2.450942308261427005 ) ) ;
#5761=CARTESIAN_POINT ( 'NONE',  ( 81.16843721835843439, 61.30356250071481128, -1.032522165606414744 ) ) ;
#5763=DIRECTION ( 'NONE',  ( -1.000000000000000000, 0.000000000000000000, 0.000000000000000000 ) ) ;
#5769=CARTESIAN_POINT ( 'NONE',  ( 72.90994289418092933, 61.20204674871914818, 3.824679913472085246 ) ) ;
#5778=CARTESIAN_POINT ( 'NONE',  ( 81.16688244586958945, 61.30299313749269174, 1.050153991572631895 ) ) ;
#5785=EDGE_CURVE ( 'NONE', #1114, #33628, #10618, .T. ) ;
#5797=CARTESIAN_POINT ( 'NONE',  ( 66.89671537544454338, 57.84689108302589489, -3.997688572865332635 ) ) ;
#5808=ORIENTED_EDGE ( 'NONE', *, *, #25291, .F. ) ;
#5810=CARTESIAN_POINT ( 'NONE',  ( 81.47505553675507883, 61.46950381087523141, -1.024355359505926266 ) ) ;
#5812=CARTESIAN_POINT ( 'NONE',  ( 81.11661571137585725, 61.75122346557051145, 2.482170738714641445 ) ) ;
#5815=CARTESIAN_POINT ( 'NONE',  ( 76.92031397606369580, 59.90536750123401077, -2.950589020716169131 ) ) ;
#5821=CARTESIAN_POINT ( 'NONE',  ( 81.44732304147247248, 62.37541782543058844, -2.773332820897494777 ) ) ;
#5822=CARTESIAN_POINT ( 'NONE',  ( 76.69853897424475520, 64.65515986876397392, 2.498359881428380724 ) ) ;
#5826=CARTESIAN_POINT ( 'NONE',  ( 79.60403240858897789, 66.28972460246990295, 1.461108304021875970 ) ) ;
#5857=CARTESIAN_POINT ( 'NONE',  ( 69.05402862303502332, 59.18504256499077343, -3.962610901733955693 ) ) ;
#5871=CARTESIAN_POINT ( 'NONE',  ( 78.53532592461078821, 65.52573200842934398, -2.475680338657053170 ) ) ;
#5873=CARTESIAN_POINT ( 'NONE',  ( 81.92776049059203558, 62.60942412355767317, -2.397965335136836185 ) ) ;
#5874=CARTESIAN_POINT ( 'NONE',  ( 78.40460260197330911, 65.77602943765538157, 1.910479420724411126 ) ) ;
#5896=ORIENTED_EDGE ( 'NONE', *, *, #19889, .T. ) ;
#5897=CARTESIAN_POINT ( 'NONE',  ( 67.54222599743037847, 57.89884484782556484, 3.985038673850038737 ) ) ;
#5902=DIRECTION ( 'NONE',  ( -0.8831583674551010121, 0.4690749385695646700, 0.000000000000000000 ) ) ;
#5914=CARTESIAN_POINT ( 'NONE',  ( 79.14833415808527661, 65.26800409942002545, -3.041370705153016107 ) ) ;
#5916=CARTESIAN_POINT ( 'NONE',  ( 79.12326768591945836, 65.24646460380061797, 3.052025427726082540 ) ) ;
#5918=ORIENTED_EDGE ( 'NONE', *, *, #34021, .F. ) ;
#5919=EDGE_CURVE ( 'NONE', #3549, #7709, #35556, .T. ) ;
#5920=CARTESIAN_POINT ( 'NONE',  ( 74.16083781478751291, 62.90537518464178390, -3.184487947857685519 ) ) ;
#5921=CARTESIAN_POINT ( 'NONE',  ( -58.80675025188774185, 28.82475471880029616, 5.862912209848245126 ) ) ;
#5929=AXIS2_PLACEMENT_3D ( 'NONE', #35134, #32247, #7305 ) ;
#5931=CARTESIAN_POINT ( 'NONE',  ( -57.16504416091206053, 33.41445838748276742, 1.000000000000000000 ) ) ;
#5932=CARTESIAN_POINT ( 'NONE',  ( 81.29167079631679371, 61.38276384236276328, 1.400336002811339631 ) ) ;
#5936=CARTESIAN_POINT ( 'NONE',  ( -64.13023603728508704, 35.23430396804722875, -4.479415521045631010 ) ) ;
#5947=CARTESIAN_POINT ( 'NONE',  ( 78.92617879813647619, 66.06909554768878934, -1.766895996212476838 ) ) ;
#5956=CARTESIAN_POINT ( 'NONE',  ( 78.95300076920055687, 65.89750638847961284, -2.156541836018598612 ) ) ;
#5957=CARTESIAN_POINT ( 'NONE',  ( -58.86630245980595788, 29.17574657131979521, -6.015288659391247350 ) ) ;
#5962=CARTESIAN_POINT ( 'NONE',  ( 81.84810375386628323, 62.06244373962199745, -1.965143080302317768 ) ) ;
#5972=CARTESIAN_POINT ( 'NONE',  ( 73.68135292868622344, 60.99150118422435440, 3.923277237825058439 ) ) ;
#5973=ORIENTED_EDGE ( 'NONE', *, *, #25995, .T. ) ;
#5979=CARTESIAN_POINT ( 'NONE',  ( -58.96492457584757574, 28.81155473361731723, -6.495248013871978365 ) ) ;
#5983=CARTESIAN_POINT ( 'NONE',  ( 79.54388053879588938, 66.09379204087662174, 2.134710458528629395 ) ) ;
#5995=ORIENTED_EDGE ( 'NONE', *, *, #37321, .T. ) ;
#5998=VECTOR ( 'NONE', #5424, 1000.000000000000000 ) ;
#6000=ORIENTED_EDGE ( 'NONE', *, *, #25541, .F. ) ;
#6004=CARTESIAN_POINT ( 'NONE',  ( 66.86134338034700875, 57.94508673653880493, -3.999594749380241510 ) ) ;
#6012=CARTESIAN_POINT ( 'NONE',  ( 25.11437021580303863, 164.7550792202006562, -4.000000000000000000 ) ) ;
#6013=ORIENTED_EDGE ( 'NONE', *, *, #4879, .F. ) ;
#6015=CARTESIAN_POINT ( 'NONE',  ( 82.31572251369546223, 62.52525979466043538, -1.394285451510165474 ) ) ;
#6016=CARTESIAN_POINT ( 'NONE',  ( 78.89771339490204127, 65.85133954292349756, 2.202709653501103482 ) ) ;
#6020=CARTESIAN_POINT ( 'NONE',  ( 78.03839322897103159, 60.52053993360666340, -3.012346708730617717 ) ) ;
#6025=CARTESIAN_POINT ( 'NONE',  ( 80.32731820218204177, 65.01876230294878667, -3.279590910092191169 ) ) ;
#6026=CARTESIAN_POINT ( 'NONE',  ( 77.45380151126714452, 63.20247531706578314, 3.748203062644110073 ) ) ;
#6030=CARTESIAN_POINT ( 'NONE',  ( -57.80939613976639180, 32.30609257358648279, 4.182684676774399257 ) ) ;
#6031=CARTESIAN_POINT ( 'NONE',  ( 82.07520363809508979, 62.17599436785813793, 1.599335268229120199 ) ) ;
#6032=CARTESIAN_POINT ( 'NONE',  ( -64.08758708074094557, 43.28886537626787145, 1.984762276592526353 ) ) ;
#6037=CARTESIAN_POINT ( 'NONE',  ( -64.20341131561859527, 34.94420666461579117, 4.877756629158603197 ) ) ;
#6045=CARTESIAN_POINT ( 'NONE',  ( 80.30472701757432219, 60.99336015429530278, -1.909150740780570121 ) ) ;
#6051=EDGE_CURVE ( 'NONE', #37345, #3549, #3158, .T. ) ;
#6052=CARTESIAN_POINT ( 'NONE',  ( -64.08758708074093136, 37.42960919638308326, -3.182465448034689892 ) ) ;
#6057=CARTESIAN_POINT ( 'NONE',  ( 70.04419837359742473, 58.36171959603688464, -3.883859131414874710 ) ) ;
#6072=CARTESIAN_POINT ( 'NONE',  ( 78.73387159939801450, 65.21990392541003700, -2.961936469198042321 ) ) ;
#6074=CARTESIAN_POINT ( 'NONE',  ( 80.87888400807966605, 65.31646575666023580, -2.869341960395656699 ) ) ;
#6075=CARTESIAN_POINT ( 'NONE',  ( 78.69113869042872977, 65.45098002628645872, 2.699019001080982250 ) ) ;
#6095=CIRCLE ( 'NONE', #34385, 95.38357402481355507 ) ;
#6101=CARTESIAN_POINT ( 'NONE',  ( 66.95378024648879034, 58.14766406364808660, 3.994852852620100592 ) ) ;
#6118=ORIENTED_EDGE ( 'NONE', *, *, #11465, .F. ) ;
#6119=CARTESIAN_POINT ( 'NONE',  ( 79.67348887277924518, 64.26584687736622925, -3.653685850874240248 ) ) ;
#6121=CARTESIAN_POINT ( 'NONE',  ( 78.54140637431730454, 65.95282500403628489, 1.409197735201547674 ) ) ;
#6125=CARTESIAN_POINT ( 'NONE',  ( -58.83478692283225087, 28.75339845897402924, 5.944647730637774075 ) ) ;
#6128=CARTESIAN_POINT ( 'NONE',  ( -64.08758708074093136, 38.55592700272130458, -3.000000000000462297 ) ) ;
#6136=CARTESIAN_POINT ( 'NONE',  ( 78.95529765307296088, 66.08830754916627370, 1.741375869723574166 ) ) ;
#6140=CARTESIAN_POINT ( 'NONE',  ( -64.85784325972055342, 34.81586596186931359, -6.466735817496061856 ) ) ;
#6146=CARTESIAN_POINT ( 'NONE',  ( -64.55204904898397444, 36.12561474966231856, -8.218049716820861050 ) ) ;
#6156=CARTESIAN_POINT ( 'NONE',  ( 80.94524665917968775, 63.44345826879091277, -3.487490852634244742 ) ) ;
#6160=ORIENTED_EDGE ( 'NONE', *, *, #34843, .F. ) ;
#6166=CARTESIAN_POINT ( 'NONE',  ( 79.14683388637743633, 65.58698894143067548, -2.758686562281584376 ) ) ;
#6172=CARTESIAN_POINT ( 'NONE',  ( 82.01382571621886086, 63.62535219989227642, -2.645340681430279339 ) ) ;
#6178=CARTESIAN_POINT ( 'NONE',  ( -64.08758708074093136, 41.04287353446839148, -4.000000000000000000 ) ) ;
#6179=CARTESIAN_POINT ( 'NONE',  ( 72.80781396401921768, 61.43345056764702861, 3.736020861133335647 ) ) ;
#6187=CARTESIAN_POINT ( 'NONE',  ( 80.14906791408223796, 65.90796394341653297, 2.445541897054074987 ) ) ;
#6190=DIRECTION ( 'NONE',  ( -1.188227527617580984E-16, -0.9905719730871677120, 0.1369933068956136479 ) ) ;
#6194=VECTOR ( 'NONE', #19336, 1000.000000000000000 ) ;
#6208=CARTESIAN_POINT ( 'NONE',  ( 66.43286826475046780, 57.76021747899716985, -4.000000000000007105 ) ) ;
#6211=CARTESIAN_POINT ( 'NONE',  ( -56.31571917568491870, 30.58480147475563626, 3.912689169536869738 ) ) ;
#6213=CARTESIAN_POINT ( 'NONE',  ( 66.41543808532628645, 57.82433660857527258, 4.000000000000015987 ) ) ;
#6217=VERTEX_POINT ( 'NONE', #4068 ) ;
#6219=CARTESIAN_POINT ( 'NONE',  ( 82.15576060805985037, 62.21674973124318342, -1.325417871280742066 ) ) ;
#6220=CARTESIAN_POINT ( 'NONE',  ( 78.78378587176689507, 65.95784816145936702, 1.911132874451720864 ) ) ;
#6224=CARTESIAN_POINT ( 'NONE',  ( 76.19461364182978969, 62.94386820200831067, -3.683100983535286588 ) ) ;
#6228=CARTESIAN_POINT ( 'NONE',  ( 81.37039951255469816, 61.83949519909545245, -2.349509806045110949 ) ) ;
#6229=CARTESIAN_POINT ( 'NONE',  ( 79.35831483666107999, 61.48221340643413413, 3.218236826935628070 ) ) ;
#6234=CARTESIAN_POINT ( 'NONE',  ( 82.31242756469306698, 63.41700585080328523, 2.192618372226454504 ) ) ;
#6239=CARTESIAN_POINT ( 'NONE',  ( -62.73984912080872789, 35.89138081568317062, -5.261690063483860591 ) ) ;
#6260=CARTESIAN_POINT ( 'NONE',  ( 68.56660431458814742, 58.72100381882076192, -3.990501929453217134 ) ) ;
#6261=CIRCLE ( 'NONE', #7536, 79.54614097552274643 ) ;
#6262=ORIENTED_EDGE ( 'NONE', *, *, #25995, .F. ) ;
#6272=CARTESIAN_POINT ( 'NONE',  ( 78.97528327045988306, 64.81351720955758822, -3.340572457511928661 ) ) ;
#6275=CARTESIAN_POINT ( 'NONE',  ( 80.50371486736973736, 65.47929316355251217, -2.914706979937543796 ) ) ;
#6277=CARTESIAN_POINT ( 'NONE',  ( 80.23208661909926320, 62.50324886901235999, 3.482780605906225624 ) ) ;
#6280=CARTESIAN_POINT ( 'NONE',  ( 79.34209122208885390, 66.30884595491197331, 1.000000000000000000 ) ) ;
#6282=ORIENTED_EDGE ( 'NONE', *, *, #10053, .T. ) ;
#6306=CARTESIAN_POINT ( 'NONE',  ( 67.03255446809592399, 57.93006272621622088, 3.998453671246410934 ) ) ;
#6308=AXIS2_PLACEMENT_3D ( 'NONE', #30399, #20499, #27295 ) ;
#6309=DIRECTION ( 'NONE',  ( 1.000000000000000000, 0.000000000000000000, 0.000000000000000000 ) ) ;
#6318=EDGE_CURVE ( 'NONE', #446, #29043, #19618, .T. ) ;
#6324=CARTESIAN_POINT ( 'NONE',  ( 80.98019550867142868, 61.28820853408534219, -1.743126864185862601 ) ) ;
#6326=CARTESIAN_POINT ( 'NONE',  ( 79.85475324883658743, 64.00275885990842539, 3.706996517075250797 ) ) ;
#6346=CARTESIAN_POINT ( 'NONE',  ( 78.67891909395969208, 66.05044883183084892, 1.113695828830612022 ) ) ;
#6351=CARTESIAN_POINT ( 'NONE',  ( -69.08758708074093136, 36.88538962427716683, 9.800414904976364028 ) ) ;
#6353=CIRCLE ( 'NONE', #37890, 3.000000000000003997 ) ;
#6363=CARTESIAN_POINT ( 'NONE',  ( 80.03809576917892343, 64.85583152007153274, -3.406228740995818516 ) ) ;
#6373=CARTESIAN_POINT ( 'NONE',  ( 78.78378587176688086, 65.95784816145936702, -1.911132874451719754 ) ) ;
#6388=CARTESIAN_POINT ( 'NONE',  ( -63.23384002544804616, 41.81976959235312563, -3.940701001627876288 ) ) ;
#6389=CARTESIAN_POINT ( 'NONE',  ( 73.33417617461327609, 60.23131181272744072, 3.934110468510651604 ) ) ;
#6395=CARTESIAN_POINT ( 'NONE',  ( 81.36533387373953019, 61.41589781867489251, 1.313329331391811960 ) ) ;
#6397=EDGE_LOOP ( 'NONE', ( #6262, #32989, #37823, #39991, #31309, #30804 ) ) ;
#6405=ORIENTED_EDGE ( 'NONE', *, *, #40286, .T. ) ;
#6413=CARTESIAN_POINT ( 'NONE',  ( 66.41802798480571823, 57.80214248194123172, -4.000000000000020428 ) ) ;
#6422=ORIENTED_EDGE ( 'NONE', *, *, #37378, .F. ) ;
#6424=CARTESIAN_POINT ( 'NONE',  ( 80.67264098608434608, 66.18930038384912962, -1.451695327222927157 ) ) ;
#6425=CARTESIAN_POINT ( 'NONE',  ( 78.91303925368887917, 65.86465164089241853, 2.189516896894255549 ) ) ;
#6426=AXIS2_PLACEMENT_3D ( 'NONE', #5931, #15182, #2866 ) ;
#6429=CARTESIAN_POINT ( 'NONE',  ( 76.81831744871801959, 63.08285468194212342, -3.722835383484654592 ) ) ;
#6434=CARTESIAN_POINT ( 'NONE',  ( 78.79418933159148253, 66.09338072887959470, -1.439474762807432695 ) ) ;
#6436=CARTESIAN_POINT ( 'NONE',  ( 79.66869450427635968, 60.77384974161341091, 2.178915381671341578 ) ) ;
#6445=CARTESIAN_POINT ( 'NONE',  ( 80.79165360588685019, 65.97001311340693519, 2.094266784918907831 ) ) ;
#6449=CARTESIAN_POINT ( 'NONE',  ( -1.432293644835494373, -27.47664038617742577, 1.000000000000000000 ) ) ;
#6454=DIRECTION ( 'NONE',  ( 1.000000000000000000, 0.000000000000000000, 0.000000000000000000 ) ) ;
#6471=CARTESIAN_POINT ( 'NONE',  ( 68.79143787039059532, 58.12720587843082853, -3.950303728398663949 ) ) ;
#6484=CARTESIAN_POINT ( 'NONE',  ( 78.40723131619293440, 65.41550730244513545, -2.551437666014013672 ) ) ;
#6488=CARTESIAN_POINT ( 'NONE',  ( 81.52287143523912505, 61.74508502528950515, -1.930361577749144519 ) ) ;
#6489=CARTESIAN_POINT ( 'NONE',  ( 80.75587274821523920, 61.22306450394816579, 1.910479420724444433 ) ) ;
#6510=CARTESIAN_POINT ( 'NONE',  ( -65.15514661499977933, 34.97220226750606997, -6.888442104241536690 ) ) ;
#6518=CARTESIAN_POINT ( 'NONE',  ( 67.46313568882432321, 58.11475875142180314, 3.998123450764770048 ) ) ;
#6533=CARTESIAN_POINT ( 'NONE',  ( 79.07938959848800664, 65.20837507400351285, -3.070011659370644796 ) ) ;
#6535=CARTESIAN_POINT ( 'NONE',  ( 80.65652637675404435, 62.34602738889181950, 3.260928702718590699 ) ) ;
#6539=CARTESIAN_POINT ( 'NONE',  ( -58.98413297244930931, 28.20303297481065385, 6.383932851085149629 ) ) ;
#6553=CARTESIAN_POINT ( 'NONE',  ( 81.15350626233055209, 61.29809656771022475, 1.122020883098631350 ) ) ;
#6557=CARTESIAN_POINT ( 'NONE',  ( -9.741734729663692249, 54.65020406074287251, -4.000000000000000000 ) ) ;
#6569=CARTESIAN_POINT ( 'NONE',  ( 79.47520324823359772, 65.51774519012143116, -2.899379378185757528 ) ) ;
#6580=CARTESIAN_POINT ( 'NONE',  ( 79.95371652093496095, 64.44169929929478258, -3.600689860192760605 ) ) ;
#6585=ORIENTED_EDGE ( 'NONE', *, *, #24126, .F. ) ;
#6586=CARTESIAN_POINT ( 'NONE',  ( 81.88652354500518982, 62.08144837224592294, -1.918505602738485027 ) ) ;
#6588=CARTESIAN_POINT ( 'NONE',  ( -77.95330471031414277, 33.71485196875532608, -46.17089178453873188 ) ) ;
#6594=CARTESIAN_POINT ( 'NONE',  ( 71.29558780583862188, 58.60460498947428931, 3.808711916423244581 ) ) ;
#6599=AXIS2_PLACEMENT_3D ( 'NONE', #23451, #2416, #20347 ) ;
#6600=CARTESIAN_POINT ( 'NONE',  ( -58.67278899370590040, 29.89537120981031393, -5.422835840279424779 ) ) ;
#6602=CARTESIAN_POINT ( 'NONE',  ( 81.73261497063184322, 63.12224843555917886, 2.914706979937429665 ) ) ;
#6618=ORIENTED_EDGE ( 'NONE', *, *, #7134, .F. ) ;
#6619=CARTESIAN_POINT ( 'NONE',  ( 66.42594280077625513, 57.77978248037106823, -4.000000000000013323 ) ) ;
#6622=CARTESIAN_POINT ( 'NONE',  ( -55.97227462678463183, 30.94442605972621507, 3.900682954687266779 ) ) ;
#6633=CARTESIAN_POINT ( 'NONE',  ( 80.02802368947523348, 66.35789156557524393, -1.168532795814369418 ) ) ;
#6634=CARTESIAN_POINT ( 'NONE',  ( 79.25227124789796562, 65.35518565838746952, 2.996423812020188038 ) ) ;
#6637=CARTESIAN_POINT ( 'NONE',  ( 77.48272095992952302, 61.71466691532025806, -3.776276000690703682 ) ) ;
#6641=CARTESIAN_POINT ( 'NONE',  ( 81.19366756170077792, 63.21158026472416225, -3.307636073424136569 ) ) ;
#6642=CARTESIAN_POINT ( 'NONE',  ( 76.15169681074907260, 61.58848496619823010, 3.887901781369003551 ) ) ;
#6645=CARTESIAN_POINT ( 'NONE',  ( -58.96512565301119224, 28.81081997859032739, 6.496329578498431623 ) ) ;
#6646=CARTESIAN_POINT ( 'NONE',  ( 82.43319509988612026, 63.84109541104528063, 1.838010297257003156 ) ) ;
#6651=FACE_OUTER_BOUND ( 'NONE', #31287, .T. ) ;
#6655=CARTESIAN_POINT ( 'NONE',  ( 76.65176712096844369, 59.82760137992013227, 3.005358148697153453 ) ) ;
#6658=CARTESIAN_POINT ( 'NONE',  ( 78.69038500580363404, 66.05859403932464602, 1.000000000000000000 ) ) ;
#6663=EDGE_CURVE ( 'NONE', #32500, #15332, #14351, .T. ) ;
#6670=CARTESIAN_POINT ( 'NONE',  ( 67.84886183593677345, 57.97047572268562021, -3.979762160777300828 ) ) ;
#6672=ADVANCED_FACE ( 'NONE', ( #7285 ), #4460, .T. ) ;
#6676=DIRECTION ( 'NONE',  ( 0.8888117386314182689, 0.4582725098355732163, 0.000000000000000000 ) ) ;
#6682=CARTESIAN_POINT ( 'NONE',  ( 78.74533340381492508, 66.05753824468469304, 1.508787936435526111 ) ) ;
#6687=CARTESIAN_POINT ( 'NONE',  ( 79.49720564641141607, 63.45635150964716331, -3.756013696796376866 ) ) ;
#6691=CARTESIAN_POINT ( 'NONE',  ( 79.31479573854757348, 66.13045663638729366, -1.878604182848723214 ) ) ;
#6692=CARTESIAN_POINT ( 'NONE',  ( 79.56639652130381535, 63.83553059081831549, 3.738478073092012632 ) ) ;
#6694=CARTESIAN_POINT ( 'NONE',  ( 78.69038500580381879, 66.05859403932473128, 1.002944004955704349 ) ) ;
#6695=CARTESIAN_POINT ( 'NONE',  ( -64.08758708074093136, 42.49042454705804772, 3.493279343125383019 ) ) ;
#6709=CARTESIAN_POINT ( 'NONE',  ( 78.69038500580363404, 66.05859403932464602, 4.000000000000000000 ) ) ;
#6718=CARTESIAN_POINT ( 'NONE',  ( 66.72638704319571445, 57.85960203741856134, 3.999543855871245945 ) ) ;
#6724=ORIENTED_EDGE ( 'NONE', *, *, #14679, .F. ) ;
#6731=CARTESIAN_POINT ( 'NONE',  ( 80.65652637675404435, 62.34602738889181950, -3.260928702718591587 ) ) ;
#6733=CARTESIAN_POINT ( 'NONE',  ( 79.43051736299561583, 64.82585401503284572, 3.419027627190938556 ) ) ;
#6742=CARTESIAN_POINT ( 'NONE',  ( -64.75098741874504071, 36.24760096809371390, -6.319851154868031173 ) ) ;
#6751=CARTESIAN_POINT ( 'NONE',  ( 81.15131294690949915, 61.29729393613784083, 1.130345937366645126 ) ) ;
#6759=CARTESIAN_POINT ( 'NONE',  ( -59.93345510331042902, 24.73247967741478703, -9.800414904976365804 ) ) ;
#6766=CARTESIAN_POINT ( 'NONE',  ( 80.54433603269384889, 64.00140174820366212, -3.588566286536284178 ) ) ;
#6770=AXIS2_PLACEMENT_3D ( 'NONE', #15362, #15975, #21760 ) ;
#6775=CARTESIAN_POINT ( 'NONE',  ( -74.92283640148291113, 18.87330372387140187, -9.800414904976365804 ) ) ;
#6776=ORIENTED_EDGE ( 'NONE', *, *, #404, .F. ) ;
#6777=CARTESIAN_POINT ( 'NONE',  ( 79.31717123896757471, 65.40625759565881481, -2.968223699503262480 ) ) ;
#6782=CARTESIAN_POINT ( 'NONE',  ( 81.92450911876609609, 64.33049094056623574, -2.665107514501070085 ) ) ;
#6784=CARTESIAN_POINT ( 'NONE',  ( -57.66409387480749871, 30.21301454600294178, -4.063144412293765662 ) ) ;
#6788=CARTESIAN_POINT ( 'NONE',  ( 71.16717283274410022, 58.92450812456241493, 3.908768822720079417 ) ) ;
#6796=CARTESIAN_POINT ( 'NONE',  ( -54.93030506612853969, 31.40261711588176397, -1.217302950687081831 ) ) ;
#6797=CARTESIAN_POINT ( 'NONE',  ( 81.57279438772143010, 63.75980975930807659, 3.125232205748817105 ) ) ;
#6802=VERTEX_POINT ( 'NONE', #20850 ) ;
#6812=VECTOR ( 'NONE', #3640, 1000.000000000000000 ) ;
#6816=EDGE_CURVE ( 'NONE', #17865, #6217, #20641, .T. ) ;
#6820=CARTESIAN_POINT ( 'NONE',  ( 66.57962043698374544, 57.80678959376348303, -3.999745625240549440 ) ) ;
#6824=LINE ( 'NONE', #28223, #12976 ) ;
#6828=CARTESIAN_POINT ( 'NONE',  ( 79.33205627562968232, 66.30342423254379014, -1.132734665583632117 ) ) ;
#6829=EDGE_CURVE ( 'NONE', #31687, #38060, #27230, .T. ) ;
#6832=CARTESIAN_POINT ( 'NONE',  ( 74.58877118170933329, 61.99488014651142009, -3.786335567263263702 ) ) ;
#6836=CARTESIAN_POINT ( 'NONE',  ( 80.26863108949493153, 64.98620546077044935, -3.307636073424134349 ) ) ;
#6837=CARTESIAN_POINT ( 'NONE',  ( 75.74268929893182190, 62.45338499886813111, 3.784676997166864343 ) ) ;
#6842=CARTESIAN_POINT ( 'NONE',  ( 82.23158145857243539, 63.37565065107725104, 2.326649614737513527 ) ) ;
#6853=VERTEX_POINT ( 'NONE', #1732 ) ;
#6869=CARTESIAN_POINT ( 'NONE',  ( 68.74365607523500898, 58.25355655637604713, -3.970924506823472644 ) ) ;
#6881=CARTESIAN_POINT ( 'NONE',  ( 80.65352406091056991, 63.67746643299658160, 3.602832836245132953 ) ) ;
#6884=CARTESIAN_POINT ( 'NONE',  ( 79.19917379928831735, 63.30335940139927686, -3.774260586041106258 ) ) ;
#6887=CARTESIAN_POINT ( 'NONE',  ( 81.69418451912821411, 62.49370361018091558, -2.611089443229507534 ) ) ;
#6888=CARTESIAN_POINT ( 'NONE',  ( 79.49720564641141607, 63.45635150964716331, 3.756013696796376422 ) ) ;
#6891=CARTESIAN_POINT ( 'NONE',  ( 82.55792188592127445, 63.20960171500894376, 1.133121492189030244 ) ) ;
#6892=CARTESIAN_POINT ( 'NONE',  ( -64.08758708074093136, 43.44410442252532079, 1.728127057092140317 ) ) ;
#6914=CARTESIAN_POINT ( 'NONE',  ( 66.88099813915303571, 57.89052526007606758, 3.999029912548879739 ) ) ;
#6921=ORIENTED_EDGE ( 'NONE', *, *, #39836, .F. ) ;
#6926=CARTESIAN_POINT ( 'NONE',  ( 78.96934220494343037, 65.43027598480369988, -2.854164747638217481 ) ) ;
#6929=CARTESIAN_POINT ( 'NONE',  ( 78.65528874306569662, 65.84149099381083658, 2.048264032867442630 ) ) ;
#6947=CARTESIAN_POINT ( 'NONE',  ( 80.80706632665069833, 63.75484916101672894, 3.549391953833845204 ) ) ;
#6949=LINE ( 'NONE', #9623, #35849 ) ;
#6959=CARTESIAN_POINT ( 'NONE',  ( 68.55047844998404116, 58.76352648041117277, 3.988324671431286106 ) ) ;
#6965=CARTESIAN_POINT ( 'NONE',  ( 79.30685661404397990, 65.70718262327383741, -2.676159939830900392 ) ) ;
#6975=CARTESIAN_POINT ( 'NONE',  ( 78.91303925368886496, 65.86465164089241853, -2.189516896894254216 ) ) ;
#6985=CARTESIAN_POINT ( 'NONE',  ( -64.08758708074093136, 44.09647858371768336, -0.9999999999999920064 ) ) ;
#6986=CARTESIAN_POINT ( 'NONE',  ( 71.87019205445125181, 60.48965333507749165, 3.909340765870004564 ) ) ;
#6993=EDGE_CURVE ( 'NONE', #23657, #18554, #20922, .T. ) ;
#6994=EDGE_LOOP ( 'NONE', ( #4236, #17218, #13991, #10063, #12793, #1965, #39682, #1469, #20048 ) ) ;
#6996=CARTESIAN_POINT ( 'NONE',  ( 78.68499968550166557, 66.05476829360674174, 1.077711394955748192 ) ) ;
#7008=CARTESIAN_POINT ( 'NONE',  ( 35.94200923520244828, 151.3264224549853907, 4.000000000000000000 ) ) ;
#7015=CARTESIAN_POINT ( 'NONE',  ( 66.42396409678360669, 57.78537248076360555, -4.000000000000015099 ) ) ;
#7023=CARTESIAN_POINT ( 'NONE',  ( 82.31416527841534503, 64.14174473599668147, -2.134985007310159943 ) ) ;
#7028=CARTESIAN_POINT ( 'NONE',  ( 75.35164290873603932, 61.82650661013094862, -3.882889210543306824 ) ) ;
#7032=CARTESIAN_POINT ( 'NONE',  ( 76.61572510735739172, 60.58450557137933146, 3.562065002338831832 ) ) ;
#7038=CARTESIAN_POINT ( 'NONE',  ( 82.09393942629682783, 63.66644892668136890, 2.541832380858824347 ) ) ;
#7059=CARTESIAN_POINT ( 'NONE',  ( 68.01940210501214779, 58.40717514567135282, -3.996230182412886744 ) ) ;
#7061=CIRCLE ( 'NONE', #11648, 5.681288188914806803 ) ;
#7075=CARTESIAN_POINT ( 'NONE',  ( 80.61377670644297666, 63.65766204751285784, 3.614389211669659208 ) ) ;
#7077=ORIENTED_EDGE ( 'NONE', *, *, #2738, .T. ) ;
#7078=CARTESIAN_POINT ( 'NONE',  ( 78.95339491453125902, 64.13176242216603384, -3.627744115730409558 ) ) ;
#7081=CARTESIAN_POINT ( 'NONE',  ( 80.63952753655819095, 65.18836132073317913, -3.079343812547462367 ) ) ;
#7082=CARTESIAN_POINT ( 'NONE',  ( 80.05518365985739138, 61.93129665380740079, 3.228498513792977143 ) ) ;
#7084=DIRECTION ( 'NONE',  ( -1.000000000000000000, 0.000000000000000000, 0.000000000000000000 ) ) ;
#7086=CARTESIAN_POINT ( 'NONE',  ( 81.35706873939174955, 65.93413826765582542, 1.145133701562419226 ) ) ;
#7088=CARTESIAN_POINT ( 'NONE',  ( -64.08758708074093136, 43.61223003624221661, 1.151950131395627519 ) ) ;
#7091=CARTESIAN_POINT ( 'NONE',  ( -64.47965924086389577, 36.51034344918424068, -5.743161323597451684 ) ) ;
#7096=ORIENTED_EDGE ( 'NONE', *, *, #22935, .T. ) ;
#7113=CARTESIAN_POINT ( 'NONE',  ( 66.84561829912908593, 57.98873651192412382, 3.999241724016629362 ) ) ;
#7122=ADVANCED_FACE ( 'NONE', ( #1839 ), #34780, .T. ) ;
#7127=CARTESIAN_POINT ( 'NONE',  ( 80.89410497084979568, 61.37834026963087553, -2.095806625474240903 ) ) ;
#7129=CARTESIAN_POINT ( 'NONE',  ( 79.30508931962911845, 64.72973333162836695, 3.449595662144110175 ) ) ;
#7132=VECTOR ( 'NONE', #4859, 1000.000000000000000 ) ;
#7134=EDGE_CURVE ( 'NONE', #15332, #15750, #25552, .T. ) ;
#7147=CARTESIAN_POINT ( 'NONE',  ( 78.92617879813646198, 66.06909554768881776, 1.766895996212466402 ) ) ;
#7149=DIRECTION ( 'NONE',  ( -0.4582725098355735494, 0.8888117386314181578, 0.000000000000000000 ) ) ;
#7154=CARTESIAN_POINT ( 'NONE',  ( -64.85784325972053921, 34.81586596186931359, 6.466735817496049421 ) ) ;
#7158=CARTESIAN_POINT ( 'NONE',  ( 69.01369661159887414, 59.28919897632942337, 3.943722715026729109 ) ) ;
#7161=CARTESIAN_POINT ( 'NONE',  ( -64.08758708074093136, 42.61892514642057961, -2.587732764668352115 ) ) ;
#7165=CARTESIAN_POINT ( 'NONE',  ( 79.14790672806260829, 65.85151465993942566, -2.407735119910378696 ) ) ;
#7169=ADVANCED_FACE ( 'NONE', ( #12248 ), #16380, .T. ) ;
#7176=CARTESIAN_POINT ( 'NONE',  ( 78.85680892556273136, 65.81502797165197194, -2.238287240292680558 ) ) ;
#7184=CARTESIAN_POINT ( 'NONE',  ( 72.38109545502503295, 59.26788356430734694, 3.856543183738433189 ) ) ;
#7186=VERTEX_POINT ( 'NONE', #37564 ) ;
#7194=CARTESIAN_POINT ( 'NONE',  ( 81.44856608406136900, 64.08396523683258295, 3.179853676208926672 ) ) ;
#7206=CARTESIAN_POINT ( 'NONE',  ( -75.45330471031414277, 33.71485196875532608, 8.800414904976364028 ) ) ;
#7213=DIRECTION ( 'NONE',  ( -0.000000000000000000, 0.000000000000000000, 1.000000000000000000 ) ) ;
#7219=EDGE_CURVE ( 'NONE', #34912, #7860, #3029, .T. ) ;
#7222=VERTEX_POINT ( 'NONE', #729 ) ;
#7223=CARTESIAN_POINT ( 'NONE',  ( -57.59497484894375674, 32.71166363405644262, -4.078840986107554301 ) ) ;
#7226=CARTESIAN_POINT ( 'NONE',  ( 79.96508732583350820, 66.32411498806374084, -1.465650077276903218 ) ) ;
#7230=CARTESIAN_POINT ( 'NONE',  ( 76.39232039721476042, 61.07121484735997541, -3.784676997173953783 ) ) ;
#7234=CARTESIAN_POINT ( 'NONE',  ( 75.95345872531818543, 63.43160129075360487, 3.385286751594689836 ) ) ;
#7240=CARTESIAN_POINT ( 'NONE',  ( 79.46293960946097457, 66.21290357410885008, 1.708467252431127070 ) ) ;
#7247=CARTESIAN_POINT ( 'NONE',  ( 67.92755604491691201, 57.95366386773438450, 3.974145956335496166 ) ) ;
#7252=CARTESIAN_POINT ( 'NONE',  ( -63.16615724057117376, 41.45860378058512907, -4.000000000000000000 ) ) ;
#7259=CARTESIAN_POINT ( 'NONE',  ( 67.46313568882432321, 58.11475875142180314, -3.998123450764770048 ) ) ;
#7274=CARTESIAN_POINT ( 'NONE',  ( 80.13254067770888867, 64.54635310605580401, 3.552238747020026732 ) ) ;
#7277=CARTESIAN_POINT ( 'NONE',  ( 78.00211021922338261, 65.46497694724934036, -2.177161688561012998 ) ) ;
#7280=CARTESIAN_POINT ( 'NONE',  ( 79.02544788879461635, 66.13175326451417391, -1.679744683809666350 ) ) ;
#7281=CARTESIAN_POINT ( 'NONE',  ( 78.71580656266537801, 64.90148335848421368, 3.195657361810692709 ) ) ;
#7284=CARTESIAN_POINT ( 'NONE',  ( 81.85052347209639834, 65.46610162458738102, 1.468380750527791268 ) ) ;
#7285=FACE_OUTER_BOUND ( 'NONE', #26338, .T. ) ;
#7305=DIRECTION ( 'NONE',  ( 0.000000000000000000, 0.000000000000000000, -1.000000000000000000 ) ) ;
#7311=CARTESIAN_POINT ( 'NONE',  ( 66.90064367344375285, 57.83598502562791310, 3.997265020308770289 ) ) ;
#7314=ORIENTED_EDGE ( 'NONE', *, *, #32458, .T. ) ;
#7322=CARTESIAN_POINT ( 'NONE',  ( 79.45016587565679345, 64.47252957033367693, -3.557377001560570573 ) ) ;
#7325=CARTESIAN_POINT ( 'NONE',  ( 79.07938959848826244, 65.20837507400389654, 3.070011659370390777 ) ) ;
#7335=ORIENTED_EDGE ( 'NONE', *, *, #40621, .F. ) ;
#7342=CARTESIAN_POINT ( 'NONE',  ( 80.22001885188443282, 64.95903095167625452, 3.330128783915578872 ) ) ;
#7350=CARTESIAN_POINT ( 'NONE',  ( -64.66796849410252435, 36.23110552202045653, 6.165526157072420688 ) ) ;
#7355=CARTESIAN_POINT ( 'NONE',  ( 69.21678231378241719, 58.76388891306111617, 3.990151341881419622 ) ) ;
#7360=CARTESIAN_POINT ( 'NONE',  ( 81.20616577872307573, 61.45478060783982244, -1.852607187800904942 ) ) ;
#7364=VERTEX_POINT ( 'NONE', #7700 ) ;
#7366=VERTEX_POINT ( 'NONE', #16355 ) ;
#7369=CARTESIAN_POINT ( 'NONE',  ( 80.72314371186274684, 62.66258842508732840, -3.386558198656251406 ) ) ;
#7371=CARTESIAN_POINT ( 'NONE',  ( 78.77108537463557525, 65.94663689831973841, 1.925402693829579626 ) ) ;
#7373=CIRCLE ( 'NONE', #38929, 98.38357402481355507 ) ;
#7379=CARTESIAN_POINT ( 'NONE',  ( -64.08758708074093136, 42.96264881669708302, -3.162281979264331966 ) ) ;
#7380=CARTESIAN_POINT ( 'NONE',  ( 72.04157359233609270, 60.08177168861285367, 3.962431611490357053 ) ) ;
#7386=ORIENTED_EDGE ( 'NONE', *, *, #39361, .T. ) ;
#7388=EDGE_CURVE ( 'NONE', #25777, #2799, #28217, .T. ) ;
#7392=CARTESIAN_POINT ( 'NONE',  ( 81.48777377602155525, 63.71638886500237220, 3.187395722566881862 ) ) ;
#7417=CARTESIAN_POINT ( 'NONE',  ( -58.33732831438487665, 31.01206039140789983, -4.738023936417821602 ) ) ;
#7419=EDGE_LOOP ( 'NONE', ( #24341, #10477, #1753, #30453 ) ) ;
#7421=CARTESIAN_POINT ( 'NONE',  ( 79.31644831670712392, 66.29498274501729327, -1.214491505233945334 ) ) ;
#7425=CARTESIAN_POINT ( 'NONE',  ( 75.34312381977423456, 60.33875818837522331, -3.724166978290133212 ) ) ;
#7429=CARTESIAN_POINT ( 'NONE',  ( 77.29563288604623494, 62.10585478181953079, 3.856837490696072290 ) ) ;
#7431=FACE_OUTER_BOUND ( 'NONE', #6994, .T. ) ;
#7435=CARTESIAN_POINT ( 'NONE',  ( 82.15165036511250207, 63.00212529317524002, 2.340562087103263078 ) ) ;
#7456=CARTESIAN_POINT ( 'NONE',  ( -73.45070404594234503, 38.65432087843066711, 9.800414904976365804 ) ) ;
#7461=CARTESIAN_POINT ( 'NONE',  ( 67.38390057489351648, 58.33093658501181267, -3.992553130659726168 ) ) ;
#7473=CARTESIAN_POINT ( 'NONE',  ( 79.78769048662040575, 65.07306089581300057, 3.312281065658529311 ) ) ;
#7477=ORIENTED_EDGE ( 'NONE', *, *, #30227, .T. ) ;
#7478=CARTESIAN_POINT ( 'NONE',  ( 79.66831987096976775, 61.58041732747442154, -3.164065397988993222 ) ) ;
#7482=CARTESIAN_POINT ( 'NONE',  ( 79.42963897889082148, 66.02853703565287447, -2.226826180274442457 ) ) ;
#7483=CARTESIAN_POINT ( 'NONE',  ( 80.30053069885686057, 62.24503436470106266, 3.340572457511948201 ) ) ;
#7487=CARTESIAN_POINT ( 'NONE',  ( 82.18775271763095702, 62.23297483488567394, 1.085061034363232979 ) ) ;
#7488=CARTESIAN_POINT ( 'NONE',  ( -64.08758708074093136, 41.04287353446839148, 3.000000000000000000 ) ) ;
#7490=CARTESIAN_POINT ( 'NONE',  ( -64.50921092724659900, 36.42665533667735644, -5.809226461016741894 ) ) ;
#7498=CARTESIAN_POINT ( 'NONE',  ( -63.08758708074093136, 41.04287353446839148, 3.000000000000000000 ) ) ;
#7507=CARTESIAN_POINT ( 'NONE',  ( 66.70283438698932343, 57.92520761901871396, 3.999543855873470388 ) ) ;
#7508=CARTESIAN_POINT ( 'NONE',  ( 71.78591447743995957, 60.68937113591298527, -3.856543183828340826 ) ) ;
#7522=CARTESIAN_POINT ( 'NONE',  ( 78.75925357433533236, 65.51276736450270732, -2.660933152496149479 ) ) ;
#7524=CARTESIAN_POINT ( 'NONE',  ( 80.87650043350870988, 61.69514696456048597, 2.603857329607122573 ) ) ;
#7536=AXIS2_PLACEMENT_3D ( 'NONE', #38904, #4547, #17069 ) ;
#7543=CARTESIAN_POINT ( 'NONE',  ( 80.28274408427736830, 64.63090917800610669, 3.500437194783546868 ) ) ;
#7553=CARTESIAN_POINT ( 'NONE',  ( 69.33847993643759366, 58.44820081139205570, 3.962610901733985447 ) ) ;
#7559=CARTESIAN_POINT ( 'NONE',  ( 78.65660921518627902, 66.03460256502702919, -1.194943971655633375 ) ) ;
#7560=DIRECTION ( 'NONE',  ( 0.4582725098355732163, -0.8888117386314183799, -1.924382947419148497E-16 ) ) ;
#7570=ORIENTED_EDGE ( 'NONE', *, *, #11465, .T. ) ;
#7571=CARTESIAN_POINT ( 'NONE',  ( 78.61080321328475407, 66.00207709680658752, -1.298998371267914953 ) ) ;
#7575=CARTESIAN_POINT ( 'NONE',  ( 81.12912465015324415, 61.32884242822650833, 1.592560325354579254 ) ) ;
#7587=AXIS2_PLACEMENT_3D ( 'NONE', #1633, #5323, #24456 ) ;
#7595=CARTESIAN_POINT ( 'NONE',  ( 80.65926296283299735, 64.83599339274636009, 3.316380171285409517 ) ) ;
#7614=CARTESIAN_POINT ( 'NONE',  ( 66.27376694609004915, 57.73522568913436004, -4.000000000000000000 ) ) ;
#7622=CARTESIAN_POINT ( 'NONE',  ( -57.81912131869246707, 32.28080896713289860, -4.194423477175957871 ) ) ;
#7625=EDGE_LOOP ( 'NONE', ( #4741, #30511, #37381, #19273 ) ) ;
#7629=CARTESIAN_POINT ( 'NONE',  ( 82.47129118679410453, 63.86074534520101764, -1.718006205139864129 ) ) ;
#7635=CARTESIAN_POINT ( 'NONE',  ( 76.07689452438883393, 60.24265224227302440, 3.527522301306113661 ) ) ;
#7644=CARTESIAN_POINT ( 'NONE',  ( 78.93443484242885688, 66.17773471521380202, 1.251938014746359240 ) ) ;
#7664=CARTESIAN_POINT ( 'NONE',  ( 67.19584252064707641, 57.93747020029492489, -3.996350724342223604 ) ) ;
#7666=ORIENTED_EDGE ( 'NONE', *, *, #13605, .F. ) ;
#7669=CARTESIAN_POINT ( 'NONE',  ( -59.87552183813128437, 24.84364830758654108, 9.681005660250221467 ) ) ;
#7677=CARTESIAN_POINT ( 'NONE',  ( 81.18025391627377019, 61.34316975053406651, 1.531260274641954133 ) ) ;
#7681=ORIENTED_EDGE ( 'NONE', *, *, #6318, .F. ) ;
#7682=CARTESIAN_POINT ( 'NONE',  ( 79.81867444595899030, 61.24600406626227311, -2.764360460937574260 ) ) ;
#7683=( BOUNDED_SURFACE ( )  B_SPLINE_SURFACE ( 3, 2, ( 
 ( #24814, #37355, #39324 ),
 ( #1082, #32966, #23874 ),
 ( #33170, #1887, #23684 ),
 ( #4956, #32573, #20386 ),
 ( #14009, #4752, #1680 ),
 ( #26784, #26188, #19989 ) ),
 .UNSPECIFIED., .F., .F., .F. ) 
 B_SPLINE_SURFACE_WITH_KNOTS ( ( 4, 2, 4 ),
 ( 3, 3 ),
 ( 0.000000000000000000, 0.001067213068432975882, 0.002134426136865951763 ),
 ( 0.000000000000000000, 1.000000000000000000 ),
 .UNSPECIFIED. ) 
 GEOMETRIC_REPRESENTATION_ITEM ( )  RATIONAL_B_SPLINE_SURFACE ( (
 ( 1.000000000000000000, 0.6872206705710276475, 1.000000000000000000),
 ( 1.000000000000000000, 0.6752582546152587906, 1.000000000000000000),
 ( 1.000000000000000000, 0.6623616715682778544, 1.000000000000000000),
 ( 1.000000000000000000, 0.6342435107462536248, 1.000000000000000000),
 ( 1.000000000000000000, 0.6188407181625764641, 1.000000000000000000),
 ( 1.000000000000000000, 0.6029302108204156463, 1.000000000000000000) ) ) 
 REPRESENTATION_ITEM ( '' )  SURFACE ( )  );
#7686=AXIS2_PLACEMENT_3D ( 'NONE', #4544, #7213, #32352 ) ;
#7687=CARTESIAN_POINT ( 'NONE',  ( 79.76387963405315418, 62.93107248426419176, 3.707164540951496168 ) ) ;
#7691=CARTESIAN_POINT ( 'NONE',  ( 81.04763707098177861, 66.10603528134694784, 1.133121492189030244 ) ) ;
#7694=CARTESIAN_POINT ( 'NONE',  ( -64.53809346645441281, 34.68836506924190388, -5.879071147244565587 ) ) ;
#7695=ORIENTED_EDGE ( 'NONE', *, *, #13605, .T. ) ;
#7700=CARTESIAN_POINT ( 'NONE',  ( -63.03213158086253287, 38.26878225442504800, 4.032857076801014351 ) ) ;
#7706=CIRCLE ( 'NONE', #6426, 2.999999999999998668 ) ;
#7709=VERTEX_POINT ( 'NONE', #34271 ) ;
#7711=CARTESIAN_POINT ( 'NONE',  ( 66.27376694608996388, 57.73522568913447373, 4.000000000000000000 ) ) ;
#7713=CARTESIAN_POINT ( 'NONE',  ( 73.49116904989887189, 59.86802450872643533, -3.864208391251975350 ) ) ;
#7717=PLANE ( 'NONE',  #16267 ) ;
#7722=EDGE_CURVE ( 'NONE', #32500, #30676, #24574, .T. ) ;
#7727=CARTESIAN_POINT ( 'NONE',  ( 80.03393078220564405, 63.38059744715224042, -3.720735635808767761 ) ) ;
#7729=CARTESIAN_POINT ( 'NONE',  ( 78.56188500726534585, 65.90376500477509580, 1.760837461004421733 ) ) ;
#7743=CARTESIAN_POINT ( 'NONE',  ( 79.02829278184948691, 65.95432764922182400, 2.098997056523008276 ) ) ;
#7745=DIRECTION ( 'NONE',  ( 1.000000000000000000, 0.000000000000000000, 0.000000000000000000 ) ) ;
#7755=CARTESIAN_POINT ( 'NONE',  ( 67.75953150630846267, 58.21208410194267202, 3.997018227265523027 ) ) ;
#7757=ADVANCED_FACE ( 'NONE', ( #488 ), #22313, .F. ) ;
#7758=CARTESIAN_POINT ( 'NONE',  ( -64.08758708074094557, 42.86724024650072096, -2.417504074514746026 ) ) ;
#7760=CARTESIAN_POINT ( 'NONE',  ( 80.26353224374044260, 64.23390916343181800, -3.625945587094181022 ) ) ;
#7763=CARTESIAN_POINT ( 'NONE',  ( -58.91620474891572456, 27.52990360452330876, 4.138963871842780584 ) ) ;
#7772=CARTESIAN_POINT ( 'NONE',  ( 80.99395165659464624, 61.72087377645419082, -2.545842637937974828 ) ) ;
#7774=CARTESIAN_POINT ( 'NONE',  ( 81.11594168931695492, 61.32525408782629484, 1.607835478472323221 ) ) ;
#7777=ORIENTED_EDGE ( 'NONE', *, *, #17403, .F. ) ;
#7782=CARTESIAN_POINT ( 'NONE',  ( -63.43903122600000444, 42.92536711289877616, -3.490931750529367772 ) ) ;
#7790=CARTESIAN_POINT ( 'NONE',  ( 81.00465555257858341, 64.24153452434767075, 3.375310687858767977 ) ) ;
#7792=DIRECTION ( 'NONE',  ( 0.000000000000000000, 0.000000000000000000, -1.000000000000000000 ) ) ;
#7821=CARTESIAN_POINT ( 'NONE',  ( -55.97227462678459631, 30.94442605972648508, -3.900682954687262782 ) ) ;
#7826=CARTESIAN_POINT ( 'NONE',  ( 81.75239774439246787, 65.41456323740523260, -1.882325606869287959 ) ) ;
#7834=CARTESIAN_POINT ( 'NONE',  ( 76.86947707741242652, 60.02096306738859255, 3.097219288968718676 ) ) ;
#7843=CARTESIAN_POINT ( 'NONE',  ( 79.43434746088968268, 66.19712225821035645, 1.744953761006671433 ) ) ;
#7860=VERTEX_POINT ( 'NONE', #24094 ) ;
#7864=CARTESIAN_POINT ( 'NONE',  ( 67.17215761800675011, 58.00255761909972563, -3.998533043703387690 ) ) ;
#7870=CARTESIAN_POINT ( 'NONE',  ( -59.89982099243564306, 24.84364830758654463, 9.562162450795216984 ) ) ;
#7872=ADVANCED_FACE ( 'NONE', ( #30285 ), #13129, .T. ) ;
#7877=CARTESIAN_POINT ( 'NONE',  ( 80.89892670780336914, 62.72941125082672187, 3.340002271463668571 ) ) ;
#7880=CARTESIAN_POINT ( 'NONE',  ( 78.21991615976335765, 63.09003589986988914, -3.816136337383043031 ) ) ;
#7883=CARTESIAN_POINT ( 'NONE',  ( 81.47197553453537466, 61.72158698297718615, -1.969816429101936439 ) ) ;
#7885=CARTESIAN_POINT ( 'NONE',  ( 80.13677637144074595, 61.33843513727117625, 2.660685394430964745 ) ) ;
#7888=CARTESIAN_POINT ( 'NONE',  ( 82.01097102582275511, 65.15803335478938152, 1.775718711109096404 ) ) ;
#7891=CARTESIAN_POINT ( 'NONE',  ( -62.87442376950072287, 35.57781650258913686, -5.904453864323630619 ) ) ;
#7895=EDGE_CURVE ( 'NONE', #38802, #34099, #1692, .T. ) ;
#7897=DIRECTION ( 'NONE',  ( 0.000000000000000000, 0.000000000000000000, 1.000000000000000000 ) ) ;
#7911=CARTESIAN_POINT ( 'NONE',  ( 66.27376694608996388, 57.73522568913447373, 4.000000000000000000 ) ) ;
#7912=CARTESIAN_POINT ( 'NONE',  ( 71.29558780583862188, 58.60460498947428931, -3.808711916423244581 ) ) ;
#7914=ORIENTED_EDGE ( 'NONE', *, *, #11645, .T. ) ;
#7925=CARTESIAN_POINT ( 'NONE',  ( 80.17375466371954928, 63.09909492358892180, -3.665158340976944817 ) ) ;
#7927=CARTESIAN_POINT ( 'NONE',  ( 79.26327435592847337, 64.69753611046425590, 3.458772244351174585 ) ) ;
#7934=CARTESIAN_POINT ( 'NONE',  ( 73.32739823182221528, 62.33856649896100777, -3.356242416136164142 ) ) ;
#7935=CIRCLE ( 'NONE', #28972, 2.500000000000002220 ) ;
#7940=CARTESIAN_POINT ( 'NONE',  ( 81.15583125883576088, 62.51952284974313301, 3.108243619504618138 ) ) ;
#7952=CARTESIAN_POINT ( 'NONE',  ( 67.89958468297673733, 58.72729936788584837, 3.969942683317638110 ) ) ;
#7956=CARTESIAN_POINT ( 'NONE',  ( 79.75420125634298074, 65.05222905597021565, -3.324099845469145276 ) ) ;
#7957=DIRECTION ( 'NONE',  ( -0.9267318687906764829, 0.3757233601570978965, 0.000000000000000000 ) ) ;
#7960=CARTESIAN_POINT ( 'NONE',  ( -59.14838763364235064, 27.28340689960987575, 4.628958989307227156 ) ) ;
#7965=CARTESIAN_POINT ( 'NONE',  ( 79.25227124789766719, 65.35518565838725635, -2.996423812020331479 ) ) ;
#7967=CARTESIAN_POINT ( 'NONE',  ( 80.23783879855322709, 63.84144632218769999, 3.668443954219270609 ) ) ;
#7971=CIRCLE ( 'NONE', #36265, 6.329987104167475565 ) ;
#7977=ORIENTED_EDGE ( 'NONE', *, *, #29022, .T. ) ;
#7983=CARTESIAN_POINT ( 'NONE',  ( 81.56578493134864516, 62.15373153752177871, 2.499697124809907578 ) ) ;
#8005=CARTESIAN_POINT ( 'NONE',  ( 66.27376694609004915, 57.73522568913436004, -4.000000000000000000 ) ) ;
#8007=DIRECTION ( 'NONE',  ( 1.000000000000000000, 0.000000000000000000, 0.000000000000000000 ) ) ;
#8009=DIRECTION ( 'NONE',  ( -1.000000000000000000, 0.000000000000000000, 0.000000000000000000 ) ) ;
#8012=CARTESIAN_POINT ( 'NONE',  ( -58.25352014915284826, 31.25337030895682133, -4.614317915849918350 ) ) ;
#8019=CARTESIAN_POINT ( 'NONE',  ( 80.71833143474471228, 65.93084270547788606, -2.217414436011610146 ) ) ;
#8024=CARTESIAN_POINT ( 'NONE',  ( 75.68633765818296411, 59.56198246982955169, 3.184487947857407963 ) ) ;
#8032=CARTESIAN_POINT ( 'NONE',  ( 81.56984355495256978, 61.60674381500906804, 1.524764441711115248 ) ) ;
#8046=CARTESIAN_POINT ( 'NONE',  ( -63.03213158086148837, 38.26878225442760595, -4.032857076800604901 ) ) ;
#8050=CARTESIAN_POINT ( 'NONE',  ( 67.71971274774827521, 58.31971506597766819, -3.997018227265501267 ) ) ;
#8063=CARTESIAN_POINT ( 'NONE',  ( 82.45631153319118312, 62.87735296625317005, -1.118100487915077546 ) ) ;
#8064=CARTESIAN_POINT ( 'NONE',  ( 80.54296318544949429, 63.62250603730376497, 3.633989118465184465 ) ) ;
#8067=CARTESIAN_POINT ( 'NONE',  ( 78.86847112531718551, 61.76850681771003337, -3.535928464255535530 ) ) ;
#8071=EDGE_CURVE ( 'NONE', #38621, #25777, #23119, .T. ) ;
#8072=CARTESIAN_POINT ( 'NONE',  ( 81.56787793379467644, 61.92707632880870960, -2.226826180274436240 ) ) ;
#8073=CARTESIAN_POINT ( 'NONE',  ( 79.93789898034924590, 60.96822905336945553, 2.313798345564227255 ) ) ;
#8076=CARTESIAN_POINT ( 'NONE',  ( 82.31572251369559012, 62.52525979466052064, 1.394285451509447382 ) ) ;
#8084=CYLINDRICAL_SURFACE ( 'NONE', #20438, 34.02204673211314656 ) ;
#8098=CARTESIAN_POINT ( 'NONE',  ( 73.43932658456094487, 59.98824119151031198, -3.894134109119617992 ) ) ;
#8102=DIRECTION ( 'NONE',  ( 0.000000000000000000, -0.5555716052200797561, -0.8314686954258614371 ) ) ;
#8111=CARTESIAN_POINT ( 'NONE',  ( 80.07543224467224263, 63.05907417235837187, -3.676305632669316203 ) ) ;
#8113=CARTESIAN_POINT ( 'NONE',  ( 80.17375466371993298, 63.09909492358909944, 3.665158340976903517 ) ) ;
#8129=CARTESIAN_POINT ( 'NONE',  ( 79.92139222979440660, 65.15389119341904234, 3.261148789966884287 ) ) ;
#8140=CARTESIAN_POINT ( 'NONE',  ( 68.17490759376208587, 57.99096015551094041, 3.964697573200901548 ) ) ;
#8145=CARTESIAN_POINT ( 'NONE',  ( 79.09180288389933366, 65.81009211479097587, -2.442092683901130545 ) ) ;
#8148=CARTESIAN_POINT ( 'NONE',  ( -58.12241481891157235, 28.59128022406730096, 4.921134609696964368 ) ) ;
#8155=CARTESIAN_POINT ( 'NONE',  ( 80.32629651820978722, 63.16159226777920566, -3.644176963625957111 ) ) ;
#8157=CARTESIAN_POINT ( 'NONE',  ( 78.93661819519711287, 65.67810670493912539, 2.545842637937921982 ) ) ;
#8161=EDGE_CURVE ( 'NONE', #23657, #24852, #33924, .T. ) ;
#8162=EDGE_CURVE ( 'NONE', #36353, #32421, #39259, .T. ) ;
#8163=CARTESIAN_POINT ( 'NONE',  ( 75.07588875331117606, 60.93231399735385878, -3.896954863271551162 ) ) ;
#8176=CARTESIAN_POINT ( 'NONE',  ( 79.40189760860924650, 66.01232247510012030, 2.246767365023765617 ) ) ;
#8204=CARTESIAN_POINT ( 'NONE',  ( 81.15619658878986797, 61.33623061796058806, -1.560659576774479973 ) ) ;
#8205=ORIENTED_EDGE ( 'NONE', *, *, #32608, .F. ) ;
#8212=CARTESIAN_POINT ( 'NONE',  ( 81.61324681686110694, 61.62795767120278612, -1.465632304122638452 ) ) ;
#8221=CARTESIAN_POINT ( 'NONE',  ( 76.13754644452941989, 60.10671110989439114, 3.424891502433685009 ) ) ;
#8229=CARTESIAN_POINT ( 'NONE',  ( 82.08208307362221490, 62.96685751817979337, 2.430878896394114808 ) ) ;
#8241=EDGE_CURVE ( 'NONE', #33614, #3549, #33935, .T. ) ;
#8248=CARTESIAN_POINT ( 'NONE',  ( 66.73521764480442187, 57.83500309307840581, -3.999076693781861813 ) ) ;
#8255=( BOUNDED_SURFACE ( )  B_SPLINE_SURFACE ( 3, 2, ( 
 ( #12958, #6178, #37859 ),
 ( #18720, #19341, #9663 ),
 ( #28188, #31704, #6388 ),
 ( #15, #12546, #3520 ),
 ( #2707, #12127, #1234 ),
 ( #20137, #19744, #7782 ),
 ( #31911, #7379, #32127 ),
 ( #10660, #29018, #19937 ),
 ( #32515, #17033, #1428 ),
 ( #822, #13960, #1026 ),
 ( #620, #13353, #26527 ),
 ( #13560, #4314, #22647 ),
 ( #28817, #26336, #13163 ),
 ( #23239, #35213, #38460 ),
 ( #25724, #16836, #38266 ),
 ( #22843, #6985, #19551 ) ),
 .UNSPECIFIED., .F., .F., .F. ) 
 B_SPLINE_SURFACE_WITH_KNOTS ( ( 4, 2, 2, 2, 2, 2, 2, 4 ),
 ( 3, 3 ),
 ( 6.938893903907228378E-18, 0.0008952345629814628409, 0.001342851844472190900, 0.001790469125962918743, 0.002238086407453646585, 0.002685703688944374862, 0.003133320970435102704, 0.003580938251925830547 ),
 ( 0.000000000000000000, 1.000000000000000000 ),
 .UNSPECIFIED. ) 
 GEOMETRIC_REPRESENTATION_ITEM ( )  RATIONAL_B_SPLINE_SURFACE ( (
 ( 1.000000000000000000, 0.7071067811865473507, 1.000000000000000000),
 ( 1.000000000000000000, 0.7332884733985617354, 1.000000000000000000),
 ( 1.000000000000000000, 0.7573851245654280584, 1.000000000000000000),
 ( 1.000000000000000000, 0.7911185894615297975, 1.000000000000000000),
 ( 1.000000000000000000, 0.8019092923332744594, 1.000000000000000000),
 ( 1.000000000000000000, 0.8220850550644049903, 1.000000000000000000),
 ( 1.000000000000000000, 0.8315581304763710602, 1.000000000000000000),
 ( 1.000000000000000000, 0.8492897706874269481, 1.000000000000000000),
 ( 1.000000000000000000, 0.8574674522647928177, 1.000000000000000000),
 ( 1.000000000000000000, 0.8719072631877536894, 1.000000000000000000),
 ( 1.000000000000000000, 0.8783188977574709622, 1.000000000000000000),
 ( 1.000000000000000000, 0.8888416513947781095, 1.000000000000000000),
 ( 1.000000000000000000, 0.8929346545673477742, 1.000000000000000000),
 ( 1.000000000000000000, 0.8985797510527644416, 1.000000000000000000),
 ( 1.000000000000000000, 0.9000264109954028147, 1.000000000000000000),
 ( 1.000000000000000000, 0.9000259740535768715, 1.000000000000000000) ) ) 
 REPRESENTATION_ITEM ( '' )  SURFACE ( )  );
#8261=CARTESIAN_POINT ( 'NONE',  ( 82.54941478318325210, 63.90107490703079662, -1.303631908149876617 ) ) ;
#8262=CARTESIAN_POINT ( 'NONE',  ( 78.72446908900997187, 66.04077733106291248, 1.541060042019483989 ) ) ;
#8266=CARTESIAN_POINT ( 'NONE',  ( 77.65955580186951579, 62.78993503910590590, -3.839379600940507231 ) ) ;
#8269=CARTESIAN_POINT ( 'NONE',  ( 81.40003982928756443, 62.35377290961280750, -2.797238656122826850 ) ) ;
#8270=CARTESIAN_POINT ( 'NONE',  ( 78.15185181088402544, 63.91595853815784523, 3.616565173810659672 ) ) ;
#8274=CARTESIAN_POINT ( 'NONE',  ( 78.98267122246093663, 66.20432814577486624, 1.134074597586614663 ) ) ;
#8291=AXIS2_PLACEMENT_3D ( 'NONE', #39843, #20686, #5254 ) ;
#8301=CARTESIAN_POINT ( 'NONE',  ( 66.41407057682036452, 57.81332248272642715, 4.000000000000022204 ) ) ;
#8303=CARTESIAN_POINT ( 'NONE',  ( 73.68879688780705806, 59.40709336146452557, -3.677837812263893280 ) ) ;
#8307=DIRECTION ( 'NONE',  ( -0.000000000000000000, -0.000000000000000000, -1.000000000000000000 ) ) ;
#8319=CARTESIAN_POINT ( 'NONE',  ( 79.65304550238739978, 63.88563316389422653, -3.730195463674648604 ) ) ;
#8321=CARTESIAN_POINT ( 'NONE',  ( 81.83960663661402180, 62.56551448482339595, -2.484976468875490063 ) ) ;
#8322=CARTESIAN_POINT ( 'NONE',  ( 78.43571320973860850, 65.80086540191352640, 1.884339924308606085 ) ) ;
#8347=CARTESIAN_POINT ( 'NONE',  ( 67.69980720754315939, 58.37350455430767937, 3.995247128881052046 ) ) ;
#8355=DIRECTION ( 'NONE',  ( -1.000000000000000000, 0.000000000000000000, 0.000000000000000000 ) ) ;
#8356=CARTESIAN_POINT ( 'NONE',  ( -57.95974551600828306, 28.52258727176715780, 2.765331207962179239 ) ) ;
#8363=CARTESIAN_POINT ( 'NONE',  ( 79.45910779949859659, 64.84755599131122494, -3.411701596789212143 ) ) ;
#8367=CARTESIAN_POINT ( 'NONE',  ( 79.06216475166051794, 65.51459655345146871, 2.804471013201318197 ) ) ;
#8371=VECTOR ( 'NONE', #21107, 1000.000000000000000 ) ;
#8372=CARTESIAN_POINT ( 'NONE',  ( 74.44738948069034734, 59.23650550459285569, -3.391332960764822602 ) ) ;
#8385=CARTESIAN_POINT ( 'NONE',  ( 80.04208101465529523, 65.56312698749549384, 2.920975158735862998 ) ) ;
#8391=ADVANCED_FACE ( 'NONE', ( #23181 ), #10495, .T. ) ;
#8408=CARTESIAN_POINT ( 'NONE',  ( 81.26385631823474398, 62.29349618781996156, -2.861733672647096327 ) ) ;
#8417=CARTESIAN_POINT ( 'NONE',  ( 79.53763471700084153, 65.25825451995501680, -3.163072811751571400 ) ) ;
#8422=CARTESIAN_POINT ( 'NONE',  ( 81.40691186390333201, 61.43583663329572886, -1.251938014746444727 ) ) ;
#8428=CARTESIAN_POINT ( 'NONE',  ( 74.39246203999459794, 62.41596060291492876, 3.584990529380562840 ) ) ;
#8434=CARTESIAN_POINT ( 'NONE',  ( -65.87013514635467004, 36.66000420377765323, 7.725785790319501523 ) ) ;
#8435=CARTESIAN_POINT ( 'NONE',  ( 79.40575531231837658, 66.18134094231186282, 1.781440269582215796 ) ) ;
#8445=DIRECTION ( 'NONE',  ( 0.000000000000000000, 0.000000000000000000, -1.000000000000000000 ) ) ;
#8447=DIRECTION ( 'NONE',  ( -1.000000000000000000, 0.000000000000000000, 0.000000000000000000 ) ) ;
#8451=EDGE_CURVE ( 'NONE', #14204, #11497, #21690, .T. ) ;
#8455=CARTESIAN_POINT ( 'NONE',  ( 66.90457105084450973, 57.82508126828634687, -3.996770903026528821 ) ) ;
#8461=CARTESIAN_POINT ( 'NONE',  ( 70.64617143260556986, 60.54601068761595428, 3.764554023424209195 ) ) ;
#8469=CARTESIAN_POINT ( 'NONE',  ( 81.35706873939176376, 65.93413826765579699, -1.145133701562419226 ) ) ;
#8470=CARTESIAN_POINT ( 'NONE',  ( 78.65282594500106939, 66.03191569515874448, 1.205449537698852325 ) ) ;
#8474=CARTESIAN_POINT ( 'NONE',  ( 78.73442292448854118, 62.77418112150552787, -3.804514705604311597 ) ) ;
#8477=CARTESIAN_POINT ( 'NONE',  ( 79.82819440665738853, 65.73008711144039751, -2.710336141770836704 ) ) ;
#8478=CARTESIAN_POINT ( 'NONE',  ( 80.27394690667868815, 60.98324426164374046, 1.908681007153611553 ) ) ;
#8479=ORIENTED_EDGE ( 'NONE', *, *, #3817, .T. ) ;
#8483=CARTESIAN_POINT ( 'NONE',  ( 80.00335259508514696, 66.34466434620095754, 1.325417871280148985 ) ) ;
#8511=CARTESIAN_POINT ( 'NONE',  ( 66.27376694608996388, 57.73522568913447373, 4.000000000000000000 ) ) ;
#8512=CARTESIAN_POINT ( 'NONE',  ( 69.07430361466936120, 59.13263628650475567, -3.969490915146614007 ) ) ;
#8515=DIRECTION ( 'NONE',  ( -0.000000000000000000, -0.000000000000000000, -1.000000000000000000 ) ) ;
#8522=CARTESIAN_POINT ( 'NONE',  ( 28.52663967383706023, 50.14399159706753295, -4.000000000000000000 ) ) ;
#8524=LINE ( 'NONE', #12230, #8371 ) ;
#8527=CARTESIAN_POINT ( 'NONE',  ( 78.56734957671525876, 65.55328818492539256, -2.456741006817813044 ) ) ;
#8529=CARTESIAN_POINT ( 'NONE',  ( 81.81391746733736170, 63.52311930392504280, -2.869341960395655811 ) ) ;
#8531=CARTESIAN_POINT ( 'NONE',  ( 79.12445352002978893, 64.93440905817641351, 3.301258712451524246 ) ) ;
#8538=ORIENTED_EDGE ( 'NONE', *, *, #39487, .T. ) ;
#8555=VERTEX_POINT ( 'NONE', #15276 ) ;
#8556=CARTESIAN_POINT ( 'NONE',  ( 67.72966869545554403, 58.29280778740498192, 3.997461085607385556 ) ) ;
#8572=CARTESIAN_POINT ( 'NONE',  ( 78.72772338417257743, 65.90741647005499715, -1.973779052376060328 ) ) ;
#8574=CARTESIAN_POINT ( 'NONE',  ( 78.62745313524290225, 65.95871297147078849, 1.682919622592493614 ) ) ;
#8579=CARTESIAN_POINT ( 'NONE',  ( 73.56486102181378328, 61.25343517167133456, -3.876585409328608289 ) ) ;
#8588=EDGE_LOOP ( 'NONE', ( #29598, #30625, #38658 ) ) ;
#8590=EDGE_CURVE ( 'NONE', #15868, #27566, #28256, .T. ) ;
#8594=CARTESIAN_POINT ( 'NONE',  ( 81.43301797337210246, 62.09285590259239740, 2.578835243349299144 ) ) ;
#8608=ORIENTED_EDGE ( 'NONE', *, *, #14333, .F. ) ;
#8610=CARTESIAN_POINT ( 'NONE',  ( 80.49267809498161341, 64.35807816991642483, -3.549391953833855862 ) ) ;
#8619=CARTESIAN_POINT ( 'NONE',  ( 79.66028364141931206, 64.99138685963065143, -3.354617312347329960 ) ) ;
#8621=CARTESIAN_POINT ( 'NONE',  ( -58.78362175692702607, 29.48419490076549465, -5.741263644839468938 ) ) ;
#8627=CARTESIAN_POINT ( 'NONE',  ( 82.29984285855074688, 63.07754316838579456, -2.094266784919526447 ) ) ;
#8635=CARTESIAN_POINT ( 'NONE',  ( 73.74018914705078487, 60.85874216252894087, 3.935025356190109402 ) ) ;
#8644=CARTESIAN_POINT ( 'NONE',  ( 81.98137654593483603, 62.63634409986677554, 2.334361474588996899 ) ) ;
#8648=CARTESIAN_POINT ( 'NONE',  ( -64.08758708074093136, 38.55573457772739943, 2.999999999999998668 ) ) ;
#8660=CARTESIAN_POINT ( 'NONE',  ( 66.85348068378573316, 57.96691244536589238, -3.999524142431097218 ) ) ;
#8661=CARTESIAN_POINT ( 'NONE',  ( -66.99872204295122913, 28.48507918597134037, -12.49999999999999645 ) ) ;
#8673=CARTESIAN_POINT ( 'NONE',  ( 80.03496335128151884, 66.36160760684386162, -1.000000000000000000 ) ) ;
#8674=CARTESIAN_POINT ( 'NONE',  ( 81.15742489870845588, 61.60174059333854757, 2.174925636353720382 ) ) ;
#8677=CARTESIAN_POINT ( 'NONE',  ( 78.85022303194006099, 62.54057813906803176, -3.766285651913924060 ) ) ;
#8680=CARTESIAN_POINT ( 'NONE',  ( 81.41366110773520859, 61.69541933536140732, -2.011547652602695191 ) ) ;
#8681=CARTESIAN_POINT ( 'NONE',  ( 80.07249602437107683, 61.49066053983646185, 2.889371261047465556 ) ) ;
#8689=CARTESIAN_POINT ( 'NONE',  ( 78.69020857030076854, 66.05846869611056604, 1.014334479594652283 ) ) ;
#8697=CARTESIAN_POINT ( 'NONE',  ( -62.86576508122317364, 38.67912974266874926, 6.999999999999999112 ) ) ;
#8705=B_SPLINE_CURVE_WITH_KNOTS ( 'NONE', 3,
 ( #32355, #23277, #16667, #13598, #38702, #23081 ),
 .UNSPECIFIED., .F., .F.,
 ( 4, 2, 4 ),
 ( 4.336808689942017255E-19, 0.001065454728147860767, 0.002130909456295721101 ),
 .UNSPECIFIED. ) ;
#8710=CARTESIAN_POINT ( 'NONE',  ( 17.97454669799173033, 51.66243977840390755, -4.000000000000000000 ) ) ;
#8715=CARTESIAN_POINT ( 'NONE',  ( 70.06771224146353916, 58.30163689823704942, -3.863726395435713723 ) ) ;
#8720=CARTESIAN_POINT ( 'NONE',  ( 69.87460780774588898, 58.79389746341001199, 3.972683913566375402 ) ) ;
#8729=CARTESIAN_POINT ( 'NONE',  ( 80.71160662450162704, 61.49558808705153012, -2.436540443961501268 ) ) ;
#8731=CARTESIAN_POINT ( 'NONE',  ( 81.54961753534276170, 61.59690320141230302, -1.551099981298398767 ) ) ;
#8733=CARTESIAN_POINT ( 'NONE',  ( 80.91727723835764152, 61.27046310099957793, 1.796258654642569841 ) ) ;
#8743=DIRECTION ( 'NONE',  ( 0.000000000000000000, 0.000000000000000000, 1.000000000000000000 ) ) ;
#8757=CARTESIAN_POINT ( 'NONE',  ( 67.13660786288076565, 58.10023080654656980, 3.998533043703386802 ) ) ;
#8760=AXIS2_PLACEMENT_3D ( 'NONE', #5505, #27935, #40478 ) ;
#8770=VERTEX_POINT ( 'NONE', #36410 ) ;
#8771=CARTESIAN_POINT ( 'NONE',  ( 78.83217078968475278, 65.79276158749699732, -2.259810845157019354 ) ) ;
#8773=CARTESIAN_POINT ( 'NONE',  ( 79.76446817951413948, 64.32424044856642809, 3.638935937159315515 ) ) ;
#8777=CARTESIAN_POINT ( 'NONE',  ( 74.49653936242856389, 60.69398666642196360, -3.911020515999844793 ) ) ;
#8789=CIRCLE ( 'NONE', #10762, 1.000000000000002220 ) ;
#8791=CARTESIAN_POINT ( 'NONE',  ( 81.39159673219469937, 61.52361671445412128, 1.704083397384870358 ) ) ;
#8793=DIRECTION ( 'NONE',  ( -0.000000000000000000, -0.000000000000000000, -1.000000000000000000 ) ) ;
#8795=DIRECTION ( 'NONE',  ( 0.8831583674551003460, -0.4690749385695657803, 0.000000000000000000 ) ) ;
#8799=CARTESIAN_POINT ( 'NONE',  ( -68.98442902999595105, 21.93515443114010210, 12.49999999999999645 ) ) ;
#8809=CARTESIAN_POINT ( 'NONE',  ( 79.05590852586871620, 65.97304283769159383, -2.079311677127757108 ) ) ;
#8822=CARTESIAN_POINT ( 'NONE',  ( 80.77858121287650306, 63.01782502344087078, -3.459421039841290568 ) ) ;
#8824=ORIENTED_EDGE ( 'NONE', *, *, #20485, .F. ) ;
#8827=EDGE_LOOP ( 'NONE', ( #29431, #36786, #2860, #19796 ) ) ;
#8828=CARTESIAN_POINT ( 'NONE',  ( 81.63785901438869530, 61.64013749223433081, -1.421876342974254248 ) ) ;
#8829=CARTESIAN_POINT ( 'NONE',  ( -2.954197855305039422, -12.43481156997016157, -1.000000000000000000 ) ) ;
#8836=CARTESIAN_POINT ( 'NONE',  ( 74.68367562674023930, 60.27297886100710400, 3.815996826674382447 ) ) ;
#8840=VECTOR ( 'NONE', #4084, 1000.000000000000000 ) ;
#8845=CARTESIAN_POINT ( 'NONE',  ( 81.37441939350044606, 61.42019823254032218, 1.301239782962658964 ) ) ;
#8864=CARTESIAN_POINT ( 'NONE',  ( 66.99315907379003932, 58.03889713220680591, -3.999016414675010012 ) ) ;
#8874=CIRCLE ( 'NONE', #5602, 7.999999999999986677 ) ;
#8880=CARTESIAN_POINT ( 'NONE',  ( 82.45631153319118312, 62.87735296625317005, -1.000000000000000000 ) ) ;
#8881=CARTESIAN_POINT ( 'NONE',  ( 80.68955802291256418, 62.97990070207239199, 3.482375488376183270 ) ) ;
#8883=ORIENTED_EDGE ( 'NONE', *, *, #6993, .T. ) ;
#8884=CARTESIAN_POINT ( 'NONE',  ( 76.72614680668752385, 63.26816225425363172, -3.643081266322632406 ) ) ;
#8888=CARTESIAN_POINT ( 'NONE',  ( 79.40189760861154866, 66.01232247510107243, -2.246767365022174001 ) ) ;
#8889=CARTESIAN_POINT ( 'NONE',  ( 78.71019189666364468, 60.57837954350641496, 2.701592190111063552 ) ) ;
#8892=CARTESIAN_POINT ( 'NONE',  ( 81.75239774439276630, 65.41456323740531786, 1.882325606868447299 ) ) ;
#8893=CARTESIAN_POINT ( 'NONE',  ( -64.85784325972055342, 34.81586596186931359, 6.466735817496056526 ) ) ;
#8899=CARTESIAN_POINT ( 'NONE',  ( -64.47965924086506107, 36.51034344918481622, 5.743161323598027224 ) ) ;
#8909=DIRECTION ( 'NONE',  ( -1.000000000000000000, 0.000000000000000000, 0.000000000000000000 ) ) ;
#8920=CARTESIAN_POINT ( 'NONE',  ( 70.76671532128065678, 59.91573877893261368, -3.942344351592494966 ) ) ;
#8937=CARTESIAN_POINT ( 'NONE',  ( 78.62541471602109766, 65.39282990155331277, -2.732428818688202199 ) ) ;
#8939=CARTESIAN_POINT ( 'NONE',  ( 81.63129934975491153, 61.79668339569251145, -1.832274617051100618 ) ) ;
#8940=CARTESIAN_POINT ( 'NONE',  ( 79.24578529683977024, 64.32976145010150049, 3.589982250315052692 ) ) ;
#8955=LINE ( 'NONE', #34321, #16174 ) ;
#8962=CARTESIAN_POINT ( 'NONE',  ( 67.49481586879284123, 58.02828806359071478, 3.995059460290581121 ) ) ;
#8967=CARTESIAN_POINT ( 'NONE',  ( -60.81661347076553170, 25.20155461598435309, 9.800414904976365804 ) ) ;
#8982=CARTESIAN_POINT ( 'NONE',  ( 78.91366476310541600, 65.65666373793331445, -2.561782662428539137 ) ) ;
#8984=CARTESIAN_POINT ( 'NONE',  ( 81.03127633846482070, 61.72971393008359797, 2.526545245021025288 ) ) ;
#8987=CARTESIAN_POINT ( 'NONE',  ( 74.25112698293331448, 59.69246930110610805, -3.692213121326705760 ) ) ;
#8989=CARTESIAN_POINT ( 'NONE',  ( -58.97367982820826171, 28.25997590259050440, 6.371614496329753408 ) ) ;
#8991=FACE_OUTER_BOUND ( 'NONE', #36882, .T. ) ;
#9004=CARTESIAN_POINT ( 'NONE',  ( 79.87861596566079925, 65.47018085071599103, 3.015642068896304817 ) ) ;
#9013=DIRECTION ( 'NONE',  ( 0.7864880931482284288, 0.000000000000000000, -0.6176054398530371747 ) ) ;
#9020=EDGE_CURVE ( 'NONE', #29749, #36272, #2690, .T. ) ;
#9021=ORIENTED_EDGE ( 'NONE', *, *, #3905, .F. ) ;
#9022=CARTESIAN_POINT ( 'NONE',  ( 81.30779604900573077, 61.65202803940792364, -2.079311677127713587 ) ) ;
#9025=DIRECTION ( 'NONE',  ( -1.000000000000000000, 0.000000000000000000, 0.000000000000000000 ) ) ;
#9033=CARTESIAN_POINT ( 'NONE',  ( 81.10109024085375040, 61.27893947540407993, -1.252362053669520359 ) ) ;
#9034=CARTESIAN_POINT ( 'NONE',  ( -58.64967482348269101, 27.97946873212456609, -5.671478272894442618 ) ) ;
#9039=CARTESIAN_POINT ( 'NONE',  ( 81.44289297360079161, 64.86039221060740090, -2.864610283900680621 ) ) ;
#9046=CARTESIAN_POINT ( 'NONE',  ( 73.68879688780705806, 59.40709336146452557, 3.677837812263893280 ) ) ;
#9052=CARTESIAN_POINT ( 'NONE',  ( -58.55403975902957114, 30.31577878493534328, -5.141676377603731751 ) ) ;
#9054=CARTESIAN_POINT ( 'NONE',  ( -55.09640557796760874, 31.27756524517855041, -1.408921623440186677 ) ) ;
#9055=CARTESIAN_POINT ( 'NONE',  ( 79.08571093829937126, 66.16712123189805084, 1.622497907168705122 ) ) ;
#9060=ADVANCED_FACE ( 'NONE', ( #32290 ), #3990, .T. ) ;
#9071=ADVANCED_FACE ( 'NONE', ( #25893 ), #11835, .F. ) ;
#9077=CARTESIAN_POINT ( 'NONE',  ( 66.96362040430034313, 58.12048686563063882, -3.996315564296189837 ) ) ;
#9089=CARTESIAN_POINT ( 'NONE',  ( 82.39191784114034078, 64.57324092874033283, -1.480606629406893804 ) ) ;
#9092=EDGE_CURVE ( 'NONE', #1802, #22985, #592, .T. ) ;
#9093=CARTESIAN_POINT ( 'NONE',  ( 78.81037980241194418, 65.98117473861063331, 1.881209715725460807 ) ) ;
#9096=CARTESIAN_POINT ( 'NONE',  ( 76.55173188639216164, 63.61528062424579133, -3.435658781974418208 ) ) ;
#9099=CARTESIAN_POINT ( 'NONE',  ( 80.52090910898354537, 64.76150916408994362, -3.396356880839462633 ) ) ;
#9100=CARTESIAN_POINT ( 'NONE',  ( 76.55173188639217585, 63.61528062424576291, 3.435658781974429754 ) ) ;
#9104=CARTESIAN_POINT ( 'NONE',  ( -58.28298022874874107, 31.18432397053788563, 4.639529439632331886 ) ) ;
#9105=CARTESIAN_POINT ( 'NONE',  ( 82.47197227462061164, 63.49890707693140257, 1.793694987645559680 ) ) ;
#9106=CARTESIAN_POINT ( 'NONE',  ( -64.08758708074094557, 43.19434570387343086, 2.104943988446417169 ) ) ;
#9112=CARTESIAN_POINT ( 'NONE',  ( -63.41460867333827167, 35.63977781315514193, -6.822401110719517270 ) ) ;
#9118=CARTESIAN_POINT ( 'NONE',  ( 78.50997293154887302, 60.39266868650268094, 2.556923618988971914 ) ) ;
#9121=CARTESIAN_POINT ( 'NONE',  ( 67.59755685981747320, 57.89445231122055446, -3.999999999999877875 ) ) ;
#9127=CARTESIAN_POINT ( 'NONE',  ( -64.08758708074093136, 36.14363715547679590, -3.800414904976364028 ) ) ;
#9133=CARTESIAN_POINT ( 'NONE',  ( 69.99634961962405555, 58.48381665884328839, -3.916752429509929190 ) ) ;
#9144=CARTESIAN_POINT ( 'NONE',  ( 80.62600653171161014, 61.47375110407241294, -2.475680338657084256 ) ) ;
#9146=CARTESIAN_POINT ( 'NONE',  ( 80.82569761265823161, 65.28806468744758718, -2.919551171211518970 ) ) ;
#9147=CARTESIAN_POINT ( 'NONE',  ( 79.14523234120532891, 64.60782394083949498, 3.482780605906210525 ) ) ;
#9157=EDGE_CURVE ( 'NONE', #10884, #7860, #9323, .T. ) ;
#9166=DIRECTION ( 'NONE',  ( 0.3757233601570931225, 0.9267318687906784813, 0.000000000000000000 ) ) ;
#9168=CARTESIAN_POINT ( 'NONE',  ( -66.12008681484671513, 35.44165918782573499, -8.117242773420016988 ) ) ;
#9169=DIRECTION ( 'NONE',  ( 0.000000000000000000, -0.000000000000000000, -1.000000000000000000 ) ) ;
#9176=CARTESIAN_POINT ( 'NONE',  ( 67.14253272251396254, 58.08395421452478757, 3.998868826385352460 ) ) ;
#9186=CARTESIAN_POINT ( 'NONE',  ( -63.99293516169446150, 35.89893413629672381, -46.17089178453873188 ) ) ;
#9189=CIRCLE ( 'NONE', #6599, 2.500000000000002220 ) ;
#9191=CARTESIAN_POINT ( 'NONE',  ( 78.57794565308390133, 65.91709162046845449, -1.743126864185871705 ) ) ;
#9193=CARTESIAN_POINT ( 'NONE',  ( 80.83598165300548999, 61.89502789394175863, 2.843122152733552177 ) ) ;
#9198=CARTESIAN_POINT ( 'NONE',  ( -73.07498068578524908, 39.58105274722134226, 12.49999999999999645 ) ) ;
#9208=CARTESIAN_POINT ( 'NONE',  ( 79.33055955479062504, 65.97011375961720603, 2.296576099417798833 ) ) ;
#9214=ORIENTED_EDGE ( 'NONE', *, *, #17230, .T. ) ;
#9216=TOROIDAL_SURFACE ( 'NONE', #14471, 67.42751648247021024, 3.000000000000000000 ) ;
#9218=CARTESIAN_POINT ( 'NONE',  ( -68.33309634912853880, 36.51831931741240567, -8.800414904976365804 ) ) ;
#9224=CARTESIAN_POINT ( 'NONE',  ( 81.32777602152022212, 61.82240453612693187, -2.372413575842100997 ) ) ;
#9235=CARTESIAN_POINT ( 'NONE',  ( 81.09516781258611218, 61.58556622376320888, -2.215902410107941645 ) ) ;
#9237=CARTESIAN_POINT ( 'NONE',  ( -9.439742135462632078, 51.66544268451064426, 1.000000000000000000 ) ) ;
#9242=CARTESIAN_POINT ( 'NONE',  ( 81.15665777833298478, 65.46403653819187696, -2.541832380859318619 ) ) ;
#9248=FACE_OUTER_BOUND ( 'NONE', #26263, .T. ) ;
#9249=CARTESIAN_POINT ( 'NONE',  ( 73.49116904989887189, 59.86802450872643533, 3.864208391251975350 ) ) ;
#9251=ORIENTED_EDGE ( 'NONE', *, *, #6993, .F. ) ;
#9255=VERTEX_POINT ( 'NONE', #5478 ) ;
#9257=CARTESIAN_POINT ( 'NONE',  ( 81.30277405988996975, 64.78683171160542997, 3.017922835037553320 ) ) ;
#9268=CARTESIAN_POINT ( 'NONE',  ( -2.954197855305039422, -12.43481156997016157, -1.000000000000000000 ) ) ;
#9271=ORIENTED_EDGE ( 'NONE', *, *, #33288, .F. ) ;
#9277=CARTESIAN_POINT ( 'NONE',  ( 66.55417948260128469, 57.87814544581552667, -3.999688274315071901 ) ) ;
#9279=CARTESIAN_POINT ( 'NONE',  ( -56.05592576813391048, 30.85738657449499200, 3.898523360614989386 ) ) ;
#9281=CARTESIAN_POINT ( 'NONE',  ( 69.01538019125142398, 59.48397956797946762, 3.903581769792375145 ) ) ;
#9286=CARTESIAN_POINT ( 'NONE',  ( 81.01700449632683387, 66.08979032036403112, -1.386429027374526335 ) ) ;
#9289=CARTESIAN_POINT ( 'NONE',  ( 81.02339296473685692, 62.20010510126473235, 2.956864960647747065 ) ) ;
#9292=CARTESIAN_POINT ( 'NONE',  ( 77.35950424652850188, 60.48040194676352144, -3.253266109310609888 ) ) ;
#9296=CARTESIAN_POINT ( 'NONE',  ( 81.27876882982985762, 62.57402737888430266, -3.057227112800022795 ) ) ;
#9297=CARTESIAN_POINT ( 'NONE',  ( 79.13122682291692911, 61.20693062157217668, 3.102003663616994533 ) ) ;
#9301=LINE ( 'NONE', #31759, #11788 ) ;
#9303=CARTESIAN_POINT ( 'NONE',  ( 81.78811924970003133, 65.04137315806649156, 2.360008641314786715 ) ) ;
#9308=CARTESIAN_POINT ( 'NONE',  ( -62.77981399768980708, 36.45869984972385680, -4.735036014756413891 ) ) ;
#9309=CARTESIAN_POINT ( 'NONE',  ( -62.74554520265134272, 35.90271204080874412, 5.263896983009515473 ) ) ;
#9317=CARTESIAN_POINT ( 'NONE',  ( 81.01435898429377858, 61.24732411474661831, -1.383612818681232426 ) ) ;
#9323=B_SPLINE_CURVE_WITH_KNOTS ( 'NONE', 3,
 ( #4864, #29580, #30397, #5272, #26891, #11022, #27094, #35971, #2003, #26698, #17398, #20705, #20105, #23404, #39643, #20497 ),
 .UNSPECIFIED., .F., .F.,
 ( 4, 2, 2, 2, 2, 2, 2, 4 ),
 ( 0.000000000000000000, 0.0004252485765279650489, 0.0008504971530559300979, 0.001275745729583895038, 0.001700994306111860196, 0.002126242882639825353, 0.002551491459167790077, 0.003401988612223739907 ),
 .UNSPECIFIED. ) ;
#9328=CARTESIAN_POINT ( 'NONE',  ( 69.43824574602471955, 58.18893279706789201, -3.907754234428237439 ) ) ;
#9343=CARTESIAN_POINT ( 'NONE',  ( 79.84787171156668251, 62.37423782317880239, -3.536670452273173559 ) ) ;
#9346=CARTESIAN_POINT ( 'NONE',  ( 81.34095870999071565, 61.40448684960411896, -1.344573736155065813 ) ) ;
#9347=CARTESIAN_POINT ( 'NONE',  ( 80.06304181921890972, 62.74582375469539386, 3.589982250315065127 ) ) ;
#9358=DIRECTION ( 'NONE',  ( 0.9267318687906771491, -0.3757233601570964532, -0.000000000000000000 ) ) ;
#9371=CYLINDRICAL_SURFACE ( 'NONE', #5629, 64.42751648247021024 ) ;
#9374=CARTESIAN_POINT ( 'NONE',  ( 67.17215761800675011, 58.00255761909972563, 3.998533043703387690 ) ) ;
#9378=CARTESIAN_POINT ( 'NONE',  ( -68.98442902999595105, 21.93515443114010210, 9.800414904976365804 ) ) ;
#9380=ADVANCED_FACE ( 'NONE', ( #29139 ), #22967, .F. ) ;
#9388=UNCERTAINTY_MEASURE_WITH_UNIT (LENGTH_MEASURE( 1.000000000000000082E-05 ), #29902, 'distance_accuracy_value', 'NONE');
#9390=CARTESIAN_POINT ( 'NONE',  ( 80.93996669421788681, 61.38942684853014953, -2.064111563736698240 ) ) ;
#9392=CARTESIAN_POINT ( 'NONE',  ( 80.98923082824005348, 61.23822351929057106, 1.409197735201532131 ) ) ;
#9397=CARTESIAN_POINT ( 'NONE',  ( -58.48742492228146261, 29.43916413120543396, 5.126953147108460840 ) ) ;
#9402=ORIENTED_EDGE ( 'NONE', *, *, #33345, .F. ) ;
#9404=CIRCLE ( 'NONE', #23887, 2.500000000000002220 ) ;
#9405=DIRECTION ( 'NONE',  ( -0.9995570907297059993, -0.02975940812527387222, 2.753298341658001615E-16 ) ) ;
#9407=CARTESIAN_POINT ( 'NONE',  ( 80.86168855680165279, 64.16696250863010675, 3.456914256421386167 ) ) ;
#9421=AXIS2_PLACEMENT_3D ( 'NONE', #12429, #94, #34481 ) ;
#9424=CARTESIAN_POINT ( 'NONE',  ( 80.17018276713265834, 64.56786917328069819, -3.540619799101245579 ) ) ;
#9427=CARTESIAN_POINT ( 'NONE',  ( -61.00670947824507806, 24.84364830758654108, 8.800414904976364028 ) ) ;
#9435=AXIS2_PLACEMENT_3D ( 'NONE', #307, #31597, #3614 ) ;
#9436=EDGE_CURVE ( 'NONE', #21757, #8555, #17742, .T. ) ;
#9439=CARTESIAN_POINT ( 'NONE',  ( 79.76203521409539121, 64.68678814937342736, -3.489836119548951121 ) ) ;
#9452=CARTESIAN_POINT ( 'NONE',  ( 74.25112698293331448, 59.69246930110610805, 3.692213121326705760 ) ) ;
#9458=CARTESIAN_POINT ( 'NONE',  ( -54.89808584415116144, 31.42838494644043124, -1.178527023292115006 ) ) ;
#9459=CARTESIAN_POINT ( 'NONE',  ( 81.83449460947102239, 63.17368474096263498, 2.819252638153798340 ) ) ;
#9469=TOROIDAL_SURFACE ( 'NONE', #27198, 114.6618724293813898, 3.000000000000000000 ) ;
#9477=CARTESIAN_POINT ( 'NONE',  ( 66.42792150476888935, 57.77419247997853091, -4.000000000000011546 ) ) ;
#9481=CARTESIAN_POINT ( 'NONE',  ( -57.02355111755381500, 29.45914411650387166, 1.982879248426694607 ) ) ;
#9485=DIRECTION ( 'NONE',  ( 0.000000000000000000, 0.000000000000000000, 1.000000000000000000 ) ) ;
#9492=CARTESIAN_POINT ( 'NONE',  ( 78.69031774315028827, 66.05854625464691310, -1.008685033153519983 ) ) ;
#9493=CARTESIAN_POINT ( 'NONE',  ( 81.19486284036338475, 61.45157923659407828, 1.862141363775751568 ) ) ;
#9496=DIRECTION ( 'NONE',  ( -1.000000000000000000, 1.789409696614061553E-15, 0.000000000000000000 ) ) ;
#9498=CARTESIAN_POINT ( 'NONE',  ( 78.14662766244079251, 60.27555255246366528, -2.661196496289815805 ) ) ;
#9504=CARTESIAN_POINT ( 'NONE',  ( 81.24750358194775401, 61.36520210808431841, -1.450104216466346907 ) ) ;
#9505=CARTESIAN_POINT ( 'NONE',  ( 77.99575034756946934, 63.53025565730434465, 3.710351296122897491 ) ) ;
#9510=CARTESIAN_POINT ( 'NONE',  ( 79.87389178145707547, 66.27500989097907791, 1.700667878122441801 ) ) ;
#9517=CARTESIAN_POINT ( 'NONE',  ( -64.58420500176730172, 36.29544061437457003, 5.991211914497711177 ) ) ;
#9527=CARTESIAN_POINT ( 'NONE',  ( -63.03213158086148837, 38.26878225442760595, -4.032857076800603124 ) ) ;
#9533=VECTOR ( 'NONE', #692, 1000.000000000000000 ) ;
#9537=CARTESIAN_POINT ( 'NONE',  ( 68.77554901931263487, 58.16923054873410592, -3.957896739784567686 ) ) ;
#9551=VERTEX_POINT ( 'NONE', #20662 ) ;
#9552=CARTESIAN_POINT ( 'NONE',  ( 80.39617744327613025, 62.02891139109912189, -3.151254463355007918 ) ) ;
#9555=CARTESIAN_POINT ( 'NONE',  ( 79.06287735990343890, 66.15384612320052327, -1.644402879615785684 ) ) ;
#9556=CARTESIAN_POINT ( 'NONE',  ( 79.42292528565204179, 64.10449580132842584, 3.686141857899477348 ) ) ;
#9575=DIRECTION ( 'NONE',  ( 0.000000000000000000, 0.000000000000000000, 1.000000000000000000 ) ) ;
#9580=CARTESIAN_POINT ( 'NONE',  ( -59.87552183813129147, 24.84364830758654108, -9.681005660250225020 ) ) ;
#9587=CARTESIAN_POINT ( 'NONE',  ( 67.51854282697247811, 57.96351248157043301, 3.990882853436548139 ) ) ;
#9603=CARTESIAN_POINT ( 'NONE',  ( 80.97051285240276286, 61.23143294393121039, -1.429680343939067955 ) ) ;
#9604=CARTESIAN_POINT ( 'NONE',  ( 80.61389980387333765, 62.62535450461751907, 3.411701596789205926 ) ) ;
#9615=EDGE_LOOP ( 'NONE', ( #21517, #27075, #5568, #1859 ) ) ;
#9617=CARTESIAN_POINT ( 'NONE',  ( -65.33937732661031816, 36.44481994370828914, 7.201454646438380180 ) ) ;
#9621=CARTESIAN_POINT ( 'NONE',  ( 79.27186652256901311, 65.93364065454110801, 2.332991218130493039 ) ) ;
#9623=CARTESIAN_POINT ( 'NONE',  ( -58.99872204295123623, 28.48507918597134037, -46.17089178453873188 ) ) ;
#9625=CARTESIAN_POINT ( 'NONE',  ( -64.09291719262364495, 35.65918410775120861, -4.099820839135469797 ) ) ;
#9633=DIRECTION ( 'NONE',  ( -1.000000000000000000, 0.000000000000000000, 0.000000000000000000 ) ) ;
#9640=CARTESIAN_POINT ( 'NONE',  ( 81.17453961776598703, 62.25628865055540473, -2.899379378185768630 ) ) ;
#9650=CARTESIAN_POINT ( 'NONE',  ( 79.44161963160777873, 65.18980684700308359, -3.197674131580387602 ) ) ;
#9658=CARTESIAN_POINT ( 'NONE',  ( 81.73829655978374831, 61.84901640042586024, -1.708467252431210115 ) ) ;
#9663=CARTESIAN_POINT ( 'NONE',  ( -63.16166472087058992, 41.43483297117672493, -4.000000000000000000 ) ) ;
#9664=CARTESIAN_POINT ( 'NONE',  ( 71.58333764992288195, 61.16654152266917066, 3.647993048544889039 ) ) ;
#9673=CARTESIAN_POINT ( 'NONE',  ( 81.67965074903510470, 61.82017115420521947, 1.781440269582215352 ) ) ;
#9698=CARTESIAN_POINT ( 'NONE',  ( 66.41209187282781556, 57.81891248311885079, -4.000000000000025757 ) ) ;
#9700=FACE_OUTER_BOUND ( 'NONE', #34394, .T. ) ;
#9705=EDGE_LOOP ( 'NONE', ( #32622, #12517, #34614, #1947, #3725, #5973 ) ) ;
#9707=CARTESIAN_POINT ( 'NONE',  ( 82.50731566719292687, 63.18365725368101238, -1.509105202935689283 ) ) ;
#9708=CARTESIAN_POINT ( 'NONE',  ( 80.72314371186318738, 62.66258842508748472, 3.386558198656121732 ) ) ;
#9711=CARTESIAN_POINT ( 'NONE',  ( 77.19967638839698054, 62.30393748795767550, -3.856837490695292026 ) ) ;
#9715=CARTESIAN_POINT ( 'NONE',  ( 79.29849762269610380, 65.95036606079992225, -2.316472630215912876 ) ) ;
#9716=CARTESIAN_POINT ( 'NONE',  ( 79.26824131213427904, 60.90178692369119062, 2.725046208697147421 ) ) ;
#9720=CARTESIAN_POINT ( 'NONE',  ( -9.741734729663692249, 54.65020406074287251, 1.000000000000000000 ) ) ;
#9722=CARTESIAN_POINT ( 'NONE',  ( 81.16905975791091521, 61.30379048835199995, 1.022614849746394938 ) ) ;
#9736=CARTESIAN_POINT ( 'NONE',  ( 78.20266744111994228, 60.29550935153869062, -2.640515453965961878 ) ) ;
#9748=CARTESIAN_POINT ( 'NONE',  ( 68.75960254727382903, 58.21139355255508008, -3.964410623304020387 ) ) ;
#9759=CARTESIAN_POINT ( 'NONE',  ( 81.13325097526887930, 61.29068799862990602, 1.183438861787475593 ) ) ;
#9763=CARTESIAN_POINT ( 'NONE',  ( 78.24936850314311698, 65.65315377296109034, -2.033355767895869359 ) ) ;
#9766=CARTESIAN_POINT ( 'NONE',  ( 81.58578928044234146, 61.77466459011638733, -1.878604182848718995 ) ) ;
#9767=CARTESIAN_POINT ( 'NONE',  ( 80.58155366896997407, 61.83530676836470974, 2.934133054905258664 ) ) ;
#9769=CARTESIAN_POINT ( 'NONE',  ( -64.08758708074093136, 43.19434570074267299, 2.104943985153647112 ) ) ;
#9794=CARTESIAN_POINT ( 'NONE',  ( 66.70577848186255210, 57.91700714588437648, 3.999628797553630655 ) ) ;
#9808=VERTEX_POINT ( 'NONE', #8710 ) ;
#9809=CARTESIAN_POINT ( 'NONE',  ( 79.35276748299774852, 64.76637986602874264, -3.438247877890630910 ) ) ;
#9811=CARTESIAN_POINT ( 'NONE',  ( 79.14833415808527661, 65.26800409942002545, 3.041370705153016996 ) ) ;
#9830=CARTESIAN_POINT ( 'NONE',  ( 80.40747942978342166, 64.69963996956802532, 3.448515284080270860 ) ) ;
#9838=CARTESIAN_POINT ( 'NONE',  ( -65.15514661499977933, 34.97220226750606997, 6.888442104241538466 ) ) ;
#9841=DIRECTION ( 'NONE',  ( 0.000000000000000000, 0.000000000000000000, 1.000000000000000000 ) ) ;
#9847=CARTESIAN_POINT ( 'NONE',  ( 78.88492378528530935, 66.04028779424463380, -1.804401104814771895 ) ) ;
#9856=ORIENTED_EDGE ( 'NONE', *, *, #29979, .T. ) ;
#9857=CARTESIAN_POINT ( 'NONE',  ( 80.78100857081943786, 62.68361397997274054, -3.372125408468112262 ) ) ;
#9865=CARTESIAN_POINT ( 'NONE',  ( 81.39510468133835275, 61.43011602722283016, -1.270639542487658424 ) ) ;
#9868=CARTESIAN_POINT ( 'NONE',  ( -58.98347169605253981, 28.20694469989773623, -6.383988387381219987 ) ) ;
#9870=DIRECTION ( 'NONE',  ( 0.9267318687906771491, -0.3757233601570964532, 0.000000000000000000 ) ) ;
#9871=CARTESIAN_POINT ( 'NONE',  ( 72.57946960881442067, 58.78899945845352448, 3.647993048395011151 ) ) ;
#9880=CARTESIAN_POINT ( 'NONE',  ( 80.97210443043506700, 64.61276409569624946, 3.292658836682931245 ) ) ;
#9889=ORIENTED_EDGE ( 'NONE', *, *, #26551, .F. ) ;
#9897=CARTESIAN_POINT ( 'NONE',  ( 66.43385761674679202, 57.75742247880091185, -4.000000000000006217 ) ) ;
#9910=CARTESIAN_POINT ( 'NONE',  ( 82.50386574309229104, 63.87755912629609867, -1.586031901070164674 ) ) ;
#9911=CARTESIAN_POINT ( 'NONE',  ( 81.10500554505499338, 61.42844135377578141, 1.938154327158146062 ) ) ;
#9914=CARTESIAN_POINT ( 'NONE',  ( 75.20156067606269801, 62.14723293136128746, -3.810661578667819516 ) ) ;
#9915=CARTESIAN_POINT ( 'NONE',  ( 28.61591789821288145, 47.14532032487838364, 4.000000000000000000 ) ) ;
#9918=CARTESIAN_POINT ( 'NONE',  ( 78.95529765307294667, 66.08830754916624528, -1.741375869723587710 ) ) ;
#9919=CARTESIAN_POINT ( 'NONE',  ( 76.23342353645796265, 61.41352271612323932, 3.867068906741275569 ) ) ;
#9923=CARTESIAN_POINT ( 'NONE',  ( -58.55427315445740533, 30.31497649546018991, 5.142179345755665487 ) ) ;
#9924=CARTESIAN_POINT ( 'NONE',  ( 82.02451737050283498, 62.15044802891524967, 1.700667878122440468 ) ) ;
#9932=DIRECTION ( 'NONE',  ( 0.000000000000000000, 0.000000000000000000, 1.000000000000000000 ) ) ;
#9933=CARTESIAN_POINT ( 'NONE',  ( 67.59777080239751967, 57.90654639195260245, 3.983714026670993835 ) ) ;
#9944=CARTESIAN_POINT ( 'NONE',  ( -11.81496944966682960, -21.25669541281728669, -4.000000000000000000 ) ) ;
#9945=CARTESIAN_POINT ( 'NONE',  ( 68.43818535210665743, 59.05932329210152432, -3.950303728398549374 ) ) ;
#9952=CARTESIAN_POINT ( 'NONE',  ( -56.59682361629209879, 30.63869417066593925, 3.015094993620162978 ) ) ;
#9953=EDGE_CURVE ( 'NONE', #15453, #7222, #26989, .T. ) ;
#9954=VERTEX_POINT ( 'NONE', #1106 ) ;
#9958=CARTESIAN_POINT ( 'NONE',  ( 81.23333979799274118, 62.00977392264719157, 2.676159939830916379 ) ) ;
#9963=CARTESIAN_POINT ( 'NONE',  ( 78.90238306073098329, 63.15141027621823611, -3.791687334209852267 ) ) ;
#9966=CARTESIAN_POINT ( 'NONE',  ( 80.19843342643493145, 65.64991096650632585, -2.811330881955115490 ) ) ;
#9967=CARTESIAN_POINT ( 'NONE',  ( 80.57587054825803818, 61.08954103313657669, 1.748505333477117896 ) ) ;
#9969=FACE_OUTER_BOUND ( 'NONE', #8588, .T. ) ;
#9971=CARTESIAN_POINT ( 'NONE',  ( -63.37463611956035692, 42.57616119279575173, 3.693273243659103588 ) ) ;
#9973=DIRECTION ( 'NONE',  ( 0.000000000000000000, 0.000000000000000000, 1.000000000000000000 ) ) ;
#9993=CARTESIAN_POINT ( 'NONE',  ( 66.54830849220104483, 57.89461212714910943, 3.999444518117950764 ) ) ;
#10004=CARTESIAN_POINT ( 'NONE',  ( 79.82585920881969344, 63.98597419336228853, -3.710743084827439198 ) ) ;
#10006=CARTESIAN_POINT ( 'NONE',  ( 80.98019550867157079, 61.28820853408525693, 1.743126864185295055 ) ) ;
#10007=CARTESIAN_POINT ( 'NONE',  ( -9.741734729663692249, 54.65020406074287251, -1.000000000000000000 ) ) ;
#10015=CARTESIAN_POINT ( 'NONE',  ( -64.95171866297674512, 36.28765213650433452, -6.629387290673639299 ) ) ;
#10023=CARTESIAN_POINT ( 'NONE',  ( 80.31657930512768928, 64.64970693426512582, 3.487490852634252292 ) ) ;
#10036=CARTESIAN_POINT ( 'NONE',  ( 68.69556364554829031, 58.38064408996493171, 3.985059344218205180 ) ) ;
#10040=CARTESIAN_POINT ( 'NONE',  ( 71.66251436080506210, 60.98061884659114895, -3.745173303738185577 ) ) ;
#10044=CARTESIAN_POINT ( 'NONE',  ( 81.24801795318222730, 61.46771992710468169, -1.817988788077152584 ) ) ;
#10048=EDGE_LOOP ( 'NONE', ( #13065, #24431, #6724, #6013 ) ) ;
#10053=EDGE_CURVE ( 'NONE', #28074, #11880, #5519, .T. ) ;
#10054=CARTESIAN_POINT ( 'NONE',  ( 78.70126604931442671, 66.02149264047228883, -1.577285172236841726 ) ) ;
#10058=LINE ( 'NONE', #6588, #6194 ) ;
#10059=CARTESIAN_POINT ( 'NONE',  ( -58.88504699088242234, 28.60929463400939099, -6.101381014920331580 ) ) ;
#10062=CARTESIAN_POINT ( 'NONE',  ( 69.77571843317402056, 59.04509999696490041, 3.985452289341159915 ) ) ;
#10063=ORIENTED_EDGE ( 'NONE', *, *, #40113, .T. ) ;
#10072=CARTESIAN_POINT ( 'NONE',  ( 79.50049935621065345, 66.06919348781509882, 2.170472567306921174 ) ) ;
#10096=CARTESIAN_POINT ( 'NONE',  ( 66.54439450091902586, 57.90558988169555477, -3.999229419688612008 ) ) ;
#10102=CARTESIAN_POINT ( 'NONE',  ( 82.01097102582248510, 65.15803335478928204, -1.775718711110015224 ) ) ;
#10106=CARTESIAN_POINT ( 'NONE',  ( 74.93610893867889899, 61.23939191379614755, -3.912919437578919357 ) ) ;
#10107=CARTESIAN_POINT ( 'NONE',  ( -74.03402466285142225, 19.33157623370700762, 9.800414904976365804 ) ) ;
#10110=CARTESIAN_POINT ( 'NONE',  ( 76.54260510937180584, 60.74419326975372968, 3.642592851547784782 ) ) ;
#10115=CARTESIAN_POINT ( 'NONE',  ( 79.78161832376108009, 66.22496747522392013, 1.859759604986721548 ) ) ;
#10137=CARTESIAN_POINT ( 'NONE',  ( 67.74957807481123950, 58.23899230517488235, -3.997461085607396214 ) ) ;
#10151=CARTESIAN_POINT ( 'NONE',  ( 80.45813098276143194, 63.95641783144333203, 3.614389211669657875 ) ) ;
#10154=CARTESIAN_POINT ( 'NONE',  ( 78.47217392918747692, 65.00024052541876074, -3.055712048904924316 ) ) ;
#10157=CARTESIAN_POINT ( 'NONE',  ( 81.75671479976286093, 62.52433184976155189, -2.563845612518023565 ) ) ;
#10158=CARTESIAN_POINT ( 'NONE',  ( 78.58588809754505178, 64.79968573292298117, 3.228498513792966484 ) ) ;
#10159=EDGE_CURVE ( 'NONE', #21319, #31581, #7935, .T. ) ;
#10161=CARTESIAN_POINT ( 'NONE',  ( 82.43037228308448050, 64.59322875725442259, 1.165579324820864571 ) ) ;
#10162=DIRECTION ( 'NONE',  ( -1.000000000000000000, 0.000000000000000000, 0.000000000000000000 ) ) ;
#10192=CARTESIAN_POINT ( 'NONE',  ( 66.56787846382142959, 57.83972306852010803, 3.999917672784798039 ) ) ;
#10205=CARTESIAN_POINT ( 'NONE',  ( 79.40660192983035870, 64.44177602733365973, -3.564905221331804874 ) ) ;
#10207=CARTESIAN_POINT ( 'NONE',  ( 80.91969899470544192, 61.54505855127009539, 2.326060681237265726 ) ) ;
#10225=CARTESIAN_POINT ( 'NONE',  ( 81.32870865761989876, 61.49729006283357080, 1.754135932968025724 ) ) ;
#10227=CYLINDRICAL_SURFACE ( 'NONE', #1003, 0.9999999999999977796 ) ;
#10233=CARTESIAN_POINT ( 'NONE',  ( -64.94969296618708654, 34.86786693855311370, 6.612442482648480002 ) ) ;
#10236=DIRECTION ( 'NONE',  ( -1.000000000000000000, 0.000000000000000000, 0.000000000000000000 ) ) ;
#10239=CARTESIAN_POINT ( 'NONE',  ( 69.13527637438681950, 58.97494527044376866, 3.984982412582155575 ) ) ;
#10245=CARTESIAN_POINT ( 'NONE',  ( 80.65352406091058413, 63.67746643299658160, -3.602832836245130288 ) ) ;
#10253=CARTESIAN_POINT ( 'NONE',  ( 79.53095237740755863, 64.90064992126218613, -3.392181771880278696 ) ) ;
#10258=CARTESIAN_POINT ( 'NONE',  ( 79.16788024942138691, 66.21349342525118686, -1.524764441711168095 ) ) ;
#10261=CARTESIAN_POINT ( 'NONE',  ( -58.90847777598104784, 28.53357273443418762, -6.181373327462416967 ) ) ;
#10264=CARTESIAN_POINT ( 'NONE',  ( 69.65195751129601831, 59.35873293165669651, 3.965028736237012907 ) ) ;
#10275=CARTESIAN_POINT ( 'NONE',  ( 81.16506502659913735, 61.30232764367859488, 1.065084354002949762 ) ) ;
#10296=CARTESIAN_POINT ( 'NONE',  ( -62.99901854238117238, 37.98537211837078331, -4.070195263748868975 ) ) ;
#10303=CARTESIAN_POINT ( 'NONE',  ( -65.15514661499977933, 34.97220226750606997, 6.888442104241535802 ) ) ;
#10307=CARTESIAN_POINT ( 'NONE',  ( 80.61888529134419912, 66.16066543623874452, -1.646077502936216685 ) ) ;
#10310=CARTESIAN_POINT ( 'NONE',  ( 76.06955384389377173, 61.76325957217478191, -3.887901781368106491 ) ) ;
#10315=CARTESIAN_POINT ( 'NONE',  ( 77.14378789031550809, 60.95143994403615295, 3.590981437852719171 ) ) ;
#10317=ADVANCED_FACE ( 'NONE', ( #19368 ), #38088, .T. ) ;
#10322=CARTESIAN_POINT ( 'NONE',  ( 78.92300404249586165, 66.17133619070195039, 1.270639542487624896 ) ) ;
#10326=AXIS2_PLACEMENT_3D ( 'NONE', #11642, #36377, #8355 ) ;
#10328=AXIS2_PLACEMENT_3D ( 'NONE', #24607, #37163, #16744 ) ;
#10342=CARTESIAN_POINT ( 'NONE',  ( -63.05049812975219226, 38.43447230638341949, -4.010972415401406366 ) ) ;
#10343=B_SPLINE_CURVE_WITH_KNOTS ( 'NONE', 3,
 ( #10953, #10558, #13861, #1719, #35502, #29513, #33007, #35701, #23134, #26822, #20428, #1322, #1515, #20033 ),
 .UNSPECIFIED., .F., .F.,
 ( 4, 2, 2, 2, 2, 2, 4 ),
 ( 2.818925648462311528E-18, 0.0006285028710944130402, 0.001257005742188823261, 0.001885508613283233591, 0.002514011484377643921, 0.003771017226566485830, 0.005028022968755326873 ),
 .UNSPECIFIED. ) ;
#10348=CARTESIAN_POINT ( 'NONE',  ( 67.72966869545554403, 58.29280778740498192, -3.997461085607385556 ) ) ;
#10359=CARTESIAN_POINT ( 'NONE',  ( -55.16612787639756732, 31.23053227951973199, 1.484562114140385747 ) ) ;
#10363=CARTESIAN_POINT ( 'NONE',  ( 81.20826633916702519, 61.35171532218112134, 1.496866203714591892 ) ) ;
#10366=CARTESIAN_POINT ( 'NONE',  ( 77.82439497328331868, 65.16220298991649429, -2.551779361026667026 ) ) ;
#10370=CARTESIAN_POINT ( 'NONE',  ( 80.78189192732895663, 64.90162691772428616, -3.235508711551936756 ) ) ;
#10371=CARTESIAN_POINT ( 'NONE',  ( 77.95070745440513349, 65.53481705947537250, 1.908681007153592235 ) ) ;
#10372=EDGE_CURVE ( 'NONE', #12131, #15868, #23461, .T. ) ;
#10374=CARTESIAN_POINT ( 'NONE',  ( 82.18073233876091876, 62.22941084722771166, 1.168532795813725045 ) ) ;
#10375=CARTESIAN_POINT ( 'NONE',  ( 25.11437021580303863, 164.7550792202006562, 1.000000000000000000 ) ) ;
#10399=CARTESIAN_POINT ( 'NONE',  ( 66.54635149611212341, 57.90010100995254305, 3.999344142520906864 ) ) ;
#10409=ORIENTED_EDGE ( 'NONE', *, *, #24798, .T. ) ;
#10411=ORIENTED_EDGE ( 'NONE', *, *, #15379, .T. ) ;
#10412=CARTESIAN_POINT ( 'NONE',  ( 80.32689410753103232, 62.53373119284189130, -3.467090974304448459 ) ) ;
#10414=CARTESIAN_POINT ( 'NONE',  ( 78.94919473400565835, 65.41189549592698427, 2.864416008774272271 ) ) ;
#10424=CARTESIAN_POINT ( 'NONE',  ( 66.27376694608931018, 57.73522568913554665, -4.000000000000000000 ) ) ;
#10431=CARTESIAN_POINT ( 'NONE',  ( 81.39824655423383604, 62.07766870923516933, 2.596981798947347819 ) ) ;
#10440=CARTESIAN_POINT ( 'NONE',  ( -64.08758708074091714, 24.84364830758654108, 3.800414904976363140 ) ) ;
#10442=CARTESIAN_POINT ( 'NONE',  ( 81.18025391627377019, 61.34316975053406651, -1.531260274641951913 ) ) ;
#10444=DIRECTION ( 'NONE',  ( 0.000000000000000000, -0.1369933068947546406, 0.9905719730872863948 ) ) ;
#10452=CARTESIAN_POINT ( 'NONE',  ( 78.75977295323076532, 65.93644120262121078, -1.938154327158300827 ) ) ;
#10459=CARTESIAN_POINT ( 'NONE',  ( -63.08758708074093136, 43.61223004741322740, 4.000000000000000000 ) ) ;
#10465=CARTESIAN_POINT ( 'NONE',  ( 71.03485184658521234, 59.25305893485334963, 3.963404584535439312 ) ) ;
#10470=AXIS2_PLACEMENT_3D ( 'NONE', #32233, #7897, #23941 ) ;
#10474=CARTESIAN_POINT ( 'NONE',  ( 81.44087877708247447, 61.54565157041406565, 1.662073781717998022 ) ) ;
#10477=ORIENTED_EDGE ( 'NONE', *, *, #17912, .F. ) ;
#10493=CARTESIAN_POINT ( 'NONE',  ( 66.27376694609004915, 57.73522568913436004, -4.000000000000000000 ) ) ;
#10495=TOROIDAL_SURFACE ( 'NONE', #23011, 6.999999999999986677, 1.000000000000000000 ) ;
#10498=CARTESIAN_POINT ( 'NONE',  ( -77.95330471031414277, 33.71485196875532608, 8.800414904976364028 ) ) ;
#10501=FACE_OUTER_BOUND ( 'NONE', #6397, .T. ) ;
#10505=CARTESIAN_POINT ( 'NONE',  ( 78.69012442119819184, 66.05840891509440382, -1.017094602978585449 ) ) ;
#10508=EDGE_CURVE ( 'NONE', #23344, #6217, #21771, .T. ) ;
#10510=CARTESIAN_POINT ( 'NONE',  ( 75.72894860151858154, 61.00966332974834927, -3.846775394605490561 ) ) ;
#10511=DIRECTION ( 'NONE',  ( 0.8888117386314211554, 0.4582725098355677762, 0.000000000000000000 ) ) ;
#10514=CARTESIAN_POINT ( 'NONE',  ( 76.72366484839766088, 61.84716987400887689, 3.872369636032537699 ) ) ;
#10515=ORIENTED_EDGE ( 'NONE', *, *, #8161, .T. ) ;
#10520=CARTESIAN_POINT ( 'NONE',  ( 82.15586074033954844, 62.44414535927739962, 1.848245342697198756 ) ) ;
#10534=EDGE_CURVE ( 'NONE', #29043, #28218, #17801, .T. ) ;
#10541=CARTESIAN_POINT ( 'NONE',  ( 67.22540103859083160, 57.85622601175691671, -3.990981480864019826 ) ) ;
#10556=CARTESIAN_POINT ( 'NONE',  ( 81.28814307398172900, 61.80674180605062418, 2.393593008231199804 ) ) ;
#10558=CARTESIAN_POINT ( 'NONE',  ( -63.70768058868311812, 44.39675795731061214, 1.212206658320163166 ) ) ;
#10561=CARTESIAN_POINT ( 'NONE',  ( 79.99044059672593221, 61.67469478680249040, -3.091829831932956019 ) ) ;
#10562=( BOUNDED_SURFACE ( )  B_SPLINE_SURFACE ( 3, 2, ( 
 ( #19094, #3283, #11313 ),
 ( #36655, #40145, #21218 ),
 ( #20798, #37813, #23879 ),
 ( #5164, #8434, #2093 ),
 ( #37056, #9617, #21015 ),
 ( #33789, #36453, #24297 ) ),
 .UNSPECIFIED., .F., .F., .T. ) 
 B_SPLINE_SURFACE_WITH_KNOTS ( ( 4, 2, 4 ),
 ( 3, 3 ),
 ( 4.712388980384689674, 5.164939930480247909, 5.617490880575807033 ),
 ( 0.000000000000000000, 1.000000000000000000 ),
 .UNSPECIFIED. ) 
 GEOMETRIC_REPRESENTATION_ITEM ( )  RATIONAL_B_SPLINE_SURFACE ( (
 ( 1.000000000000000000, 0.7071067811865475727, 1.000000000000000000),
 ( 1.000000000000000000, 0.6870851634080177295, 1.000000000000000000),
 ( 1.000000000000000000, 0.6661308060340611625, 1.000000000000000000),
 ( 1.000000000000000000, 0.6267038978092043244, 1.000000000000000000),
 ( 1.000000000000000000, 0.6082500109239441510, 1.000000000000000000),
 ( 1.000000000000000000, 0.5935057080259639184, 1.000000000000000000) ) ) 
 REPRESENTATION_ITEM ( '' )  SURFACE ( )  );
#10565=CARTESIAN_POINT ( 'NONE',  ( 79.04416262434902762, 66.14279969385735569, -1.662073781712726017 ) ) ;
#10566=CARTESIAN_POINT ( 'NONE',  ( 79.22522514097650514, 63.97890519848278501, 3.707164540951486398 ) ) ;
#10569=CARTESIAN_POINT ( 'NONE',  ( 79.33847868486732580, 66.30689617902915245, 1.090531591958330937 ) ) ;
#10573=FACE_OUTER_BOUND ( 'NONE', #11911, .T. ) ;
#10591=CARTESIAN_POINT ( 'NONE',  ( 66.69694663263604184, 57.94160696200565042, 3.999246569073970026 ) ) ;
#10601=VERTEX_POINT ( 'NONE', #40455 ) ;
#10604=CARTESIAN_POINT ( 'NONE',  ( 78.87241222613832292, 65.34207468649371719, -2.902290250791178305 ) ) ;
#10607=CARTESIAN_POINT ( 'NONE',  ( 80.51397140397814667, 62.59311809350369060, 3.432573985763616164 ) ) ;
#10614=CARTESIAN_POINT ( 'NONE',  ( 78.42694857803141417, 65.87163300571076263, -1.555883980134156186 ) ) ;
#10617=FACE_OUTER_BOUND ( 'NONE', #11928, .T. ) ;
#10618=CIRCLE ( 'NONE', #40222, 6.329987104167475565 ) ;
#10622=CARTESIAN_POINT ( 'NONE',  ( 81.23980251882781545, 61.36242252098747940, 1.459100623883065717 ) ) ;
#10635=CARTESIAN_POINT ( 'NONE',  ( 68.61500287773905882, 58.59333675578601230, 3.993768376023893563 ) ) ;
#10638=CARTESIAN_POINT ( 'NONE',  ( -64.08758708074093136, 42.98405160571059014, -2.320550953111519377 ) ) ;
#10640=CARTESIAN_POINT ( 'NONE',  ( 79.89688848262225918, 64.77169266163328132, -3.452358620554651036 ) ) ;
#10643=CARTESIAN_POINT ( 'NONE',  ( -57.73493806181992483, 28.75062263012322106, 2.538950603207606349 ) ) ;
#10649=ORIENTED_EDGE ( 'NONE', *, *, #22930, .F. ) ;
#10650=CARTESIAN_POINT ( 'NONE',  ( 80.39951605126471179, 63.19197404919984962, -3.632888195267880427 ) ) ;
#10652=CARTESIAN_POINT ( 'NONE',  ( 80.65725571609037559, 62.96675706018874052, 3.489836119548948901 ) ) ;
#10654=AXIS2_PLACEMENT_3D ( 'NONE', #2525, #15050, #12375 ) ;
#10657=CARTESIAN_POINT ( 'NONE',  ( -58.83360130232286878, 28.75651630857863950, -5.941118172103339035 ) ) ;
#10660=CARTESIAN_POINT ( 'NONE',  ( -64.08758708074093136, 42.86724024435063285, -2.417504070309356212 ) ) ;
#10670=CARTESIAN_POINT ( 'NONE',  ( 81.69067057340667759, 62.21317191937867364, 2.410848004515911303 ) ) ;
#10674=EDGE_LOOP ( 'NONE', ( #5107, #10895, #7681, #37030 ) ) ;
#10686=DIRECTION ( 'NONE',  ( 0.9637806624122927657, -0.2666961468790326473, 0.000000000000000000 ) ) ;
#10689=ORIENTED_EDGE ( 'NONE', *, *, #6051, .F. ) ;
#10698=CARTESIAN_POINT ( 'NONE',  ( -58.56870219631065311, 27.89510117891458663, -3.538387446898162647 ) ) ;
#10702=CARTESIAN_POINT ( 'NONE',  ( 79.92383974732979368, 66.30194418458911798, -1.599335268229509888 ) ) ;
#10708=CARTESIAN_POINT ( 'NONE',  ( 75.46848212330048966, 60.05767933327602037, 3.584990529380366997 ) ) ;
#10716=CARTESIAN_POINT ( 'NONE',  ( 80.64500926360319966, 65.89167229754917798, 2.340562087103263966 ) ) ;
#10732=EDGE_CURVE ( 'NONE', #30327, #38236, #30313, .T. ) ;
#10737=CARTESIAN_POINT ( 'NONE',  ( 67.54222599743037847, 57.89884484782556484, -3.985038673850038737 ) ) ;
#10749=CARTESIAN_POINT ( 'NONE',  ( 81.19396390929411211, 61.77420168221061658, 2.442092683901115446 ) ) ;
#10754=CARTESIAN_POINT ( 'NONE',  ( 78.36941018910007983, 65.17477963226572513, -2.845586111146954700 ) ) ;
#10756=CARTESIAN_POINT ( 'NONE',  ( 80.57438652552279734, 65.15318659310567284, -3.125353918834855360 ) ) ;
#10758=CARTESIAN_POINT ( 'NONE',  ( 78.24936850314311698, 65.65315377296109034, 2.033355767895868915 ) ) ;
#10761=B_SPLINE_CURVE_WITH_KNOTS ( 'NONE', 3,
 ( #40330, #14597, #18303, #39518 ),
 .UNSPECIFIED., .F., .F.,
 ( 4, 4 ),
 ( 0.000000000000000000, 0.0008960438496711642777 ),
 .UNSPECIFIED. ) ;
#10762=AXIS2_PLACEMENT_3D ( 'NONE', #10107, #25568, #10511 ) ;
#10763=CARTESIAN_POINT ( 'NONE',  ( 82.34614708994683951, 62.54074552962158862, 1.204231967107850076 ) ) ;
#10767=CARTESIAN_POINT ( 'NONE',  ( -64.38387608637881954, 34.70929407487278695, -5.501206404649174431 ) ) ;
#10786=CARTESIAN_POINT ( 'NONE',  ( 66.41209187282773030, 57.81891248311896447, 4.000000000000023093 ) ) ;
#10787=CARTESIAN_POINT ( 'NONE',  ( 71.74426859761079811, 60.78783288850195987, -3.823636340558493885 ) ) ;
#10788=AXIS2_PLACEMENT_3D ( 'NONE', #18796, #3194, #28682 ) ;
#10799=CARTESIAN_POINT ( 'NONE',  ( 80.37564778476929916, 62.54931541869399325, -3.458772244351171476 ) ) ;
#10800=CARTESIAN_POINT ( 'NONE',  ( -56.59682361629209879, 30.63869417066593925, 3.015094993620162978 ) ) ;
#10801=CARTESIAN_POINT ( 'NONE',  ( 80.89520131247735435, 61.53942361443156983, 2.340042473998425354 ) ) ;
#10808=DIRECTION ( 'NONE',  ( 0.4690749385695657803, 0.8831583674551003460, 0.000000000000000000 ) ) ;
#10809=DIRECTION ( 'NONE',  ( -0.8831583674551141128, 0.4690749385695399676, 0.000000000000000000 ) ) ;
#10812=DIRECTION ( 'NONE',  ( 0.3757233601570978965, 0.9267318687906764829, 0.000000000000000000 ) ) ;
#10821=CARTESIAN_POINT ( 'NONE',  ( 81.21493646480149664, 62.54560775605910550, 3.083955809406639048 ) ) ;
#10832=CARTESIAN_POINT ( 'NONE',  ( 69.43824574602471955, 58.18893279706789201, 3.907754234428237439 ) ) ;
#10839=CARTESIAN_POINT ( 'NONE',  ( 80.61377670644299087, 63.65766204751285784, -3.614389211669656987 ) ) ;
#10841=CIRCLE ( 'NONE', #36483, 6.681288188914807691 ) ;
#10843=CARTESIAN_POINT ( 'NONE',  ( -58.83253814471410692, 27.61819298006738421, 3.984408728655188803 ) ) ;
#10844=EDGE_LOOP ( 'NONE', ( #32749, #27822, #23135, #11352, #34022, #2626 ) ) ;
#10849=CARTESIAN_POINT ( 'NONE',  ( 78.66262733798787110, 65.98865143197190264, -1.634613895560575125 ) ) ;
#10851=CARTESIAN_POINT ( 'NONE',  ( 78.75977295323087901, 65.93644120262132446, 1.938154327158139845 ) ) ;
#10855=CARTESIAN_POINT ( 'NONE',  ( -56.59682361629209879, 30.63869417066593925, -3.015094993620159425 ) ) ;
#10871=CARTESIAN_POINT ( 'NONE',  ( 79.82819440665414845, 65.73008711143909011, 2.710336141772892393 ) ) ;
#10879=CARTESIAN_POINT ( 'NONE',  ( -63.03213158086253287, 38.26878225442504800, 4.032857076801014351 ) ) ;
#10884=VERTEX_POINT ( 'NONE', #8893 ) ;
#10886=CARTESIAN_POINT ( 'NONE',  ( -68.98442902999595105, 21.93515443114010210, 8.800414904976364028 ) ) ;
#10892=CARTESIAN_POINT ( 'NONE',  ( -62.96427906878926706, 37.71115934644217305, -4.137654479798320573 ) ) ;
#10893=CARTESIAN_POINT ( 'NONE',  ( -75.45330471031414277, 33.71485196875532608, -46.17089178453873188 ) ) ;
#10895=ORIENTED_EDGE ( 'NONE', *, *, #10534, .F. ) ;
#10903=EDGE_CURVE ( 'NONE', #15032, #21175, #15423, .T. ) ;
#10906=CARTESIAN_POINT ( 'NONE',  ( 82.47197227462035585, 63.49890707693131731, -1.793694987646316186 ) ) ;
#10913=CARTESIAN_POINT ( 'NONE',  ( 75.14412900705532650, 60.78131343986104440, 3.865308561588337799 ) ) ;
#10922=CARTESIAN_POINT ( 'NONE',  ( 81.60288604192470530, 64.55353989381950441, 2.864610283900509202 ) ) ;
#10932=CARTESIAN_POINT ( 'NONE',  ( -55.15112219448760555, 31.23515184556838165, -9.800414904976365804 ) ) ;
#10934=AXIS2_PLACEMENT_3D ( 'NONE', #30993, #27074, #21308 ) ;
#10940=CARTESIAN_POINT ( 'NONE',  ( 67.50273067437429120, 58.00668225682344570, -3.993945454764282310 ) ) ;
#10951=CARTESIAN_POINT ( 'NONE',  ( 81.16957891225081312, 61.30398062001320625, -1.000000000000000000 ) ) ;
#10952=CARTESIAN_POINT ( 'NONE',  ( 80.65823571794965119, 63.30623879605499837, 3.578839808218917895 ) ) ;
#10953=CARTESIAN_POINT ( 'NONE',  ( -63.70768058868311812, 44.39675795731059793, 1.000000000000000000 ) ) ;
#10955=CARTESIAN_POINT ( 'NONE',  ( 78.43336062804344522, 61.18469638573554903, -3.363831406679923752 ) ) ;
#10959=CARTESIAN_POINT ( 'NONE',  ( 80.30538902758895858, 65.37113732874213667, -3.059106349689739712 ) ) ;
#10960=CARTESIAN_POINT ( 'NONE',  ( 79.19917379928831735, 63.30335940139927686, 3.774260586041106258 ) ) ;
#10962=AXIS2_PLACEMENT_3D ( 'NONE', #27346, #11887, #9013 ) ;
#10966=CARTESIAN_POINT ( 'NONE',  ( 81.62248346935344046, 65.70993096190733240, 1.153249692834613427 ) ) ;
#10967=DIRECTION ( 'NONE',  ( 0.000000000000000000, -1.000000000000000000, 0.000000000000000000 ) ) ;
#10971=CARTESIAN_POINT ( 'NONE',  ( -66.99872204295122913, 28.48507918597134037, -12.49999999999999645 ) ) ;
#10978=CARTESIAN_POINT ( 'NONE',  ( -9.439742135462632078, 51.66544268451064426, -1.000000000000000000 ) ) ;
#10986=CARTESIAN_POINT ( 'NONE',  ( 66.57570644833764106, 57.81776741001107922, 3.999845987728086083 ) ) ;
#10987=CARTESIAN_POINT ( 'NONE',  ( 73.13464764220530867, 62.20839851451114555, -3.391332960900173887 ) ) ;
#10997=CARTESIAN_POINT ( 'NONE',  ( 80.83613523452670790, 61.24682340193510299, -1.855758959884428849 ) ) ;
#10999=CARTESIAN_POINT ( 'NONE',  ( 80.20116317610164458, 62.79640268260013158, 3.571698303486883663 ) ) ;
#11008=CARTESIAN_POINT ( 'NONE',  ( -77.95330471031414277, 33.71485196875532608, -46.17089178453873188 ) ) ;
#11016=CARTESIAN_POINT ( 'NONE',  ( 80.84084779726516956, 63.39242392479003740, 3.526329879082121810 ) ) ;
#11018=B_SPLINE_CURVE_WITH_KNOTS ( 'NONE', 3,
 ( #35096, #35692, #3804, #13440, #16323, #28897 ),
 .UNSPECIFIED., .F., .F.,
 ( 4, 2, 4 ),
 ( 4.336808689942017736E-19, 0.001078930742623167250, 0.002157861485246334067 ),
 .UNSPECIFIED. ) ;
#11021=LINE ( 'NONE', #11830, #1730 ) ;
#11022=CARTESIAN_POINT ( 'NONE',  ( -64.41607093812410767, 34.69667448355765771, 5.588514499911548583 ) ) ;
#11025=( BOUNDED_SURFACE ( )  B_SPLINE_SURFACE ( 3, 2, ( 
 ( #4548, #23083, #4739 ),
 ( #38500, #11097, #29456 ),
 ( #1069, #35450, #33154 ),
 ( #13994, #7821, #7223 ),
 ( #17270, #13600, #26567 ),
 ( #32555, #1871, #20568 ),
 ( #4939, #23477, #7622 ),
 ( #26171, #29650, #23668 ),
 ( #29852, #38705, #19784 ),
 ( #36234, #20176, #8012 ),
 ( #35647, #38906, #7417 ),
 ( #19975, #4354, #1266 ),
 ( #10698, #30259, #21611 ),
 ( #30681, #23857, #27162 ),
 ( #33570, #39717, #2490 ),
 ( #18090, #2697, #30885 ),
 ( #12113, #34192, #8621 ),
 ( #30467, #9034, #5957 ),
 ( #18502, #15012, #2078 ),
 ( #27367, #31086, #5349 ),
 ( #2896, #15215, #21409 ),
 ( #37037, #26965, #24692 ) ),
 .UNSPECIFIED., .F., .F., .T. ) 
 B_SPLINE_SURFACE_WITH_KNOTS ( ( 4, 2, 2, 2, 2, 2, 2, 2, 2, 2, 4 ),
 ( 3, 3 ),
 ( 0.02037793668903936650, 0.02161998616042463614, 0.02224101089611726922, 0.02286203563180990578, 0.02410408510319517195, 0.02534613457458044158, 0.02658818404596571122, 0.02720920878165834431, 0.02783023351735097739, 0.02907228298873624703, 0.03031433246012151667 ),
 ( 0.1026333575651713903, 1.000000000000000000 ),
 .UNSPECIFIED. ) 
 GEOMETRIC_REPRESENTATION_ITEM ( )  RATIONAL_B_SPLINE_SURFACE ( (
 ( 0.9460492146741656949, 0.7371673956414426243, 1.000000000000000000),
 ( 0.9472507007640582621, 0.7430206879744423176, 1.000000000000000000),
 ( 0.9486044478916659806, 0.7496157519951633930, 1.000000000000000000),
 ( 0.9508882531966607043, 0.7607417901526136728, 1.000000000000000000),
 ( 0.9516917417591811423, 0.7646561537746467963, 1.000000000000000000),
 ( 0.9533874343465102985, 0.7729170770629283371, 1.000000000000000000),
 ( 0.9542843507619054311, 0.7772865941316136063, 1.000000000000000000),
 ( 0.9570723184632317082, 0.7908687655009754014, 1.000000000000000000),
 ( 0.9590598677958013241, 0.8005515303433297092, 1.000000000000000000),
 ( 0.9632568686825866422, 0.8209981033988795751, 1.000000000000000000),
 ( 0.9654881076387393790, 0.8318680535256492981, 1.000000000000000000),
 ( 0.9699646227543765598, 0.8536763389692718640, 1.000000000000000000),
 ( 0.9722104709448077253, 0.8646174610552612716, 1.000000000000000000),
 ( 0.9754590750861481530, 0.8804437197805374815, 1.000000000000000000),
 ( 0.9765212693044509340, 0.8856184224478864664, 1.000000000000000000),
 ( 0.9785718366633011644, 0.8956081928670607262, 1.000000000000000000),
 ( 0.9795574793614638676, 0.9004099586942033717, 1.000000000000000000),
 ( 0.9822852879408858762, 0.9136990522410552984, 1.000000000000000000),
 ( 0.9838235476076093722, 0.9211930079257193427, 1.000000000000000000),
 ( 0.9859690325004739631, 0.9316451890867138985, 1.000000000000000000),
 ( 0.9865248671184559948, 0.9343530544005280714, 1.000000000000000000),
 ( 0.9864639028331373405, 0.9340560540550024715, 1.000000000000000000) ) ) 
 REPRESENTATION_ITEM ( '' )  SURFACE ( )  );
#11026=CARTESIAN_POINT ( 'NONE',  ( 67.71971274774827521, 58.31971506597766819, 3.997018227265501267 ) ) ;
#11029=AXIS2_PLACEMENT_3D ( 'NONE', #6351, #3488, #3085 ) ;
#11032=CARTESIAN_POINT ( 'NONE',  ( 81.21317738564107458, 61.78038839029203189, -2.432199249741020086 ) ) ;
#11036=CARTESIAN_POINT ( 'NONE',  ( -59.00289461565213855, 28.67396232720155780, 6.820567581290490899 ) ) ;
#11037=ORIENTED_EDGE ( 'NONE', *, *, #4786, .F. ) ;
#11040=AXIS2_PLACEMENT_3D ( 'NONE', #1957, #2570, #5429 ) ;
#11046=CARTESIAN_POINT ( 'NONE',  ( 79.39546522070064327, 65.15502244391674935, -3.213872034465286021 ) ) ;
#11048=CARTESIAN_POINT ( 'NONE',  ( 80.39050082614866710, 63.54812927569808778, 3.668443954219270164 ) ) ;
#11067=CARTESIAN_POINT ( 'NONE',  ( 80.21610222778484456, 65.32174013293413850, 3.113722587674275566 ) ) ;
#11070=EDGE_LOOP ( 'NONE', ( #13892, #3584, #26340, #37811 ) ) ;
#11090=CARTESIAN_POINT ( 'NONE',  ( -62.85318495816863305, 36.92099889189292838, -4.451173097142522295 ) ) ;
#11097=CARTESIAN_POINT ( 'NONE',  ( -55.57018072619552385, 31.35870463729781576, -3.952748674019516795 ) ) ;
#11102=CARTESIAN_POINT ( 'NONE',  ( 81.84349429120946695, 61.90138267109050929, -1.539394129974354763 ) ) ;
#11104=AXIS2_PLACEMENT_3D ( 'NONE', #36662, #30093, #11324 ) ;
#11110=CARTESIAN_POINT ( 'NONE',  ( 74.21382537490346465, 62.79450482958245772, 3.300071129360917066 ) ) ;
#11120=CARTESIAN_POINT ( 'NONE',  ( 81.39510468133838117, 61.43011602722285147, 1.270639542487624007 ) ) ;
#11125=EDGE_CURVE ( 'NONE', #26757, #29749, #32875, .T. ) ;
#11131=EDGE_CURVE ( 'NONE', #31247, #9551, #23398, .T. ) ;
#11138=CARTESIAN_POINT ( 'NONE',  ( 67.06207392303235792, 57.84849753947618467, -3.994852852620101480 ) ) ;
#11145=CARTESIAN_POINT ( 'NONE',  ( 78.31613663886943755, 65.79311636994390255, 1.652891522390884216 ) ) ;
#11152=CARTESIAN_POINT ( 'NONE',  ( 79.70553327529583498, 65.02082924290297683, 3.340002271463677896 ) ) ;
#11154=VERTEX_POINT ( 'NONE', #29377 ) ;
#11155=CARTESIAN_POINT ( 'NONE',  ( 78.10617727715711567, 63.31486359019600485, -3.780406938340842515 ) ) ;
#11158=CARTESIAN_POINT ( 'NONE',  ( 79.69124582247823696, 65.94093779614992457, -2.443770662193227139 ) ) ;
#11159=CARTESIAN_POINT ( 'NONE',  ( 79.25863321418395913, 62.43675908411266562, 3.670385203786648010 ) ) ;
#11163=CARTESIAN_POINT ( 'NONE',  ( 82.33210628740353343, 64.54215504103274270, 1.775718711109096404 ) ) ;
#11170=CARTESIAN_POINT ( 'NONE',  ( 17.97454669799173033, 51.66243977840390755, 4.000000000000000000 ) ) ;
#11171=CARTESIAN_POINT ( 'NONE',  ( -62.86576508122317364, 38.67912974266874926, 4.000000000000000000 ) ) ;
#11185=CARTESIAN_POINT ( 'NONE',  ( 73.17398396214588274, 60.59975200455691891, -3.944160774623525434 ) ) ;
#11202=CARTESIAN_POINT ( 'NONE',  ( 79.01107290893718016, 64.84207397985339583, -3.331801170923394562 ) ) ;
#11204=CARTESIAN_POINT ( 'NONE',  ( 80.24765655772201001, 65.96146312294936820, -2.334361474589122576 ) ) ;
#11205=CARTESIAN_POINT ( 'NONE',  ( 78.75925357433533236, 65.51276736450270732, 2.660933152496150811 ) ) ;
#11212=VECTOR ( 'NONE', #25955, 1000.000000000000000 ) ;
#11217=CARTESIAN_POINT ( 'NONE',  ( 78.88492378528533777, 66.04028779424464801, 1.804401104814770784 ) ) ;
#11228=CARTESIAN_POINT ( 'NONE',  ( 67.43143073044585378, 58.20127550988744503, 3.998123450764769604 ) ) ;
#11234=CARTESIAN_POINT ( 'NONE',  ( 80.80454364895454944, 63.02910633771584514, -3.452358620554643487 ) ) ;
#11243=CARTESIAN_POINT ( 'NONE',  ( 79.33915194569547680, 65.11111034845936274, -3.233326467035622098 ) ) ;
#11244=CARTESIAN_POINT ( 'NONE',  ( -60.81661347076553881, 25.20155461598434954, -8.800414904976364028 ) ) ;
#11245=CARTESIAN_POINT ( 'NONE',  ( 81.07324312733541660, 61.26878263851436657, 1.298998371267757745 ) ) ;
#11249=CARTESIAN_POINT ( 'NONE',  ( 75.87451422959399849, 60.69085731309660758, -3.756674307851894490 ) ) ;
#11264=CARTESIAN_POINT ( 'NONE',  ( 78.99802787997056441, 66.11506539533188231, 1.704083397384887233 ) ) ;
#11267=DIRECTION ( 'NONE',  ( -1.000000000000000000, 0.000000000000000000, 0.000000000000000000 ) ) ;
#11289=DIRECTION ( 'NONE',  ( -0.000000000000000000, -1.000000000000000000, 0.000000000000000000 ) ) ;
#11291=ORIENTED_EDGE ( 'NONE', *, *, #3623, .T. ) ;
#11298=CARTESIAN_POINT ( 'NONE',  ( 82.09872185058162586, 62.41535711090991612, -1.944145319385669923 ) ) ;
#11305=CARTESIAN_POINT ( 'NONE',  ( 74.04982613775094080, 61.68561850464361385, 3.815996826674513009 ) ) ;
#11310=CARTESIAN_POINT ( 'NONE',  ( -55.16612787639762416, 31.23053227951969646, -1.484562114140327793 ) ) ;
#11313=CARTESIAN_POINT ( 'NONE',  ( -69.08758708074093136, 36.88538962427717394, 8.800414904976364028 ) ) ;
#11314=CARTESIAN_POINT ( 'NONE',  ( 81.16673370561990453, 65.10603640127602887, 2.903340743335354190 ) ) ;
#11320=CIRCLE ( 'NONE', #6770, 1.000000000000000666 ) ;
#11324=DIRECTION ( 'NONE',  ( 1.000000000000000000, 0.000000000000000000, 0.000000000000000000 ) ) ;
#11335=CARTESIAN_POINT ( 'NONE',  ( 67.17808119270118539, 57.98628055940345405, -3.998197261021421589 ) ) ;
#11348=CARTESIAN_POINT ( 'NONE',  ( 80.71704827558885142, 66.21292280724347279, -1.118100487915077546 ) ) ;
#11350=CARTESIAN_POINT ( 'NONE',  ( 81.12869333199854793, 61.28902183752150279, 1.194943971655654691 ) ) ;
#11352=ORIENTED_EDGE ( 'NONE', *, *, #38162, .T. ) ;
#11353=CARTESIAN_POINT ( 'NONE',  ( 77.76298154960852571, 62.57953843473561051, -3.839379600940507675 ) ) ;
#11356=CARTESIAN_POINT ( 'NONE',  ( 81.42847900441161357, 61.86412877313428993, -2.316472630215918205 ) ) ;
#11357=CARTESIAN_POINT ( 'NONE',  ( 78.73442292448851276, 62.77418112150555629, 3.804514705604325364 ) ) ;
#11362=ADVANCED_FACE ( 'NONE', ( #37567 ), #3638, .T. ) ;
#11363=CARTESIAN_POINT ( 'NONE',  ( 82.50803812506910617, 63.51743744066186537, 1.680016503630071600 ) ) ;
#11368=FACE_OUTER_BOUND ( 'NONE', #36103, .T. ) ;
#11369=ORIENTED_EDGE ( 'NONE', *, *, #10903, .F. ) ;
#11386=CARTESIAN_POINT ( 'NONE',  ( 66.41110252083142029, 57.82170748331523669, 4.000000000000023981 ) ) ;
#11387=CARTESIAN_POINT ( 'NONE',  ( 72.42208042952545100, 59.16915255968121556, -3.823636340456165073 ) ) ;
#11389=ORIENTED_EDGE ( 'NONE', *, *, #8451, .F. ) ;
#11394=DIRECTION ( 'NONE',  ( -0.000000000000000000, -0.000000000000000000, 1.000000000000000000 ) ) ;
#11402=CARTESIAN_POINT ( 'NONE',  ( 80.76516742887832834, 61.34548671587045732, -2.174061886842025171 ) ) ;
#11404=CARTESIAN_POINT ( 'NONE',  ( 80.83921286824487140, 61.18398161863572682, 1.552792442904345815 ) ) ;
#11420=CARTESIAN_POINT ( 'NONE',  ( -63.70768058868311812, 44.39675795731061214, 4.000000000000000000 ) ) ;
#11432=CARTESIAN_POINT ( 'NONE',  ( 67.39181666045010388, 58.30934502646129403, 3.993945454764281422 ) ) ;
#11439=CARTESIAN_POINT ( 'NONE',  ( -58.91453996558632156, 28.99622802882459638, 6.206785453512805972 ) ) ;
#11445=CARTESIAN_POINT ( 'NONE',  ( 81.01114204962451026, 61.40637449960411942, -2.012706562768916907 ) ) ;
#11448=CARTESIAN_POINT ( 'NONE',  ( 81.02780191652733777, 61.56951766280584337, 2.259810845156954517 ) ) ;
#11450=DIRECTION ( 'NONE',  ( 0.000000000000000000, 0.000000000000000000, 1.000000000000000000 ) ) ;
#11453=CARTESIAN_POINT ( 'NONE',  ( 74.08781496033066105, 60.06802034872734453, -3.841642203975295544 ) ) ;
#11465=EDGE_CURVE ( 'NONE', #31687, #15032, #16987, .T. ) ;
#11466=CARTESIAN_POINT ( 'NONE',  ( 35.94200923520244828, 151.3264224549853907, -1.000000000000000000 ) ) ;
#11468=CARTESIAN_POINT ( 'NONE',  ( 79.22754343383607534, 66.08014515007958778, 1.953285432047549230 ) ) ;
#11470=FACE_OUTER_BOUND ( 'NONE', #10048, .T. ) ;
#11486=AXIS2_PLACEMENT_3D ( 'NONE', #22983, #19484, #19685 ) ;
#11490=CARTESIAN_POINT ( 'NONE',  ( 80.53345128649183948, 64.37995495044674499, -3.533418250979443176 ) ) ;
#11497=VERTEX_POINT ( 'NONE', #10978 ) ;
#11499=CARTESIAN_POINT ( 'NONE',  ( 81.19486284036338475, 61.45157923659408539, -1.862141363775748903 ) ) ;
#11505=CARTESIAN_POINT ( 'NONE',  ( 81.16810052477266879, 61.30343919788879248, -1.037317649801931863 ) ) ;
#11508=VECTOR ( 'NONE', #27528, 1000.000000000000000 ) ;
#11513=CARTESIAN_POINT ( 'NONE',  ( 74.23991766213896426, 61.26593220986219279, 3.911020515999898528 ) ) ;
#11515=CIRCLE ( 'NONE', #39817, 82.54614097552274643 ) ;
#11519=CARTESIAN_POINT ( 'NONE',  ( -62.99176104828779899, 35.53767314789729426, 6.181002566280151989 ) ) ;
#11520=FACE_OUTER_BOUND ( 'NONE', #32645, .T. ) ;
#11521=CARTESIAN_POINT ( 'NONE',  ( 81.94287803445145357, 63.22849810396159853, 2.713791510777069149 ) ) ;
#11538=CARTESIAN_POINT ( 'NONE',  ( 66.98331017875999294, 58.06610265625960210, -3.998453671246410934 ) ) ;
#11550=CARTESIAN_POINT ( 'NONE',  ( 82.35470118046110599, 62.54510421749741056, -1.103079483641125069 ) ) ;
#11552=CARTESIAN_POINT ( 'NONE',  ( 80.23319818986580287, 64.21721675003155383, 3.633989118465187129 ) ) ;
#11555=CARTESIAN_POINT ( 'NONE',  ( 78.34663729941159716, 61.36874863982424699, -3.480716904142254986 ) ) ;
#11558=CARTESIAN_POINT ( 'NONE',  ( 79.72834705193074001, 65.67299761742589226, -2.773332820897498774 ) ) ;
#11559=CARTESIAN_POINT ( 'NONE',  ( 79.02450826907198689, 62.91033389078318550, 3.791687334209853155 ) ) ;
#11563=CARTESIAN_POINT ( 'NONE',  ( 82.52664026313796342, 63.88931701666353291, 1.444831904608907092 ) ) ;
#11590=CARTESIAN_POINT ( 'NONE',  ( 66.27376694608996388, 57.73522568913447373, 4.000000000000000000 ) ) ;
#11591=CARTESIAN_POINT ( 'NONE',  ( 69.27779986746136842, 58.60568623525134768, -3.981537309218750487 ) ) ;
#11598=EDGE_CURVE ( 'NONE', #35091, #34454, #13716, .T. ) ;
#11599=CARTESIAN_POINT ( 'NONE',  ( -68.19214907655110380, 40.83859674667183981, -4.000000000000000000 ) ) ;
#11601=CIRCLE ( 'NONE', #10962, 0.9999999999999983347 ) ;
#11603=ORIENTED_EDGE ( 'NONE', *, *, #5785, .T. ) ;
#11607=CARTESIAN_POINT ( 'NONE',  ( 78.83700374940842437, 65.31049604782703000, -2.918211652848219373 ) ) ;
#11609=CARTESIAN_POINT ( 'NONE',  ( 81.52783586777042046, 64.51439989829013655, -2.952528780688971288 ) ) ;
#11610=CARTESIAN_POINT ( 'NONE',  ( 80.67643653137164961, 61.85813826494483436, 2.902290250791176085 ) ) ;
#11628=AXIS2_PLACEMENT_3D ( 'NONE', #27412, #22021, #21246 ) ;
#11634=CARTESIAN_POINT ( 'NONE',  ( 67.97136023280155825, 58.53559134324396496, 3.990965707299543475 ) ) ;
#11636=EDGE_CURVE ( 'NONE', #31330, #31687, #35428, .T. ) ;
#11642=CARTESIAN_POINT ( 'NONE',  ( 27.60344192425479193, 81.15229837709949834, 1.000000000000000000 ) ) ;
#11645=EDGE_CURVE ( 'NONE', #28100, #22494, #33462, .T. ) ;
#11648=AXIS2_PLACEMENT_3D ( 'NONE', #12710, #25481, #18895 ) ;
#11649=CARTESIAN_POINT ( 'NONE',  ( 78.70885197775000108, 65.89012877898849752, -1.994058748902171496 ) ) ;
#11653=CARTESIAN_POINT ( 'NONE',  ( 81.06091538032737276, 61.57736434115996360, 2.238287240292558433 ) ) ;
#11658=CARTESIAN_POINT ( 'NONE',  ( 74.03116782478153368, 60.19763641771454132, -3.876585409280477901 ) ) ;
#11671=CARTESIAN_POINT ( 'NONE',  ( 81.16101395366627003, 61.30084446962307254, 1.089225060639237519 ) ) ;
#11678=CARTESIAN_POINT ( 'NONE',  ( -65.15514661499977933, 34.97220226750605576, -6.888442104241543795 ) ) ;
#11684=CIRCLE ( 'NONE', #16964, 67.42751648247021024 ) ;
#11688=CARTESIAN_POINT ( 'NONE',  ( 80.17140661427380621, 64.93185644258198863, -3.352621494407066915 ) ) ;
#11692=DIRECTION ( 'NONE',  ( 0.000000000000000000, 0.000000000000000000, -1.000000000000000000 ) ) ;
#11701=CARTESIAN_POINT ( 'NONE',  ( 79.22373596144829833, 65.64748706429479341, -2.718470589328617848 ) ) ;
#11708=CARTESIAN_POINT ( 'NONE',  ( 80.79165360588653755, 65.97001311340675045, -2.094266784919526447 ) ) ;
#11714=CARTESIAN_POINT ( 'NONE',  ( 73.13464764220530867, 62.20839851451114555, 3.391332960900173887 ) ) ;
#11715=B_SPLINE_CURVE_WITH_KNOTS ( 'NONE', 3,
 ( #17350, #20063, #23560, #33239 ),
 .UNSPECIFIED., .F., .F.,
 ( 4, 4 ),
 ( 8.673617379884035472E-19, 0.0005391349717845210499 ),
 .UNSPECIFIED. ) ;
#11723=CARTESIAN_POINT ( 'NONE',  ( 80.24765655772210948, 65.96146312294942504, 2.334361474588997787 ) ) ;
#11738=CARTESIAN_POINT ( 'NONE',  ( 66.83775678531991105, 58.01055738293738528, -3.998747512904051060 ) ) ;
#11745=CARTESIAN_POINT ( 'NONE',  ( 71.72536746055673973, 61.26079380681123610, 3.629563705067941903 ) ) ;
#11753=CARTESIAN_POINT ( 'NONE',  ( 82.53033050081239708, 64.25366301186836893, -1.161365684106807850 ) ) ;
#11754=CARTESIAN_POINT ( 'NONE',  ( 80.84870020435621996, 62.70902516261514847, 3.354617312347321967 ) ) ;
#11755=LINE ( 'NONE', #24748, #2230 ) ;
#11757=CARTESIAN_POINT ( 'NONE',  ( 79.19973406752563960, 61.05435877263160904, -2.913524936156958844 ) ) ;
#11760=CARTESIAN_POINT ( 'NONE',  ( 78.68330935989223462, 66.05356751642949575, -1.089225060638855602 ) ) ;
#11761=CARTESIAN_POINT ( 'NONE',  ( 77.57568143946795658, 64.97578145858237519, 2.643019404357015656 ) ) ;
#11764=CARTESIAN_POINT ( 'NONE',  ( 81.46661790917879387, 61.46529165999842093, 1.093381982072756164 ) ) ;
#11788=VECTOR ( 'NONE', #2967, 1000.000000000000000 ) ;
#11791=CARTESIAN_POINT ( 'NONE',  ( 70.73355890789336797, 59.99733340013641936, -3.925556587156273647 ) ) ;
#11807=CARTESIAN_POINT ( 'NONE',  ( 80.58155366896997407, 61.83530676836470974, -2.934133054905257776 ) ) ;
#11810=CARTESIAN_POINT ( 'NONE',  ( 80.19490802141253027, 65.93291197049440200, -2.397965335136836629 ) ) ;
#11811=CARTESIAN_POINT ( 'NONE',  ( 78.46701299008461206, 65.82614401021746176, 1.855758959884434400 ) ) ;
#11812=ORIENTED_EDGE ( 'NONE', *, *, #17360, .F. ) ;
#11814=AXIS2_PLACEMENT_3D ( 'NONE', #18428, #9169, #34323 ) ;
#11830=CARTESIAN_POINT ( 'NONE',  ( -60.75950795826495465, 23.17721540975219696, -12.49999999999999645 ) ) ;
#11835=TOROIDAL_SURFACE ( 'NONE', #31594, 10.99999999999998579, 3.000000000000000000 ) ;
#11842=CARTESIAN_POINT ( 'NONE',  ( 67.39973655466486946, 58.28774108029888623, 3.995059460290580233 ) ) ;
#11857=CARTESIAN_POINT ( 'NONE',  ( 81.00146336277434500, 61.29413404061270398, -1.724274471760811167 ) ) ;
#11859=CARTESIAN_POINT ( 'NONE',  ( 79.45910779949859659, 64.84755599131123915, 3.411701596789212143 ) ) ;
#11862=CARTESIAN_POINT ( 'NONE',  ( 74.35309583984513893, 59.45637312398173435, -3.556895493431092348 ) ) ;
#11877=CARTESIAN_POINT ( 'NONE',  ( 80.07838786650494001, 65.24465706271048759, 3.189931650267152641 ) ) ;
#11879=LINE ( 'NONE', #24454, #26611 ) ;
#11880=VERTEX_POINT ( 'NONE', #15967 ) ;
#11887=DIRECTION ( 'NONE',  ( 0.5991095979999722099, -0.2428960078352049856, 0.7629346098860843028 ) ) ;
#11895=CARTESIAN_POINT ( 'NONE',  ( 79.55653453243729700, 65.56957575487831491, -2.861733672647129634 ) ) ;
#11899=FACE_OUTER_BOUND ( 'NONE', #39502, .T. ) ;
#11900=ORIENTED_EDGE ( 'NONE', *, *, #3392, .F. ) ;
#11906=CARTESIAN_POINT ( 'NONE',  ( 80.81256737103976207, 62.69530837521176636, -3.364061116559605935 ) ) ;
#11911=EDGE_LOOP ( 'NONE', ( #33311, #29144, #30526, #24486 ) ) ;
#11912=CARTESIAN_POINT ( 'NONE',  ( 79.87389178145686230, 66.27500989097897843, -1.700667878122840593 ) ) ;
#11920=CARTESIAN_POINT ( 'NONE',  ( 73.50720661118039345, 61.38260725348155944, 3.841642204035220942 ) ) ;
#11928=EDGE_LOOP ( 'NONE', ( #7570, #39713, #23440, #31489 ) ) ;
#11929=CARTESIAN_POINT ( 'NONE',  ( 80.10847647497645596, 65.88576991956399809, 2.484976468875361277 ) ) ;
#11942=CYLINDRICAL_SURFACE ( 'NONE', #16478, 1.000000000000000000 ) ;
#11948=CARTESIAN_POINT ( 'NONE',  ( 66.88492799900151908, 57.87961537897388808, -3.998747512900713730 ) ) ;
#11959=CARTESIAN_POINT ( 'NONE',  ( 80.71704827558885142, 66.21292280724347279, -1.000000000000000000 ) ) ;
#11961=CARTESIAN_POINT ( 'NONE',  ( 81.11033257497912530, 61.28231361833088897, 1.235082213173759547 ) ) ;
#11964=CARTESIAN_POINT ( 'NONE',  ( 76.91271350297704146, 62.89131350122335817, -3.776276000685965251 ) ) ;
#11968=CARTESIAN_POINT ( 'NONE',  ( 78.81184074671398321, 66.10527324714774977, -1.416821487223371978 ) ) ;
#11970=CARTESIAN_POINT ( 'NONE',  ( 79.19973406752559697, 61.05435877263168720, 2.913524936157070755 ) ) ;
#11974=CARTESIAN_POINT ( 'NONE',  ( 80.30118292188606688, 66.27423127454436269, 1.564050819713522777 ) ) ;
#11981=CARTESIAN_POINT ( 'NONE',  ( -64.46937875527800088, 36.54399046018752273, 5.728582434991126071 ) ) ;
#11995=CARTESIAN_POINT ( 'NONE',  ( -62.89172142731304405, 37.18122596373097366, -4.326867315595535501 ) ) ;
#12001=CARTESIAN_POINT ( 'NONE',  ( 70.90076320674430121, 59.58500768881799559, -3.976054184260641833 ) ) ;
#12006=CARTESIAN_POINT ( 'NONE',  ( 69.84993430378905543, 58.85661355152254970, 3.977789803233258148 ) ) ;
#12017=CARTESIAN_POINT ( 'NONE',  ( 80.72339804071911828, 61.33444547702553962, -2.197205184446166637 ) ) ;
#12019=CARTESIAN_POINT ( 'NONE',  ( 81.40473435056793505, 64.45019880697486769, -3.071899782094857034 ) ) ;
#12020=CARTESIAN_POINT ( 'NONE',  ( 78.85457743492895588, 65.01671056748381261, 3.151254463354984825 ) ) ;
#12021=EDGE_CURVE ( 'NONE', #7186, #3289, #35139, .T. ) ;
#12029=PLANE ( 'NONE',  #10328 ) ;
#12043=VERTEX_POINT ( 'NONE', #40159 ) ;
#12044=CARTESIAN_POINT ( 'NONE',  ( 66.98823442903206171, 58.05250069757015297, 3.998791315154375692 ) ) ;
#12056=DIRECTION ( 'NONE',  ( 0.000000000000000000, 1.000000000000000000, 0.000000000000000000 ) ) ;
#12060=CARTESIAN_POINT ( 'NONE',  ( 80.36115745751311579, 63.17601289530517761, -3.638935937159312850 ) ) ;
#12064=CARTESIAN_POINT ( 'NONE',  ( 80.52560336917662198, 62.91486207252171425, 3.518158556798114400 ) ) ;
#12065=CARTESIAN_POINT ( 'NONE',  ( -63.99293516169446150, 35.89893413629672381, -46.17089178453873188 ) ) ;
#12070=CARTESIAN_POINT ( 'NONE',  ( 74.30428547378053850, 61.12304205247700395, -3.924711207976832927 ) ) ;
#12078=VERTEX_POINT ( 'NONE', #18328 ) ;
#12085=CARTESIAN_POINT ( 'NONE',  ( 79.52751932686963698, 65.84655314362326806, 2.556731990914093533 ) ) ;
#12091=ORIENTED_EDGE ( 'NONE', *, *, #24798, .F. ) ;
#12093=FACE_OUTER_BOUND ( 'NONE', #18948, .T. ) ;
#12100=ORIENTED_EDGE ( 'NONE', *, *, #1837, .T. ) ;
#12101=CARTESIAN_POINT ( 'NONE',  ( 79.42405716688904249, 65.78352207363049331, -2.615128354545405376 ) ) ;
#12109=EDGE_CURVE ( 'NONE', #446, #36272, #27605, .T. ) ;
#12111=CARTESIAN_POINT ( 'NONE',  ( 81.13619541807486257, 61.97540048441254612, -2.718470589328601417 ) ) ;
#12113=CARTESIAN_POINT ( 'NONE',  ( -59.14838763364237906, 27.28340689960984733, -4.628958989307211169 ) ) ;
#12120=CARTESIAN_POINT ( 'NONE',  ( 81.94417840557096611, 63.58970459987528301, -2.726953404243311230 ) ) ;
#12127=CARTESIAN_POINT ( 'NONE',  ( -64.08758708074093136, 42.49068820928864199, -3.479708933549301442 ) ) ;
#12128=CARTESIAN_POINT ( 'NONE',  ( 73.38675137958711048, 60.10977650211887635, 3.914122288815133910 ) ) ;
#12131=VERTEX_POINT ( 'NONE', #26998 ) ;
#12138=CARTESIAN_POINT ( 'NONE',  ( 81.51618470504207892, 61.58087653888393476, 1.588372325568258914 ) ) ;
#12142=AXIS2_PLACEMENT_3D ( 'NONE', #37486, #21859, #34435 ) ;
#12143=CARTESIAN_POINT ( 'NONE',  ( -64.08758708074093136, 38.13199975834322686, 3.043809435734686097 ) ) ;
#12151=FACE_OUTER_BOUND ( 'NONE', #14199, .T. ) ;
#12157=FACE_OUTER_BOUND ( 'NONE', #3154, .T. ) ;
#12159=CARTESIAN_POINT ( 'NONE',  ( 66.90849722842033032, 57.81418058710544727, -3.996206253853811674 ) ) ;
#12169=CARTESIAN_POINT ( 'NONE',  ( -65.04872026876938662, 34.92042435966252611, 6.752913741461252783 ) ) ;
#12176=CARTESIAN_POINT ( 'NONE',  ( 80.38645948019593845, 66.31981033314001195, -1.000000000000000000 ) ) ;
#12177=CARTESIAN_POINT ( 'NONE',  ( 80.27036958223403929, 63.85842528439429344, 3.661914029440276774 ) ) ;
#12181=CARTESIAN_POINT ( 'NONE',  ( 77.16059773406421129, 63.78117330919809547, -3.480716904142247881 ) ) ;
#12185=CARTESIAN_POINT ( 'NONE',  ( 81.11561130678553866, 63.91242180913142334, -3.402511877377342397 ) ) ;
#12187=CARTESIAN_POINT ( 'NONE',  ( 78.25991397077970646, 61.55280089391300891, 3.597602401604638178 ) ) ;
#12191=CARTESIAN_POINT ( 'NONE',  ( -63.08758708074093136, 38.76906266698303227, 3.000000000000000000 ) ) ;
#12192=CARTESIAN_POINT ( 'NONE',  ( 80.93658766080277189, 66.04709959793324003, 1.728104186157678468 ) ) ;
#12198=CARTESIAN_POINT ( 'NONE',  ( -64.08758708074093136, 36.14363715547680300, 3.800414904976361807 ) ) ;
#12200=FACE_BOUND ( 'NONE', #24942, .T. ) ;
#12205=CARTESIAN_POINT ( 'NONE',  ( 81.06639586472026338, 61.26627432693234709, 1.317842247490183860 ) ) ;
#12220=CARTESIAN_POINT ( 'NONE',  ( 70.66749459857992122, 60.15980271599462981, -3.887826097256385172 ) ) ;
#12230=CARTESIAN_POINT ( 'NONE',  ( 89.09355779190869384, 24.84364830758654108, 8.800414904976364028 ) ) ;
#12235=CARTESIAN_POINT ( 'NONE',  ( 80.56990227295247564, 61.62418804268438066, -2.732428818688231065 ) ) ;
#12237=CARTESIAN_POINT ( 'NONE',  ( 79.13116897371943992, 66.19293011460082710, -1.571309534768106086 ) ) ;
#12238=CARTESIAN_POINT ( 'NONE',  ( 79.52562300987042931, 63.81209149333333386, 3.741985197832885301 ) ) ;
#12248=FACE_OUTER_BOUND ( 'NONE', #34330, .T. ) ;
#12263=CARTESIAN_POINT ( 'NONE',  ( 67.45521008556633547, 58.13638817365040978, 3.998402061830689025 ) ) ;
#12279=CARTESIAN_POINT ( 'NONE',  ( 78.65528874306559715, 65.84149099381058079, -2.048264032867935569 ) ) ;
#12281=CARTESIAN_POINT ( 'NONE',  ( 80.74625401487976717, 62.12052764141679262, 3.052025427726071438 ) ) ;
#12284=DIRECTION ( 'NONE',  ( 0.000000000000000000, 0.000000000000000000, 1.000000000000000000 ) ) ;
#12285=VECTOR ( 'NONE', #30601, 1000.000000000000000 ) ;
#12286=CARTESIAN_POINT ( 'NONE',  ( -80.19065981525227471, 31.27226540113725051, 8.800414904976364028 ) ) ;
#12290=CIRCLE ( 'NONE', #10326, 34.02204673211314656 ) ;
#12296=AXIS2_PLACEMENT_3D ( 'NONE', #790, #34786, #10236 ) ;
#12300=CARTESIAN_POINT ( 'NONE',  ( 81.26611686294327797, 61.37229692769314227, 1.428845309148520037 ) ) ;
#12304=CARTESIAN_POINT ( 'NONE',  ( -64.52609798206562175, 34.68664092740665694, -5.853076040061139906 ) ) ;
#12306=EDGE_CURVE ( 'NONE', #15467, #15868, #4037, .T. ) ;
#12309=CARTESIAN_POINT ( 'NONE',  ( -66.90228649916429049, 37.07846761000594427, -9.592188357273899513 ) ) ;
#12317=CARTESIAN_POINT ( 'NONE',  ( 80.98576866654174466, 63.46339031992854984, -3.471690071579498493 ) ) ;
#12330=CARTESIAN_POINT ( 'NONE',  ( 81.17223480711247419, 61.34085670634290466, -1.541060042019461340 ) ) ;
#12336=CARTESIAN_POINT ( 'NONE',  ( 80.91683595914862792, 65.70075836866568864, -2.460680857249041509 ) ) ;
#12343=CARTESIAN_POINT ( 'NONE',  ( 74.19779514372055473, 59.81543539827580958, 3.749455561448977736 ) ) ;
#12353=CARTESIAN_POINT ( 'NONE',  ( 80.02729359676493459, 65.84138187185888569, 2.563845612517933858 ) ) ;
#12357=CARTESIAN_POINT ( 'NONE',  ( -66.99872204295122913, 28.48507918597134037, 6.999999999999999112 ) ) ;
#12368=DIRECTION ( 'NONE',  ( 0.8459487642040833810, 0.000000000000000000, 0.5332641825039293737 ) ) ;
#12375=DIRECTION ( 'NONE',  ( -1.000000000000000000, 0.000000000000000000, 0.000000000000000000 ) ) ;
#12377=CARTESIAN_POINT ( 'NONE',  ( 66.58157743075884127, 57.80130068828511014, -3.999688274311175906 ) ) ;
#12382=ORIENTED_EDGE ( 'NONE', *, *, #25074, .T. ) ;
#12387=CARTESIAN_POINT ( 'NONE',  ( 81.46190421581948726, 61.46294189193148583, -1.114595100209338163 ) ) ;
#12389=CARTESIAN_POINT ( 'NONE',  ( 81.17225696364401699, 61.44517649410260418, 1.881209715725439269 ) ) ;
#12390=DIRECTION ( 'NONE',  ( 0.000000000000000000, 0.000000000000000000, 1.000000000000000000 ) ) ;
#12392=CARTESIAN_POINT ( 'NONE',  ( 76.69853897424475520, 64.65515986876398813, -2.498359881428370066 ) ) ;
#12397=CARTESIAN_POINT ( 'NONE',  ( 81.39943925848315587, 61.85181198611487474, -2.332991218130514355 ) ) ;
#12398=CARTESIAN_POINT ( 'NONE',  ( 77.20018789615933485, 65.00686241173514190, 2.285396881590278984 ) ) ;
#12402=CARTESIAN_POINT ( 'NONE',  ( -57.16504416091206053, 33.41445838748276742, 4.000000000000000000 ) ) ;
#12403=CARTESIAN_POINT ( 'NONE',  ( 82.21758965863736535, 62.47540435105901935, 1.725837398062986638 ) ) ;
#12423=CARTESIAN_POINT ( 'NONE',  ( -62.81463675898083210, 36.67811266762162603, -4.600311178732272133 ) ) ;
#12429=CARTESIAN_POINT ( 'NONE',  ( 35.94200923520244828, 151.3264224549853907, 4.000000000000000000 ) ) ;
#12430=CARTESIAN_POINT ( 'NONE',  ( 69.41850365747683327, 58.24027689931818230, -3.921432738910689331 ) ) ;
#12442=CARTESIAN_POINT ( 'NONE',  ( 80.49182418769539993, 61.81278841749718822, -2.961936469198068078 ) ) ;
#12445=CARTESIAN_POINT ( 'NONE',  ( 78.68779346184201984, 66.05675297672225099, -1.054034669008010905 ) ) ;
#12446=CARTESIAN_POINT ( 'NONE',  ( 79.93872656714209768, 63.00306196921508217, 3.690346394509887773 ) ) ;
#12449=CARTESIAN_POINT ( 'NONE',  ( 82.26973386304365476, 64.90130211351629441, 1.000000000000000000 ) ) ;
#12459=AXIS2_PLACEMENT_3D ( 'NONE', #1988, #10808, #36548 ) ;
#12475=CARTESIAN_POINT ( 'NONE',  ( 67.04239844378345481, 57.90286417203066094, 3.997553359131193584 ) ) ;
#12492=CARTESIAN_POINT ( 'NONE',  ( 79.52504771873071832, 64.52527500529767224, -3.543129918319044780 ) ) ;
#12494=CARTESIAN_POINT ( 'NONE',  ( 79.70130230958179141, 64.28379252955069489, 3.649417990092605368 ) ) ;
#12498=CARTESIAN_POINT ( 'NONE',  ( -64.08758708074093136, 38.60011822860993647, -4.018727294472382638 ) ) ;
#12502=ORIENTED_EDGE ( 'NONE', *, *, #7388, .F. ) ;
#12503=CARTESIAN_POINT ( 'NONE',  ( -65.15514661499977933, 34.97220226750606997, -6.888442104241543795 ) ) ;
#12506=CARTESIAN_POINT ( 'NONE',  ( 81.45253739226701839, 61.71286443377144337, 1.983726836936649196 ) ) ;
#12517=ORIENTED_EDGE ( 'NONE', *, *, #31818, .T. ) ;
#12522=CARTESIAN_POINT ( 'NONE',  ( 81.23686708412716939, 61.78859655676697571, -2.419967184825706497 ) ) ;
#12523=CARTESIAN_POINT ( 'NONE',  ( -66.99872204295122913, 28.48507918597134037, -4.000000000000000000 ) ) ;
#12529=VERTEX_POINT ( 'NONE', #6658 ) ;
#12533=CARTESIAN_POINT ( 'NONE',  ( 79.12626349118841063, 65.57005066984849861, -2.769656700700048990 ) ) ;
#12539=ORIENTED_EDGE ( 'NONE', *, *, #21900, .T. ) ;
#12540=CARTESIAN_POINT ( 'NONE',  ( 80.36115181822145814, 66.02274906846022873, -2.190303691588677104 ) ) ;
#12546=CARTESIAN_POINT ( 'NONE',  ( -64.08758708074093136, 42.32104734179812766, -3.571363574845913380 ) ) ;
#12547=CARTESIAN_POINT ( 'NONE',  ( 73.23371602657820745, 61.99063567959824894, 3.556895493546552878 ) ) ;
#12552=CARTESIAN_POINT ( 'NONE',  ( -59.00110696496998486, 28.68040728033255249, -6.866973098862638736 ) ) ;
#12555=CARTESIAN_POINT ( 'NONE',  ( 81.56442676284315496, 64.14391357696001705, 3.071899782094677178 ) ) ;
#12561=EDGE_CURVE ( 'NONE', #7366, #35091, #32088, .T. ) ;
#12574=CARTESIAN_POINT ( 'NONE',  ( 66.69694663263604184, 57.94160696200565042, -3.999246569073970026 ) ) ;
#12578=CARTESIAN_POINT ( 'NONE',  ( -58.07367359896441172, 31.71941035118960883, 4.399945119674323557 ) ) ;
#12586=CARTESIAN_POINT ( 'NONE',  ( 80.01568814228012627, 66.35127795588805100, -1.246975333547555742 ) ) ;
#12587=CARTESIAN_POINT ( 'NONE',  ( 80.30796587587546753, 63.87804906342756084, 3.654032574946330936 ) ) ;
#12590=CARTESIAN_POINT ( 'NONE',  ( 77.22142874756843867, 60.78359660874937020, -3.498861892161951648 ) ) ;
#12596=CARTESIAN_POINT ( 'NONE',  ( 80.58645273467564607, 64.40825618792592877, -3.509897338575004078 ) ) ;
#12597=CARTESIAN_POINT ( 'NONE',  ( 78.33250027093573920, 62.86460196216437168, 3.816136337383051025 ) ) ;
#12604=CARTESIAN_POINT ( 'NONE',  ( 81.16926347961613430, 61.30386509772021242, 1.017094602978565909 ) ) ;
#12609=CARTESIAN_POINT ( 'NONE',  ( -63.05388691672963830, 35.53807678487858368, -6.298580386186273472 ) ) ;
#12610=CARTESIAN_POINT ( 'NONE',  ( -64.72110749213834424, 34.74377494905843378, 6.240054254829134450 ) ) ;
#12627=CARTESIAN_POINT ( 'NONE',  ( 68.80725167329416081, 58.08536582812667604, -3.941639393089865440 ) ) ;
#12643=CARTESIAN_POINT ( 'NONE',  ( 78.49476978275076533, 65.27812458131612061, -2.797036776683045733 ) ) ;
#12646=CARTESIAN_POINT ( 'NONE',  ( 80.42837321984433174, 65.43835520823199658, -2.971291902545808217 ) ) ;
#12647=CARTESIAN_POINT ( 'NONE',  ( 79.74939209361063774, 63.58699539661090228, 3.734652355492745990 ) ) ;
#12649=CARTESIAN_POINT ( 'NONE',  ( 89.09355779190869384, 24.84364830758654108, -8.800414904976364028 ) ) ;
#12673=CARTESIAN_POINT ( 'NONE',  ( 67.04731915158012612, 57.88926793091046363, 3.996990690923977407 ) ) ;
#12689=CARTESIAN_POINT ( 'NONE',  ( 79.20958446297056810, 65.00485465208042513, -3.275607309966719338 ) ) ;
#12691=CARTESIAN_POINT ( 'NONE',  ( 80.99919828920802445, 61.56308015027072145, 2.277920705665342993 ) ) ;
#12698=ADVANCED_FACE ( 'NONE', ( #26597 ), #3789, .T. ) ;
#12704=CARTESIAN_POINT ( 'NONE',  ( -64.84514717441444986, 36.26677316194228951, -6.475000919363135488 ) ) ;
#12708=AXIS2_PLACEMENT_3D ( 'NONE', #25639, #20064, #19860 ) ;
#12710=CARTESIAN_POINT ( 'NONE',  ( -68.98442902999595105, 21.93515443114010210, -8.800414904976364028 ) ) ;
#12711=CARTESIAN_POINT ( 'NONE',  ( 79.10630237408686583, 66.00617110148432687, 2.043563575549256495 ) ) ;
#12722=ORIENTED_EDGE ( 'NONE', *, *, #33278, .T. ) ;
#12726=CARTESIAN_POINT ( 'NONE',  ( 81.13780861853922488, 61.29235415973831635, -1.171933751919293831 ) ) ;
#12736=CARTESIAN_POINT ( 'NONE',  ( 79.57367618494546946, 64.93149010139244126, -3.380189700376623474 ) ) ;
#12741=CARTESIAN_POINT ( 'NONE',  ( 79.21008177357728641, 66.23692415242760489, -1.465632304122640228 ) ) ;
#12750=CARTESIAN_POINT ( 'NONE',  ( 69.50581201620700256, 59.72791825745761685, 3.883859131414829413 ) ) ;
#12754=CARTESIAN_POINT ( 'NONE',  ( -57.69456667414278428, 32.53259245237469344, -4.116672578207452915 ) ) ;
#12755=DIRECTION ( 'NONE',  ( 0.8459487642040750544, 0.000000000000000000, -0.5332641825039424743 ) ) ;
#12756=CARTESIAN_POINT ( 'NONE',  ( 79.35885969106158200, 66.15515411851721694, 1.832274617051027121 ) ) ;
#12761=AXIS2_PLACEMENT_3D ( 'NONE', #10459, #23040, #35606 ) ;
#12774=ORIENTED_EDGE ( 'NONE', *, *, #40218, .F. ) ;
#12777=CARTESIAN_POINT ( 'NONE',  ( 66.55809347730310321, 57.86716763633229021, -3.999802976172705193 ) ) ;
#12782=ORIENTED_EDGE ( 'NONE', *, *, #23306, .F. ) ;
#12784=CARTESIAN_POINT ( 'NONE',  ( -58.99948754145754037, 28.61410076184115070, -6.947368380125259257 ) ) ;
#12787=CARTESIAN_POINT ( 'NONE',  ( 81.72179206571539112, 61.68197623675723662, -1.214491505233944002 ) ) ;
#12788=CARTESIAN_POINT ( 'NONE',  ( 79.86701161339794908, 64.38869582053085594, 3.619557188109057133 ) ) ;
#12793=ORIENTED_EDGE ( 'NONE', *, *, #1649, .T. ) ;
#12794=CARTESIAN_POINT ( 'NONE',  ( 77.53347081925224415, 60.09046002684883803, -2.805892758502992468 ) ) ;
#12796=CARTESIAN_POINT ( 'NONE',  ( -55.16612787639756732, 31.23053227951973199, 1.484562114140385747 ) ) ;
#12798=CARTESIAN_POINT ( 'NONE',  ( 80.03255827398538713, 65.21842193378445529, -3.211742283750908644 ) ) ;
#12799=CARTESIAN_POINT ( 'NONE',  ( 77.48714025262371763, 64.49898405264991652, 3.102003663616900830 ) ) ;
#12804=CARTESIAN_POINT ( 'NONE',  ( -59.00110696496997775, 28.68040728033253473, 6.866925925439470113 ) ) ;
#12805=CARTESIAN_POINT ( 'NONE',  ( 82.39984057372362258, 63.46184634947046987, 2.021051955676536505 ) ) ;
#12811=CARTESIAN_POINT ( 'NONE',  ( -64.25913952751501768, 36.58001704789108288, 5.467911005455182938 ) ) ;
#12830=CARTESIAN_POINT ( 'NONE',  ( 67.92345958529671179, 58.66354838738842403, -3.978477839347868361 ) ) ;
#12847=CARTESIAN_POINT ( 'NONE',  ( 80.12095330986326758, 62.19218463582609502, -3.375657603866087264 ) ) ;
#12850=CARTESIAN_POINT ( 'NONE',  ( 81.44856608406118426, 64.08396523683251189, -3.179853676209052793 ) ) ;
#12851=CARTESIAN_POINT ( 'NONE',  ( 78.35540530300707474, 65.82096406625564100, 1.612955153530279295 ) ) ;
#12854=PLANE ( 'NONE',  #34418 ) ;
#12882=CARTESIAN_POINT ( 'NONE',  ( 66.88885785885000246, 57.86870549787170859, 3.998465113252547720 ) ) ;
#12885=AXIS2_PLACEMENT_3D ( 'NONE', #28107, #31416, #9166 ) ;
#12897=CARTESIAN_POINT ( 'NONE',  ( 80.51397140397763508, 62.59311809350356981, -3.432573985763844426 ) ) ;
#12899=CARTESIAN_POINT ( 'NONE',  ( 80.90366483818405641, 61.70104970548236878, 2.590854534519439145 ) ) ;
#12902=CARTESIAN_POINT ( 'NONE',  ( -57.37129370382410798, 30.38064075563917044, 3.769987657317164231 ) ) ;
#12908=CARTESIAN_POINT ( 'NONE',  ( -65.04873975080087689, 34.92043383559632019, -6.752938550805224871 ) ) ;
#12910=ADVANCED_FACE ( 'NONE', ( #4768 ), #1905, .F. ) ;
#12916=CARTESIAN_POINT ( 'NONE',  ( 78.79418933159148253, 66.09338072887962312, 1.439474762807422703 ) ) ;
#12920=CARTESIAN_POINT ( 'NONE',  ( -67.52519766902113929, 36.12526529565825939, 8.800414904976360475 ) ) ;
#12926=CARTESIAN_POINT ( 'NONE',  ( -64.75098741874282382, 36.24760096809094989, 6.319851154869007281 ) ) ;
#12929=DIRECTION ( 'NONE',  ( -0.000000000000000000, -0.000000000000000000, -1.000000000000000000 ) ) ;
#12936=CARTESIAN_POINT ( 'NONE',  ( 80.34143827441936025, 64.27643806731579446, -3.602832836245127623 ) ) ;
#12946=CARTESIAN_POINT ( 'NONE',  ( 79.41630106684689849, 65.17102571570140412, -3.206617288017370448 ) ) ;
#12953=CARTESIAN_POINT ( 'NONE',  ( 81.31254497084465527, 65.18305021144011846, -2.731810022748015321 ) ) ;
#12958=CARTESIAN_POINT ( 'NONE',  ( -64.08758708074093136, 41.04287353446839148, -3.000000000000000000 ) ) ;
#12959=CARTESIAN_POINT ( 'NONE',  ( 70.66749459857992122, 60.15980271599462981, 3.887826097256385172 ) ) ;
#12967=CARTESIAN_POINT ( 'NONE',  ( -55.02847197064691898, 31.32671726583495442, -1.333002506602602999 ) ) ;
#12968=CARTESIAN_POINT ( 'NONE',  ( 81.68688842593508070, 61.98347795596147591, 2.134710458528625843 ) ) ;
#12976=VECTOR ( 'NONE', #22482, 1000.000000000000114 ) ;
#12989=CARTESIAN_POINT ( 'NONE',  ( 66.71166677010936041, 57.90060579507158423, -3.999756211082797996 ) ) ;
#12997=CARTESIAN_POINT ( 'NONE',  ( 81.94344439483582221, 61.95170768642834958, -1.250177805244664375 ) ) ;
#12998=CARTESIAN_POINT ( 'NONE',  ( 78.61848929481175219, 66.00753381999014380, 1.284346554836966581 ) ) ;
#13003=CARTESIAN_POINT ( 'NONE',  ( 74.79578028543750179, 61.54621940999656715, -3.896954863271601788 ) ) ;
#13008=CARTESIAN_POINT ( 'NONE',  ( 78.67891909395969208, 66.05044883183083471, -1.113695828830620016 ) ) ;
#13009=CARTESIAN_POINT ( 'NONE',  ( 78.14662766244083514, 60.27555255246360133, 2.661196496289686575 ) ) ;
#13014=CARTESIAN_POINT ( 'NONE',  ( -58.94604240597273304, 28.88056450265317210, 6.383919085388007453 ) ) ;
#13015=CARTESIAN_POINT ( 'NONE',  ( 78.68944183191024422, 66.05792399308623430, 1.032522165606396092 ) ) ;
#13022=CARTESIAN_POINT ( 'NONE',  ( 67.10243339269433704, 57.83959038316312729, 3.993403965430729841 ) ) ;
#13037=CARTESIAN_POINT ( 'NONE',  ( 68.09143390058649459, 58.21448531840948704, -3.990965707299596321 ) ) ;
#13047=CARTESIAN_POINT ( 'NONE',  ( 79.10769140560611845, 65.82222301601623826, 2.432199249741004987 ) ) ;
#13051=CARTESIAN_POINT ( 'NONE',  ( 79.76387963405315418, 62.93107248426419176, -3.707164540951496168 ) ) ;
#13055=CARTESIAN_POINT ( 'NONE',  ( 81.16306007146947366, 61.30159356321330932, -1.077711394953977386 ) ) ;
#13057=CARTESIAN_POINT ( 'NONE',  ( 80.39537321288027272, 61.58102678004054553, 2.797036776683078596 ) ) ;
#13061=CARTESIAN_POINT ( 'NONE',  ( -64.08758708074093136, 43.62395174008263865, 2.468800635787086417 ) ) ;
#13065=ORIENTED_EDGE ( 'NONE', *, *, #452, .F. ) ;
#13071=ORIENTED_EDGE ( 'NONE', *, *, #28296, .T. ) ;
#13087=CARTESIAN_POINT ( 'NONE',  ( 66.83775678531991105, 58.01055738293738528, 3.998747512904051060 ) ) ;
#13100=UNCERTAINTY_MEASURE_WITH_UNIT (LENGTH_MEASURE( 1.000000000000000082E-05 ), #32951, 'distance_accuracy_value', 'NONE');
#13103=CARTESIAN_POINT ( 'NONE',  ( 78.54140637431730454, 65.95282500403628489, -1.409197735201547674 ) ) ;
#13105=CARTESIAN_POINT ( 'NONE',  ( 78.89219914629886432, 65.63660985470716014, 2.576318598473995802 ) ) ;
#13124=CARTESIAN_POINT ( 'NONE',  ( 81.36347513509556961, 62.06248151587793416, 2.615128354545396494 ) ) ;
#13129=TOROIDAL_SURFACE ( 'NONE', #11104, 5.329987104167480894, 1.000000000000000000 ) ;
#13135=CARTESIAN_POINT ( 'NONE',  ( 69.17602579976487220, 58.86946863987066791, 3.990151341881416514 ) ) ;
#13138=CARTESIAN_POINT ( 'NONE',  ( 72.80781396401921768, 61.43345056764702150, -3.736020861133335647 ) ) ;
#13142=CARTESIAN_POINT ( 'NONE',  ( 80.21507364257669792, 64.59331366548809683, -3.526329879082137797 ) ) ;
#13151=CARTESIAN_POINT ( 'NONE',  ( 80.96353394671048420, 62.18107606247197339, -2.978180346930979994 ) ) ;
#13163=CARTESIAN_POINT ( 'NONE',  ( -63.68223573671823345, 44.25617700581931047, -1.889122668681848527 ) ) ;
#13164=CARTESIAN_POINT ( 'NONE',  ( 72.12755885004493450, 59.87634726091143023, 3.962431611477345239 ) ) ;
#13167=EDGE_LOOP ( 'NONE', ( #40492, #28289, #6618, #672 ) ) ;
#13173=CARTESIAN_POINT ( 'NONE',  ( 81.59312859629706338, 63.05267747589692107, 3.015199126130972740 ) ) ;
#13182=DIRECTION ( 'NONE',  ( 1.000000000000000000, 1.301859416973403519E-15, 0.000000000000000000 ) ) ;
#13190=CARTESIAN_POINT ( 'NONE',  ( 66.42297474478729669, 57.78816748095987776, -4.000000000000015987 ) ) ;
#13200=CARTESIAN_POINT ( 'NONE',  ( 82.44602376881505279, 63.15227202030949627, -1.728104186158371913 ) ) ;
#13204=CARTESIAN_POINT ( 'NONE',  ( 75.00613679496295561, 61.08591394029932076, -3.912919437578906035 ) ) ;
#13208=CARTESIAN_POINT ( 'NONE',  ( 75.81058488580242738, 63.71552251304081693, 3.121245466998407103 ) ) ;
#13216=CARTESIAN_POINT ( 'NONE',  ( 82.12703758395463183, 64.04502942998723825, 2.474249079298665333 ) ) ;
#13237=CARTESIAN_POINT ( 'NONE',  ( 67.91151009994659660, 58.69545974841741298, -3.974537232972598755 ) ) ;
#13248=CARTESIAN_POINT ( 'NONE',  ( 81.13780861853922488, 61.29235415973830925, 1.171933751919296274 ) ) ;
#13252=CARTESIAN_POINT ( 'NONE',  ( 78.19518920554678232, 64.50268734400745529, -3.317372267376125450 ) ) ;
#13255=CARTESIAN_POINT ( 'NONE',  ( 79.35885969106151094, 66.15515411851717431, -1.832274617051104393 ) ) ;
#13256=CARTESIAN_POINT ( 'NONE',  ( 80.71621671784500052, 61.21110637000719379, 1.935054690158737323 ) ) ;
#13257=ORIENTED_EDGE ( 'NONE', *, *, #22577, .T. ) ;
#13261=CARTESIAN_POINT ( 'NONE',  ( 79.67387220895498956, 66.32735109421597031, 1.189854999565118199 ) ) ;
#13262=CARTESIAN_POINT ( 'NONE',  ( -64.08758708074307719, 42.81481910881112896, 3.292730723027928796 ) ) ;
#13273=DIRECTION ( 'NONE',  ( -0.000000000000000000, -0.000000000000000000, -1.000000000000000000 ) ) ;
#13281=CARTESIAN_POINT ( 'NONE',  ( 66.82203765260634043, 58.05418649187924274, 3.997265020314329842 ) ) ;
#13282=AXIS2_PLACEMENT_3D ( 'NONE', #9944, #896, #35687 ) ;
#13292=CARTESIAN_POINT ( 'NONE',  ( 80.75052706852349615, 61.66721672131044585, -2.660933152496147258 ) ) ;
#13294=CARTESIAN_POINT ( 'NONE',  ( 79.52504771873113043, 64.52527500529804172, 3.543129918318852045 ) ) ;
#13301=CARTESIAN_POINT ( 'NONE',  ( -63.96695182803195934, 19.27020452292900288, 9.800414904976365804 ) ) ;
#13312=CARTESIAN_POINT ( 'NONE',  ( 78.67710717883703353, 66.04916176178687692, 1.122020883098625355 ) ) ;
#13321=CARTESIAN_POINT ( 'NONE',  ( 69.31827979293011310, 58.50063561948233115, 3.969490915146638876 ) ) ;
#13324=CARTESIAN_POINT ( 'NONE',  ( -64.08758708074093136, 43.28737448368270435, -1.986914326131290931 ) ) ;
#13328=CARTESIAN_POINT ( 'NONE',  ( 78.67160034737365493, 66.04525015085646089, -1.145133111591881026 ) ) ;
#13332=DIRECTION ( 'NONE',  ( -0.3103887796125159859, -0.9506097019758703581, 0.000000000000000000 ) ) ;
#13339=EDGE_CURVE ( 'NONE', #32211, #15032, #32932, .T. ) ;
#13342=CARTESIAN_POINT ( 'NONE',  ( 80.88543547514458965, 62.41573260227067976, -3.197674131580382717 ) ) ;
#13347=CARTESIAN_POINT ( 'NONE',  ( 80.51660522894103167, 65.82269567859330550, -2.502189764415934548 ) ) ;
#13353=CARTESIAN_POINT ( 'NONE',  ( -64.08758708073987975, 43.72986257717802516, -2.307254338139467897 ) ) ;
#13354=CARTESIAN_POINT ( 'NONE',  ( 70.80012018114213390, 59.83342440824694819, 3.954977122261609690 ) ) ;
#13362=CARTESIAN_POINT ( 'NONE',  ( 81.04289631908092417, 64.65011820513348084, 3.243459512806144307 ) ) ;
#13398=CARTESIAN_POINT ( 'NONE',  ( 82.29876416100408676, 62.79692783100093578, -1.831286414254867934 ) ) ;
#13400=EDGE_LOOP ( 'NONE', ( #40708, #6282, #22830 ) ) ;
#13401=CARTESIAN_POINT ( 'NONE',  ( 75.43741953989466253, 63.08613174173243010, -3.462570962765005866 ) ) ;
#13403=FACE_BOUND ( 'NONE', #20034, .T. ) ;
#13406=CARTESIAN_POINT ( 'NONE',  ( 76.63461511614542587, 62.03359853006617186, 3.872369636031695705 ) ) ;
#13411=CARTESIAN_POINT ( 'NONE',  ( 80.07729437284027085, 66.15382583937156369, 2.040045296073325520 ) ) ;
#13419=CARTESIAN_POINT ( 'NONE',  ( 71.53106143128088945, 58.56707856135989942, 3.757617741137792677 ) ) ;
#13423=LINE ( 'NONE', #4769, #14082 ) ;
#13433=CARTESIAN_POINT ( 'NONE',  ( 67.81915466200213416, 58.05084569011909679, -3.988165415173097195 ) ) ;
#13440=CARTESIAN_POINT ( 'NONE',  ( -64.08758708074093136, 37.43074634367857101, 3.182173495014448239 ) ) ;
#13448=VECTOR ( 'NONE', #18531, 1000.000000000000000 ) ;
#13449=CARTESIAN_POINT ( 'NONE',  ( 79.44789965344523353, 65.49939714349790165, 2.911438267503724475 ) ) ;
#13452=CARTESIAN_POINT ( 'NONE',  ( 78.28284693538141426, 65.31437991193503478, -2.608847861177645111 ) ) ;
#13456=CARTESIAN_POINT ( 'NONE',  ( 79.08571093829934284, 66.16712123189802242, -1.622497907168747089 ) ) ;
#13457=CARTESIAN_POINT ( 'NONE',  ( 79.08256350411643609, 63.89089281391859032, 3.718817779187653549 ) ) ;
#13458=FACE_OUTER_BOUND ( 'NONE', #37891, .T. ) ;
#13459=CARTESIAN_POINT ( 'NONE',  ( 80.02802368947529033, 66.35789156557528656, 1.168532795813725045 ) ) ;
#13460=CARTESIAN_POINT ( 'NONE',  ( -64.08758708074093136, 41.64119180492454575, 2.960472591334007753 ) ) ;
#13463=CARTESIAN_POINT ( 'NONE',  ( -64.17943696418035415, 35.01970154838168980, -4.761094547372056063 ) ) ;
#13486=CARTESIAN_POINT ( 'NONE',  ( 66.85348068378573316, 57.96691244536589238, 3.999524142431096330 ) ) ;
#13498=VERTEX_POINT ( 'NONE', #15819 ) ;
#13503=CARTESIAN_POINT ( 'NONE',  ( 78.57218090866955151, 65.76747258267620566, -2.123311106147462546 ) ) ;
#13505=CARTESIAN_POINT ( 'NONE',  ( 79.79878548311236841, 63.97024398824610358, 3.714073935154437844 ) ) ;
#13509=CARTESIAN_POINT ( 'NONE',  ( -80.92837670882107659, 2.429809908903242555, 12.50000000000000000 ) ) ;
#13516=CARTESIAN_POINT ( 'NONE',  ( 71.72449567874917875, 61.26021252176497001, -3.629688915602770294 ) ) ;
#13523=CARTESIAN_POINT ( 'NONE',  ( 78.78605531729427014, 66.08782950793387556, 1.450104216466330920 ) ) ;
#13534=CARTESIAN_POINT ( 'NONE',  ( 69.11491457486368972, 59.02763561571557460, 3.981537309218734055 ) ) ;
#13540=CARTESIAN_POINT ( 'NONE',  ( 79.58225024864499630, 65.28851876552752742, -3.146509185145911935 ) ) ;
#13543=CARTESIAN_POINT ( 'NONE',  ( -56.50908310466263629, 29.95896301100009040, 1.719924897558617438 ) ) ;
#13545=CARTESIAN_POINT ( 'NONE',  ( -60.14275962559869981, 24.84364830758654108, -9.154021781743367114 ) ) ;
#13549=CARTESIAN_POINT ( 'NONE',  ( 80.00358288781660576, 64.08847832824481827, -3.683925914261568124 ) ) ;
#13554=CARTESIAN_POINT ( 'NONE',  ( 81.37441939350041764, 61.42019823254031508, -1.301239782962684499 ) ) ;
#13560=CARTESIAN_POINT ( 'NONE',  ( -64.08758708074093136, 43.44355869127355163, -1.729337824599811668 ) ) ;
#13561=CARTESIAN_POINT ( 'NONE',  ( 72.50225525176000474, 58.97572275893025306, 3.745173303611597948 ) ) ;
#13571=CARTESIAN_POINT ( 'NONE',  ( 81.64588081866192226, 62.19174680641864228, 2.443770662203105459 ) ) ;
#13593=CARTESIAN_POINT ( 'NONE',  ( 66.27376694609004915, 57.73522568913436004, -4.000000000000000000 ) ) ;
#13598=CARTESIAN_POINT ( 'NONE',  ( -64.08758708074093136, 36.76569972833215161, -3.434863364314911571 ) ) ;
#13599=EDGE_LOOP ( 'NONE', ( #12382, #19797, #6000, #37955 ) ) ;
#13600=CARTESIAN_POINT ( 'NONE',  ( -56.05592576813389627, 30.85738657449433120, -3.898523360614985833 ) ) ;
#13602=ORIENTED_EDGE ( 'NONE', *, *, #4786, .T. ) ;
#13604=CARTESIAN_POINT ( 'NONE',  ( 81.49402754981267094, 65.64225023272284432, -1.838010297257802517 ) ) ;
#13605=EDGE_CURVE ( 'NONE', #11880, #22985, #18753, .T. ) ;
#13608=CARTESIAN_POINT ( 'NONE',  ( 76.31287196683634022, 61.24236878174163934, -3.825872951957620671 ) ) ;
#13612=CARTESIAN_POINT ( 'NONE',  ( 77.29397510068359622, 60.62518447217941997, 3.385286751607368139 ) ) ;
#13618=CARTESIAN_POINT ( 'NONE',  ( 81.41940809751211816, 61.44195378529070695, 1.227604746834739080 ) ) ;
#13643=CARTESIAN_POINT ( 'NONE',  ( 67.67991563464998706, 58.42724437289452055, -3.992148460412344502 ) ) ;
#13645=VECTOR ( 'NONE', #14363, 1000.000000000000000 ) ;
#13649=CARTESIAN_POINT ( 'NONE',  ( -60.14275962559869981, 24.84364830758654108, 9.154021781743367114 ) ) ;
#13659=CARTESIAN_POINT ( 'NONE',  ( 80.79424907316142423, 63.37012793878832184, 3.540619799101252685 ) ) ;
#13662=CARTESIAN_POINT ( 'NONE',  ( 79.66869450427640231, 60.77384974161335407, -2.178915381671177265 ) ) ;
#13665=CARTESIAN_POINT ( 'NONE',  ( 81.48104477345277985, 62.99720032632139066, -3.089171411835851089 ) ) ;
#13666=CARTESIAN_POINT ( 'NONE',  ( 80.45616750117871163, 61.42990784962029949, 2.551437666014049199 ) ) ;
#13670=CARTESIAN_POINT ( 'NONE',  ( 81.74784679736075077, 61.69507302169112251, 1.045691535380373960 ) ) ;
#13675=CARTESIAN_POINT ( 'NONE',  ( -64.44214806826670383, 36.58397470404546681, -5.707342493246947868 ) ) ;
#13689=CYLINDRICAL_SURFACE ( 'NONE', #29927, 3.873277249845555215 ) ;
#13695=CARTESIAN_POINT ( 'NONE',  ( 66.90457105084450973, 57.82508126828634687, 3.996770903026528821 ) ) ;
#13696=CARTESIAN_POINT ( 'NONE',  ( -64.08758708074093136, 38.27681294190825412, 4.090925416972679862 ) ) ;
#13700=( BOUNDED_CURVE ( )  B_SPLINE_CURVE ( 3, ( #6510, #9168, #2620, #18427 ),
 .UNSPECIFIED., .F., .T. ) 
 B_SPLINE_CURVE_WITH_KNOTS ( ( 4, 4 ),
 ( 0.6656944266037794211, 1.570796326794896558 ),
 .UNSPECIFIED. ) 
 CURVE ( )  GEOMETRIC_REPRESENTATION_ITEM ( )  RATIONAL_B_SPLINE_CURVE ( ( 1.000000000000000000, 0.9328897322841716022, 0.9328897322841716022, 1.000000000000000000 ) ) 
 REPRESENTATION_ITEM ( '' )  );
#13701=ORIENTED_EDGE ( 'NONE', *, *, #14864, .F. ) ;
#13711=CARTESIAN_POINT ( 'NONE',  ( 78.47952394835841972, 65.90892955575903045, -1.487544896896269897 ) ) ;
#13714=CARTESIAN_POINT ( 'NONE',  ( 80.68879072954337062, 62.10584950744630106, 3.070011659370367241 ) ) ;
#13715=DIRECTION ( 'NONE',  ( -1.000000000000000000, 0.000000000000000000, 0.000000000000000000 ) ) ;
#13716=CIRCLE ( 'NONE', #1245, 2.681419499219045655 ) ;
#13723=CARTESIAN_POINT ( 'NONE',  ( 78.67055650824026714, 66.04450565822685348, -1.166185623126624993 ) ) ;
#13733=CARTESIAN_POINT ( 'NONE',  ( 79.17166177841365027, 65.86836750419900000, 2.393593008231245545 ) ) ;
#13742=CARTESIAN_POINT ( 'NONE',  ( -63.96695182803194513, 19.27020452292901709, -8.800414904976364028 ) ) ;
#13743=CARTESIAN_POINT ( 'NONE',  ( 69.39861229970156842, 58.29198505329483027, 3.933428174212719952 ) ) ;
#13748=CARTESIAN_POINT ( 'NONE',  ( 81.15585419290073332, 61.98190721255070201, -2.710038060602454113 ) ) ;
#13758=CARTESIAN_POINT ( 'NONE',  ( 80.84665409946079251, 62.14681778383292254, -3.018898740118487911 ) ) ;
#13759=CARTESIAN_POINT ( 'NONE',  ( -64.08758708074091714, 24.84364830758654108, -8.800414904976364028 ) ) ;
#13760=CARTESIAN_POINT ( 'NONE',  ( 81.10356443252399572, 61.32192396066507456, 1.621665796799052206 ) ) ;
#13764=CARTESIAN_POINT ( 'NONE',  ( -58.38231031521774383, 29.55838692813951951, -4.971618182862113322 ) ) ;
#13778=CARTESIAN_POINT ( 'NONE',  ( 81.12957769509937123, 64.69578868775874980, 3.179853676208927560 ) ) ;
#13786=CARTESIAN_POINT ( 'NONE',  ( -63.06901714727342068, 38.60153782280264778, 3.999999999999999112 ) ) ;
#13801=VECTOR ( 'NONE', #11450, 1000.000000000000000 ) ;
#13810=CARTESIAN_POINT ( 'NONE',  ( 78.69020857030078275, 66.05846869611056604, -1.014334479594670713 ) ) ;
#13816=CARTESIAN_POINT ( 'NONE',  ( 78.03839322897110264, 60.52053993360658524, 3.012346708730509803 ) ) ;
#13819=CARTESIAN_POINT ( 'NONE',  ( -11.81496944966682960, -21.25669541281728669, 4.000000000000000000 ) ) ;
#13823=CARTESIAN_POINT ( 'NONE',  ( -62.84805993229080912, 35.59861336795816555, 5.826615769580637760 ) ) ;
#13825=CARTESIAN_POINT ( 'NONE',  ( 81.24150567074694607, 65.50891479330012146, 2.400449347018090318 ) ) ;
#13826=CARTESIAN_POINT ( 'NONE',  ( -64.08758708074094557, 43.59044912938107075, 1.299988725261512545 ) ) ;
#13840=AXIS2_PLACEMENT_3D ( 'NONE', #7206, #19765, #13182 ) ;
#13841=ORIENTED_EDGE ( 'NONE', *, *, #13339, .T. ) ;
#13844=CARTESIAN_POINT ( 'NONE',  ( 67.16623404331231484, 58.01883467879599721, -3.998868826385353348 ) ) ;
#13860=CARTESIAN_POINT ( 'NONE',  ( 81.20569604368299110, 61.99964894245921698, 2.688322534164198085 ) ) ;
#13861=CARTESIAN_POINT ( 'NONE',  ( -63.70319261593226656, 44.37193174353182457, 1.420345578797184150 ) ) ;
#13863=CARTESIAN_POINT ( 'NONE',  ( 78.69960226590261243, 64.59913094042720161, -3.401284978681007320 ) ) ;
#13866=CARTESIAN_POINT ( 'NONE',  ( 81.30751890105065627, 61.38951540425596676, -1.382728580142338570 ) ) ;
#13867=CARTESIAN_POINT ( 'NONE',  ( 78.36941018910007983, 65.17477963226572513, 2.845586111146954700 ) ) ;
#13871=CARTESIAN_POINT ( 'NONE',  ( 80.01568814228021154, 66.35127795588812205, 1.246975333546937126 ) ) ;
#13874=CARTESIAN_POINT ( 'NONE',  ( -64.08758708074093136, 36.14363715547680300, -3.800414904976362696 ) ) ;
#13888=AXIS2_PLACEMENT_3D ( 'NONE', #10886, #4141, #38689 ) ;
#13889=ADVANCED_FACE ( 'NONE', ( #5274 ), #17815, .T. ) ;
#13892=ORIENTED_EDGE ( 'NONE', *, *, #6816, .F. ) ;
#13894=CARTESIAN_POINT ( 'NONE',  ( 66.43187891275407253, 57.76301247919355575, 4.000000000000005329 ) ) ;
#13895=CARTESIAN_POINT ( 'NONE',  ( 71.16717283274410022, 58.92450812456241493, -3.908768822720080305 ) ) ;
#13905=CARTESIAN_POINT ( 'NONE',  ( 78.99843287308405593, 65.13824187233505825, -3.101774481621350610 ) ) ;
#13907=CARTESIAN_POINT ( 'NONE',  ( 79.97265554093038986, 63.70311272660544688, 3.710743084827281546 ) ) ;
#13908=DIRECTION ( 'NONE',  ( 0.8831583674551010121, -0.4690749385695646700, 0.000000000000000000 ) ) ;
#13921=CARTESIAN_POINT ( 'NONE',  ( 81.28781607649123941, 61.48165154268892252, 1.786209778413323734 ) ) ;
#13931=CARTESIAN_POINT ( 'NONE',  ( 68.53436546801150087, 58.80600050245282517, 3.985059344218149668 ) ) ;
#13935=LINE ( 'NONE', #1403, #1706 ) ;
#13937=ADVANCED_FACE ( 'NONE', ( #31220 ), #9371, .F. ) ;
#13938=CARTESIAN_POINT ( 'NONE',  ( 78.65282594500106939, 66.03191569515874448, -1.205449537698850326 ) ) ;
#13944=LINE ( 'NONE', #26514, #18125 ) ;
#13949=EDGE_LOOP ( 'NONE', ( #40654, #8608, #34150, #8824 ) ) ;
#13951=CARTESIAN_POINT ( 'NONE',  ( 79.49051211673854311, 64.87125159350625836, -3.403428918328330610 ) ) ;
#13953=CARTESIAN_POINT ( 'NONE',  ( 80.20530801487242911, 63.82446735998111365, 3.674973878998263999 ) ) ;
#13957=CARTESIAN_POINT ( 'NONE',  ( -56.74920310314012539, 30.60922821844966180, -3.177981099252243258 ) ) ;
#13960=CARTESIAN_POINT ( 'NONE',  ( -64.08758708074093136, 43.62247136636499079, -2.470836091660580713 ) ) ;
#13969=CARTESIAN_POINT ( 'NONE',  ( 81.43955525001683782, 63.33353925139297047, 3.171364025132952680 ) ) ;
#13984=ORIENTED_EDGE ( 'NONE', *, *, #19443, .T. ) ;
#13991=ORIENTED_EDGE ( 'NONE', *, *, #34802, .T. ) ;
#13994=CARTESIAN_POINT ( 'NONE',  ( -56.11355572853777574, 30.33753280151830367, -1.575778306538754725 ) ) ;
#14000=CARTESIAN_POINT ( 'NONE',  ( 82.39441792515134466, 64.18328374515905921, -1.882325606869287515 ) ) ;
#14006=CARTESIAN_POINT ( 'NONE',  ( 74.86608108239484238, 61.39286988729297434, 3.912919437578932236 ) ) ;
#14007=CIRCLE ( 'NONE', #21249, 114.6618724293813898 ) ;
#14009=CARTESIAN_POINT ( 'NONE',  ( -64.08758708074093136, 36.43951107221849384, 3.602717568031709394 ) ) ;
#14014=CARTESIAN_POINT ( 'NONE',  ( 81.16729622508351838, 61.30314466175459387, 1.045986116561637314 ) ) ;
#14026=CARTESIAN_POINT ( 'NONE',  ( -63.70768058868311812, 44.39675795731059793, -1.000000000000000000 ) ) ;
#14033=CARTESIAN_POINT ( 'NONE',  ( 67.70975997764571730, 58.34660981014267378, -3.996132678073276878 ) ) ;
#14047=CARTESIAN_POINT ( 'NONE',  ( 78.64903117394807452, 66.02922079195218430, 1.215327096190495615 ) ) ;
#14048=AXIS2_PLACEMENT_3D ( 'NONE', #7008, #29243, #26161 ) ;
#14051=CARTESIAN_POINT ( 'NONE',  ( 78.82422632494606773, 64.37263203041347026, -3.536670452273165566 ) ) ;
#14054=CARTESIAN_POINT ( 'NONE',  ( 80.08603431819594221, 65.58772839307371783, -2.892908819258016795 ) ) ;
#14055=CARTESIAN_POINT ( 'NONE',  ( 79.45360044721715553, 62.79974527947165797, 3.729426069516725395 ) ) ;
#14058=CARTESIAN_POINT ( 'NONE',  ( 78.69036185089561286, 66.05857758962513060, 1.005837412005772036 ) ) ;
#14062=CARTESIAN_POINT ( 'NONE',  ( -63.58520484588292732, 35.72026407271199133, -6.999999999999995559 ) ) ;
#14074=DIRECTION ( 'NONE',  ( 1.000000000000000000, 0.000000000000000000, 0.000000000000000000 ) ) ;
#14080=CARTESIAN_POINT ( 'NONE',  ( 66.27376694608996388, 57.73522568913447373, 4.000000000000000000 ) ) ;
#14081=CARTESIAN_POINT ( 'NONE',  ( 71.87019205445125181, 60.48965333507749165, -3.909340765870004564 ) ) ;
#14082=VECTOR ( 'NONE', #1695, 1000.000000000000000 ) ;
#14086=EDGE_CURVE ( 'NONE', #36353, #35702, #29318, .T. ) ;
#14094=CARTESIAN_POINT ( 'NONE',  ( 79.03665253560640735, 65.17130141867492910, -3.087291694836853395 ) ) ;
#14097=CARTESIAN_POINT ( 'NONE',  ( 79.37660656468254672, 64.78470313322952734, 3.432573985763631708 ) ) ;
#14107=CARTESIAN_POINT ( 'NONE',  ( 77.73210138736416752, 65.38047884209385074, -2.040462881234939907 ) ) ;
#14113=CARTESIAN_POINT ( 'NONE',  ( 80.70080623961233357, 63.70112813535636320, 3.588566286536278849 ) ) ;
#14125=CARTESIAN_POINT ( 'NONE',  ( 68.11537257328342321, 58.15040817571434673, 3.985705108533863505 ) ) ;
#14128=CARTESIAN_POINT ( 'NONE',  ( -64.08758708074093136, 42.48851732804387638, -2.660621167144407995 ) ) ;
#14131=CARTESIAN_POINT ( 'NONE',  ( 78.73074668855629454, 66.04592173387707987, -1.531260274641971675 ) ) ;
#14135=CARTESIAN_POINT ( 'NONE',  ( -59.46024017484869972, 26.94883531126005849, 5.502890977078418011 ) ) ;
#14145=CARTESIAN_POINT ( 'NONE',  ( 79.09343976728325742, 65.54176476638896531, -2.787474064117370975 ) ) ;
#14147=CARTESIAN_POINT ( 'NONE',  ( 79.73292928667240176, 64.66788176856890402, 3.497296750721718084 ) ) ;
#14168=CARTESIAN_POINT ( 'NONE',  ( 80.08603431818187346, 65.58772839306588764, 2.892908819267548282 ) ) ;
#14174=AXIS2_PLACEMENT_3D ( 'NONE', #8967, #21964, #5902 ) ;
#14190=CARTESIAN_POINT ( 'NONE',  ( 66.27376694609004915, 57.73522568913436004, -4.000000000000000000 ) ) ;
#14193=CIRCLE ( 'NONE', #12885, 0.9999999999999998890 ) ;
#14199=EDGE_LOOP ( 'NONE', ( #6405, #24662, #11389, #2189 ) ) ;
#14202=CARTESIAN_POINT ( 'NONE',  ( 81.41940809751206132, 61.44195378529067852, -1.227604746834842553 ) ) ;
#14204=VERTEX_POINT ( 'NONE', #6557 ) ;
#14208=CARTESIAN_POINT ( 'NONE',  ( 75.63732367802946044, 59.67466586216193036, 3.300071129360657718 ) ) ;
#14213=DIRECTION ( 'NONE',  ( -0.000000000000000000, -0.000000000000000000, -1.000000000000000000 ) ) ;
#14214=DIRECTION ( 'NONE',  ( 0.000000000000000000, 0.000000000000000000, -1.000000000000000000 ) ) ;
#14216=CARTESIAN_POINT ( 'NONE',  ( 81.23963933823235095, 65.14454330635810209, 2.817575383041586168 ) ) ;
#14222=EDGE_CURVE ( 'NONE', #38011, #18554, #29455, .T. ) ;
#14225=CARTESIAN_POINT ( 'NONE',  ( -81.07947155388370675, 30.81399289130170871, -9.800414904976365804 ) ) ;
#14226=ADVANCED_FACE ( 'NONE', ( #15812 ), #31671, .T. ) ;
#14236=CARTESIAN_POINT ( 'NONE',  ( 67.44728384595320847, 58.15801736331750504, -3.998402061830689025 ) ) ;
#14241=CARTESIAN_POINT ( 'NONE',  ( 78.42699581646675711, 65.87166649608005287, 1.555834701912668150 ) ) ;
#14248=CARTESIAN_POINT ( 'NONE',  ( 81.15585419290071911, 61.98190721255070201, 2.710038060602456778 ) ) ;
#14252=CARTESIAN_POINT ( 'NONE',  ( 78.04063183619210520, 64.12728436294460721, -3.505091495581006189 ) ) ;
#14256=CARTESIAN_POINT ( 'NONE',  ( 81.40528610411905674, 61.52959015154601019, -1.692865493181702430 ) ) ;
#14257=CARTESIAN_POINT ( 'NONE',  ( 79.57354641881573798, 61.78191946445392801, 3.317372267376139217 ) ) ;
#14262=CARTESIAN_POINT ( 'NONE',  ( 82.38651420471397557, 62.84168609110421500, 1.553473047276233476 ) ) ;
#14265=CARTESIAN_POINT ( 'NONE',  ( -64.37872067649583130, 36.58503142451505141, -5.660009492437820811 ) ) ;
#14266=ORIENTED_EDGE ( 'NONE', *, *, #11598, .T. ) ;
#14278=DIRECTION ( 'NONE',  ( 1.000000000000000000, 0.000000000000000000, 0.000000000000000000 ) ) ;
#14284=CARTESIAN_POINT ( 'NONE',  ( 66.27376694608996388, 57.73522568913447373, 4.000000000000000000 ) ) ;
#14286=CARTESIAN_POINT ( 'NONE',  ( 71.91282362819097784, 60.38839763785598080, -3.929231508849751364 ) ) ;
#14290=CARTESIAN_POINT ( 'NONE',  ( -60.36144324275490902, 24.84364830758653397, 8.926047827505314558 ) ) ;
#14294=FACE_OUTER_BOUND ( 'NONE', #14586, .T. ) ;
#14298=CARTESIAN_POINT ( 'NONE',  ( 79.98243830041433000, 63.02105934045280833, -3.686141857899485341 ) ) ;
#14300=CARTESIAN_POINT ( 'NONE',  ( 79.93741260258519787, 63.33597468792986973, 3.730195463674649048 ) ) ;
#14316=CARTESIAN_POINT ( 'NONE',  ( 81.32346312764153140, 61.65804850752792987, 2.069468987430086226 ) ) ;
#14325=CARTESIAN_POINT ( 'NONE',  ( 68.01940210501214779, 58.40717514567135282, 3.996230182412886744 ) ) ;
#14330=CARTESIAN_POINT ( 'NONE',  ( 78.84693035237090442, 66.01116107573028557, -1.842213953838235163 ) ) ;
#14333=EDGE_CURVE ( 'NONE', #12043, #32308, #21634, .T. ) ;
#14334=CARTESIAN_POINT ( 'NONE',  ( -58.78362175692702607, 29.48419490076549465, 5.741263644839468938 ) ) ;
#14339=CARTESIAN_POINT ( 'NONE',  ( 78.79145472225366120, 65.75511795602321286, -2.294512580621462572 ) ) ;
#14341=LINE ( 'NONE', #11244, #29923 ) ;
#14343=CARTESIAN_POINT ( 'NONE',  ( 78.58771539371637971, 65.98568759316006549, 1.340350474428749106 ) ) ;
#14348=CARTESIAN_POINT ( 'NONE',  ( 75.40715271138134312, 60.19559828969859439, -3.661998389317127511 ) ) ;
#14351=CIRCLE ( 'NONE', #18296, 117.6618724293813898 ) ;
#14357=ORIENTED_EDGE ( 'NONE', *, *, #3948, .T. ) ;
#14363=DIRECTION ( 'NONE',  ( 0.000000000000000000, 0.000000000000000000, 1.000000000000000000 ) ) ;
#14364=CARTESIAN_POINT ( 'NONE',  ( 81.34875679478896870, 63.64560584540186738, 3.283621700565935164 ) ) ;
#14376=ORIENTED_EDGE ( 'NONE', *, *, #29231, .T. ) ;
#14390=EDGE_CURVE ( 'NONE', #28218, #33723, #35576, .T. ) ;
#14401=CARTESIAN_POINT ( 'NONE',  ( 79.56604632444070546, 66.26916991809633828, -1.539394129974356096 ) ) ;
#14403=DIRECTION ( 'NONE',  ( -0.000000000000000000, -0.000000000000000000, -1.000000000000000000 ) ) ;
#14409=CARTESIAN_POINT ( 'NONE',  ( 73.86803306573551708, 62.08347648694397947, 3.642458757454824614 ) ) ;
#14416=CARTESIAN_POINT ( 'NONE',  ( -62.77989223203980629, 36.45919279222904663, 4.734733336003105642 ) ) ;
#14418=CARTESIAN_POINT ( 'NONE',  ( 81.87949262442930376, 63.91736224575979008, 2.817575383041585724 ) ) ;
#14427=CARTESIAN_POINT ( 'NONE',  ( -75.45330471031414277, 33.71485196875532608, -8.800414904976364028 ) ) ;
#14434=CARTESIAN_POINT ( 'NONE',  ( 67.18992292689074475, 57.95373832061253694, -3.997022163556062324 ) ) ;
#14448=CARTESIAN_POINT ( 'NONE',  ( 82.43037228308448050, 64.59322875725442259, -1.165579324820864571 ) ) ;
#14449=CARTESIAN_POINT ( 'NONE',  ( 80.83425215363003247, 63.04220640063321213, 3.443978770203983242 ) ) ;
#14453=CARTESIAN_POINT ( 'NONE',  ( 77.50572060368776306, 65.09508644891813844, -2.418543376929283450 ) ) ;
#14456=CARTESIAN_POINT ( 'NONE',  ( 81.34308989086048314, 63.28542802927258748, -3.228380831070265078 ) ) ;
#14457=CARTESIAN_POINT ( 'NONE',  ( 78.04063183619207678, 64.12728436294460721, 3.505091495581009298 ) ) ;
#14460=CARTESIAN_POINT ( 'NONE',  ( 81.16936534046872964, 61.30390240240431865, 1.014334479594651173 ) ) ;
#14464=DIRECTION ( 'NONE',  ( 1.000000000000000000, 0.000000000000000000, -0.000000000000000000 ) ) ;
#14471=AXIS2_PLACEMENT_3D ( 'NONE', #9268, #22268, #647 ) ;
#14482=APPLICATION_CONTEXT ( 'automotive_design' ) ;
#14485=CARTESIAN_POINT ( 'NONE',  ( 66.41901733680195719, 57.79934748174507320, 4.000000000000016875 ) ) ;
#14486=CARTESIAN_POINT ( 'NONE',  ( 72.57946960881442067, 58.78899945845352448, -3.647993048395011595 ) ) ;
#14491=CARTESIAN_POINT ( 'NONE',  ( -54.79610818216033152, 31.51396769785350926, 4.000000000000000000 ) ) ;
#14498=CARTESIAN_POINT ( 'NONE',  ( -59.01947560891952804, 27.90920910948504385, -6.147301388271595890 ) ) ;
#14499=AXIS2_PLACEMENT_3D ( 'NONE', #16111, #9932, #6454 ) ;
#14501=CARTESIAN_POINT ( 'NONE',  ( 78.72519613238203817, 65.48187369539458302, -2.679976076788564754 ) ) ;
#14503=CARTESIAN_POINT ( 'NONE',  ( 80.62899510017081184, 61.84672251665477205, 2.918211652848217152 ) ) ;
#14516=CARTESIAN_POINT ( 'NONE',  ( 79.33528816075222778, 65.72664079943768911, 2.661900242191239219 ) ) ;
#14517=DIRECTION ( 'NONE',  ( -0.000000000000000000, 1.000000000000000000, 0.000000000000000000 ) ) ;
#14527=CARTESIAN_POINT ( 'NONE',  ( 68.10340323693496600, 58.18244674706191688, 3.988335407916730802 ) ) ;
#14533=CARTESIAN_POINT ( 'NONE',  ( -58.25352014915284826, 31.25337030895682133, 4.614317915849918350 ) ) ;
#14538=CARTESIAN_POINT ( 'NONE',  ( 78.93661819519692813, 65.67810670493901171, -2.545842637937977937 ) ) ;
#14540=CARTESIAN_POINT ( 'NONE',  ( 80.84665409946110515, 62.14681778383299360, 3.018898740118469703 ) ) ;
#14545=CARTESIAN_POINT ( 'NONE',  ( 73.97359482965943300, 60.32890003735500528, -3.899931323540655637 ) ) ;
#14577=ORIENTED_EDGE ( 'NONE', *, *, #30439, .T. ) ;
#14586=EDGE_LOOP ( 'NONE', ( #35372, #4933, #35427, #39316 ) ) ;
#14589=CARTESIAN_POINT ( 'NONE',  ( 79.70553327529583498, 65.02082924290299104, -3.340002271463676120 ) ) ;
#14596=CARTESIAN_POINT ( 'NONE',  ( 81.24150567074659079, 65.50891479329992251, -2.400449347018692059 ) ) ;
#14597=CARTESIAN_POINT ( 'NONE',  ( -59.00782325774520132, 28.07066389825120822, 6.403654028263575881 ) ) ;
#14601=CARTESIAN_POINT ( 'NONE',  ( 75.27660179239936156, 61.98686977074611804, 3.846775394605563836 ) ) ;
#14608=CARTESIAN_POINT ( 'NONE',  ( -62.88953457012820536, 35.56785342129472838, 5.946384872131353916 ) ) ;
#14610=CARTESIAN_POINT ( 'NONE',  ( 81.51784234612475188, 64.89972252180031376, 2.776691787112188337 ) ) ;
#14630=CARTESIAN_POINT ( 'NONE',  ( 66.72049918463439155, 57.87600310258397940, -3.999713739232678034 ) ) ;
#14643=CARTESIAN_POINT ( 'NONE',  ( 82.25590015743732408, 64.89408798057370120, -1.328060019258380242 ) ) ;
#14644=CARTESIAN_POINT ( 'NONE',  ( 80.04018988431747061, 64.49293993294402583, 3.578839808218922780 ) ) ;
#14648=CARTESIAN_POINT ( 'NONE',  ( 79.26824131213432167, 60.90178692369111957, -2.725046208697020855 ) ) ;
#14651=CARTESIAN_POINT ( 'NONE',  ( 78.82533416220574907, 66.11379887182106074, -1.400336002810711244 ) ) ;
#14652=CARTESIAN_POINT ( 'NONE',  ( 79.75127500915171197, 61.39906162938306977, 2.976941560848460178 ) ) ;
#14657=CARTESIAN_POINT ( 'NONE',  ( 82.16824647341044852, 62.22308028923548306, 1.246975333546937348 ) ) ;
#14661=CARTESIAN_POINT ( 'NONE',  ( -1.432293644835494373, -27.47664038617742577, -4.000000000000000000 ) ) ;
#14666=EDGE_CURVE ( 'NONE', #29368, #1666, #8955, .T. ) ;
#14679=EDGE_CURVE ( 'NONE', #1666, #30327, #14193, .T. ) ;
#14685=CARTESIAN_POINT ( 'NONE',  ( 66.42594280077616986, 57.77978248037118192, 4.000000000000010658 ) ) ;
#14686=CARTESIAN_POINT ( 'NONE',  ( 69.31827979293011310, 58.50063561948233115, -3.969490915146639765 ) ) ;
#14696=CARTESIAN_POINT ( 'NONE',  ( 17.04338035915418459, 48.81061067247630092, -1.000000000000000000 ) ) ;
#14698=CARTESIAN_POINT ( 'NONE',  ( 79.36500080098822707, 64.41263654525117488, -3.571698303486884107 ) ) ;
#14700=CARTESIAN_POINT ( 'NONE',  ( 81.90837201943155321, 62.87926165960869440, -2.626729253126907526 ) ) ;
#14701=CARTESIAN_POINT ( 'NONE',  ( 80.53991883815837127, 62.31343731104875872, 3.289664858626286659 ) ) ;
#14712=CARTESIAN_POINT ( 'NONE',  ( -59.93345510331043613, 24.73247967741477993, 9.800414904976365804 ) ) ;
#14727=CARTESIAN_POINT ( 'NONE',  ( 68.13924211849639789, 58.08649371134929140, 3.978477839347963840 ) ) ;
#14741=ORIENTED_EDGE ( 'NONE', *, *, #12021, .F. ) ;
#14742=CARTESIAN_POINT ( 'NONE',  ( 80.93309715666640614, 61.70751139687529019, -2.576318598473983368 ) ) ;
#14745=CARTESIAN_POINT ( 'NONE',  ( 79.37669412903255761, 65.14038507876448136, 3.220356845321968198 ) ) ;
#14749=CARTESIAN_POINT ( 'NONE',  ( -2.954197855305039422, -12.43481156997016157, -4.000000000000000000 ) ) ;
#14750=CARTESIAN_POINT ( 'NONE',  ( 73.81116006253010653, 62.20691382096257627, -3.564124015814260638 ) ) ;
#14753=CARTESIAN_POINT ( 'NONE',  ( -57.21827861686057304, 30.45169051924667514, -3.625703664980399754 ) ) ;
#14765=CARTESIAN_POINT ( 'NONE',  ( 81.16204935228437023, 61.30122352005683695, 1.083735637653854722 ) ) ;
#14786=CARTESIAN_POINT ( 'NONE',  ( 80.61469348477538688, 64.03810969304559819, -3.562450064734663524 ) ) ;
#14795=CARTESIAN_POINT ( 'NONE',  ( 80.91556171499746597, 62.42588715431494961, -3.188730975143399871 ) ) ;
#14797=DIRECTION ( 'NONE',  ( -0.000000000000000000, -0.000000000000000000, -1.000000000000000000 ) ) ;
#14803=CARTESIAN_POINT ( 'NONE',  ( 81.16877391194421421, 61.30368580354083008, -1.027726681410897625 ) ) ;
#14810=CARTESIAN_POINT ( 'NONE',  ( 75.07588875331117606, 60.93231399735385878, 3.896954863271551162 ) ) ;
#14820=CARTESIAN_POINT ( 'NONE',  ( 81.98790212893285911, 62.35967063417187717, 2.110636331688407807 ) ) ;
#14824=DIRECTION ( 'NONE',  ( -0.000000000000000000, -0.000000000000000000, -1.000000000000000000 ) ) ;
#14831=DIRECTION ( 'NONE',  ( -0.000000000000000000, -0.000000000000000000, 1.000000000000000000 ) ) ;
#14838=CARTESIAN_POINT ( 'NONE',  ( 66.97346358352143625, 58.09330026553017490, -3.997553359131193584 ) ) ;
#14845=CARTESIAN_POINT ( 'NONE',  ( 76.46985044344074822, 64.49630587417807703, 2.565399245510498361 ) ) ;
#14852=CARTESIAN_POINT ( 'NONE',  ( 82.18775271763095702, 62.23297483488567394, -1.085061034363232979 ) ) ;
#14853=CARTESIAN_POINT ( 'NONE',  ( 79.79114114151838066, 64.70569453017795070, 3.482375488376185935 ) ) ;
#14856=CARTESIAN_POINT ( 'NONE',  ( 77.88532341798189407, 63.74564772441265603, -3.640295653904956907 ) ) ;
#14861=CARTESIAN_POINT ( 'NONE',  ( 79.58537830806109525, 65.88021587146388924, -2.518708746843062229 ) ) ;
#14862=CARTESIAN_POINT ( 'NONE',  ( 77.90798433017856439, 65.01733068894688472, 2.764360460937555164 ) ) ;
#14864=EDGE_CURVE ( 'NONE', #30246, #7186, #15346, .T. ) ;
#14866=CARTESIAN_POINT ( 'NONE',  ( 78.99269976270093707, 66.20980237122186907, 1.093381982072756164 ) ) ;
#14867=DIRECTION ( 'NONE',  ( -0.000000000000000000, -0.000000000000000000, 1.000000000000000000 ) ) ;
#14896=CARTESIAN_POINT ( 'NONE',  ( 69.84993430378905543, 58.85661355152254970, -3.977789803233258148 ) ) ;
#14901=LINE ( 'NONE', #14491, #23245 ) ;
#14908=EDGE_CURVE ( 'NONE', #12529, #34454, #940, .T. ) ;
#14917=CARTESIAN_POINT ( 'NONE',  ( 78.54017873204453792, 65.73972836631979533, -2.148686496494745857 ) ) ;
#14919=CARTESIAN_POINT ( 'NONE',  ( 81.81758241818907607, 62.27516227682815497, -2.299173245602590399 ) ) ;
#14920=CARTESIAN_POINT ( 'NONE',  ( 78.49831277043062983, 65.85142261852138290, 1.827177995460262716 ) ) ;
#14944=CARTESIAN_POINT ( 'NONE',  ( 67.84886183593677345, 57.97047572268562021, 3.979762160777300828 ) ) ;
#14960=CARTESIAN_POINT ( 'NONE',  ( 79.92041472187213458, 64.04075560556069036, -3.697630003121160858 ) ) ;
#14964=CARTESIAN_POINT ( 'NONE',  ( 79.03702048636715460, 65.49184929578454728, 2.818206040476803231 ) ) ;
#14970=CARTESIAN_POINT ( 'NONE',  ( 73.70000790436553473, 62.44749314232891635, -3.395557233589456381 ) ) ;
#14978=EDGE_LOOP ( 'NONE', ( #15735, #34718, #7477, #2061, #21652, #12091 ) ) ;
#14983=CARTESIAN_POINT ( 'NONE',  ( 80.32731820217895802, 65.01876230294769243, 3.279590910093583389 ) ) ;
#14993=CYLINDRICAL_SURFACE ( 'NONE', #38565, 79.54614097552274643 ) ;
#15000=CARTESIAN_POINT ( 'NONE',  ( 79.39921707337093437, 65.76781561079134519, -2.628317182735761204 ) ) ;
#15010=CARTESIAN_POINT ( 'NONE',  ( 78.64903117394807452, 66.02922079195218430, -1.215327096190493616 ) ) ;
#15012=CARTESIAN_POINT ( 'NONE',  ( -58.76908243668979281, 27.83904476269671235, -5.922484465878603999 ) ) ;
#15015=ORIENTED_EDGE ( 'NONE', *, *, #1494, .T. ) ;
#15016=CARTESIAN_POINT ( 'NONE',  ( 78.97185648144787251, 66.19841638340299994, -1.173033592341553355 ) ) ;
#15024=CARTESIAN_POINT ( 'NONE',  ( 74.08781496033066105, 60.06802034872734453, 3.841642203975295544 ) ) ;
#15030=ORIENTED_EDGE ( 'NONE', *, *, #14666, .T. ) ;
#15032=VERTEX_POINT ( 'NONE', #26847 ) ;
#15033=CARTESIAN_POINT ( 'NONE',  ( 79.63061436091763312, 66.14207560456347323, 2.046910133536372634 ) ) ;
#15050=DIRECTION ( 'NONE',  ( -0.000000000000000000, -0.000000000000000000, -1.000000000000000000 ) ) ;
#15051=CARTESIAN_POINT ( 'NONE',  ( 67.03255446809592399, 57.93006272621622088, -3.998453671246410934 ) ) ;
#15053=CARTESIAN_POINT ( 'NONE',  ( -62.81463675898083210, 36.67811266762162603, 4.600311178732273021 ) ) ;
#15064=CARTESIAN_POINT ( 'NONE',  ( 81.04763707098177861, 66.10603528134693363, -1.000000000000000000 ) ) ;
#15065=CARTESIAN_POINT ( 'NONE',  ( 79.66028364141931206, 64.99138685963063722, 3.354617312347331293 ) ) ;
#15070=CARTESIAN_POINT ( 'NONE',  ( 75.95345872531814280, 63.43160129075363329, -3.385286751594662746 ) ) ;
#15073=CARTESIAN_POINT ( 'NONE',  ( 78.97265649164266677, 66.09949689503568493, -1.726519205788536571 ) ) ;
#15074=CARTESIAN_POINT ( 'NONE',  ( 79.44050761702634134, 61.30339496468049987, 3.042889847487580290 ) ) ;
#15077=CARTESIAN_POINT ( 'NONE',  ( 78.98807859296744027, 66.20728402696082071, 1.114595100209202494 ) ) ;
#15083=CARTESIAN_POINT ( 'NONE',  ( -62.83712641625182016, 35.61106514070144868, 5.789832448495932482 ) ) ;
#15095=DIRECTION ( 'NONE',  ( -1.000000000000000000, -1.038556294491206740E-15, 0.000000000000000000 ) ) ;
#15098=CARTESIAN_POINT ( 'NONE',  ( -64.08758708074093136, 36.43951107222060415, -3.602717568033520834 ) ) ;
#15104=CARTESIAN_POINT ( 'NONE',  ( 70.53871541878200446, 60.47550293342311534, -3.775670717450619218 ) ) ;
#15110=CARTESIAN_POINT ( 'NONE',  ( 70.06771224146353916, 58.30163689823704942, 3.863726395435713723 ) ) ;
#15121=CARTESIAN_POINT ( 'NONE',  ( 78.43571320973860850, 65.80086540191352640, -1.884339924308604086 ) ) ;
#15123=CARTESIAN_POINT ( 'NONE',  ( 81.56442676284295601, 64.14391357695993179, -3.071899782094856590 ) ) ;
#15124=CARTESIAN_POINT ( 'NONE',  ( 80.72570547868225788, 61.86964107431865045, 2.884918531047036439 ) ) ;
#15141=B_SPLINE_CURVE_WITH_KNOTS ( 'NONE', 3,
 ( #20112, #17011, #29587, #16419, #35391, #13324, #1002, #10638, #7758, #7161, #14128, #32487, #22621, #23019, #32691, #4678 ),
 .UNSPECIFIED., .F., .F.,
 ( 4, 2, 2, 2, 2, 2, 2, 4 ),
 ( 0.000000000000000000, 0.0004519050042106062602, 0.0009038100084212125204, 0.001355715012631818726, 0.001807620016842425041, 0.002259525021053031355, 0.002711430025263637453, 0.003615240033684850082 ),
 .UNSPECIFIED. ) ;
#15146=CARTESIAN_POINT ( 'NONE',  ( 67.21358634547439692, 57.88870193986200974, 3.993497817183392584 ) ) ;
#15147=EDGE_CURVE ( 'NONE', #3289, #30686, #9404, .T. ) ;
#15157=ORIENTED_EDGE ( 'NONE', *, *, #21243, .T. ) ;
#15163=CARTESIAN_POINT ( 'NONE',  ( 80.57935153413077956, 62.61414007970553541, -3.419027627190931451 ) ) ;
#15165=CARTESIAN_POINT ( 'NONE',  ( 78.66262733798791373, 65.98865143197195948, 1.634613895560430796 ) ) ;
#15169=CARTESIAN_POINT ( 'NONE',  ( 74.80267162900737787, 60.00335986791986898, -3.708893976703238948 ) ) ;
#15171=B_SPLINE_CURVE_WITH_KNOTS ( 'NONE', 3,
 ( #26166, #11090, #1262, #10892, #10296, #38698 ),
 .UNSPECIFIED., .F., .F.,
 ( 4, 2, 4 ),
 ( 0.000000000000000000, 0.0008616653180068700344, 0.001723330636013740069 ),
 .UNSPECIFIED. ) ;
#15182=DIRECTION ( 'NONE',  ( -0.7376613619250370624, -0.6751708784618154491, 0.000000000000000000 ) ) ;
#15183=CARTESIAN_POINT ( 'NONE',  ( 80.79744990009734806, 64.13345242326639095, 3.486376426170536558 ) ) ;
#15197=ORIENTED_EDGE ( 'NONE', *, *, #14679, .T. ) ;
#15205=CARTESIAN_POINT ( 'NONE',  ( 78.77361741396553896, 66.07891176884447759, -1.467306180864093701 ) ) ;
#15214=CARTESIAN_POINT ( 'NONE',  ( 79.87286157980665280, 64.75688458792352264, -3.459421039841298562 ) ) ;
#15215=CARTESIAN_POINT ( 'NONE',  ( -58.97877168559173811, 27.59157091290065367, -6.753965997777704899 ) ) ;
#15220=CARTESIAN_POINT ( 'NONE',  ( 81.38476203741939230, 61.42515712988156906, -1.285939662725171351 ) ) ;
#15222=LINE ( 'NONE', #30066, #15374 ) ;
#15228=CARTESIAN_POINT ( 'NONE',  ( 73.22742653720867168, 60.47695785811286839, 3.944160774617319287 ) ) ;
#15234=CARTESIAN_POINT ( 'NONE',  ( -58.11958539874534324, 31.63166798347506159, -4.423482167568619339 ) ) ;
#15236=CARTESIAN_POINT ( 'NONE',  ( 81.04721337197119624, 65.04274187704046994, 3.019849704268902535 ) ) ;
#15251=EDGE_CURVE ( 'NONE', #26757, #446, #2201, .T. ) ;
#15256=CARTESIAN_POINT ( 'NONE',  ( 66.82203765260634043, 58.05418649187924274, -3.997265020314329842 ) ) ;
#15258=CARTESIAN_POINT ( 'NONE',  ( -59.00782325774518000, 28.07066389825142139, -6.403654028263551012 ) ) ;
#15263=ORIENTED_EDGE ( 'NONE', *, *, #17360, .T. ) ;
#15268=CARTESIAN_POINT ( 'NONE',  ( 82.10909544300281482, 65.20937546977818045, -1.000000000000000000 ) ) ;
#15269=CARTESIAN_POINT ( 'NONE',  ( 78.62614802285547455, 66.01297166972811681, 1.268354304253248577 ) ) ;
#15272=CARTESIAN_POINT ( 'NONE',  ( 76.81217388538108537, 61.66049381551730590, -3.848392762315877569 ) ) ;
#15276=CARTESIAN_POINT ( 'NONE',  ( -55.16612787639762416, 31.23053227951969646, -1.484562114140327793 ) ) ;
#15277=CARTESIAN_POINT ( 'NONE',  ( 81.29167079631734794, 61.38276384236289829, -1.400336002810706360 ) ) ;
#15278=CARTESIAN_POINT ( 'NONE',  ( 78.86847112531712867, 61.76850681771009732, 3.535928464255590598 ) ) ;
#15284=CARTESIAN_POINT ( 'NONE',  ( 81.71086237227946469, 61.67650090218641168, 1.250621450094001830 ) ) ;
#15285=CARTESIAN_POINT ( 'NONE',  ( -64.08758708074091714, 42.49506848047520435, 2.672779995105290407 ) ) ;
#15289=CARTESIAN_POINT ( 'NONE',  ( -64.08758708074093136, -65.19654454972992141, -8.800414904976381791 ) ) ;
#15301=DIRECTION ( 'NONE',  ( -0.000000000000000000, -0.000000000000000000, -1.000000000000000000 ) ) ;
#15312=CARTESIAN_POINT ( 'NONE',  ( 69.03381461298826594, 59.23726071663833181, -3.954017255840780454 ) ) ;
#15324=CARTESIAN_POINT ( 'NONE',  ( 80.68211079047073042, 61.32331416546043812, -2.218931858625937004 ) ) ;
#15326=CARTESIAN_POINT ( 'NONE',  ( 81.96106518217325743, 62.90574382782719454, -2.573500632437588642 ) ) ;
#15328=CARTESIAN_POINT ( 'NONE',  ( 78.53532592461078821, 65.52573200842934398, 2.475680338657054058 ) ) ;
#15332=VERTEX_POINT ( 'NONE', #40614 ) ;
#15346=CIRCLE ( 'NONE', #12708, 2.500000000000002220 ) ;
#15353=CARTESIAN_POINT ( 'NONE',  ( 66.99315907379003932, 58.03889713220680591, 3.999016414675010012 ) ) ;
#15356=CIRCLE ( 'NONE', #16014, 83.68529983683480111 ) ;
#15362=CARTESIAN_POINT ( 'NONE',  ( -74.03402466285147909, 19.33157623370696498, -9.800414904976365804 ) ) ;
#15367=CARTESIAN_POINT ( 'NONE',  ( 80.96289755590194659, 61.39497013797979008, -2.048264032867926687 ) ) ;
#15370=CARTESIAN_POINT ( 'NONE',  ( 78.87073352949229843, 65.61655597148102004, 2.590854534519452024 ) ) ;
#15374=VECTOR ( 'NONE', #1879, 1000.000000000000000 ) ;
#15375=CARTESIAN_POINT ( 'NONE',  ( -59.01453825321729596, 27.97194601286735960, 6.240525879293456590 ) ) ;
#15377=CARTESIAN_POINT ( 'NONE',  ( -63.05048152672962658, 38.43432252562774210, -4.010992198732260761 ) ) ;
#15379=EDGE_CURVE ( 'NONE', #38060, #7364, #32357, .T. ) ;
#15390=CARTESIAN_POINT ( 'NONE',  ( 80.79838846785789030, 64.52093256242035579, 3.402511877379641891 ) ) ;
#15394=CARTESIAN_POINT ( 'NONE',  ( -64.24896514350277243, 34.84424003550355309, -5.066824151024967193 ) ) ;
#15398=CARTESIAN_POINT ( 'NONE',  ( -65.27430759792098058, 36.41843883184579056, -8.800656633793916939 ) ) ;
#15404=CARTESIAN_POINT ( 'NONE',  ( 81.24448906778437163, 62.55865020921709885, -3.071811904357653500 ) ) ;
#15413=CARTESIAN_POINT ( 'NONE',  ( 81.15742489870845588, 61.60174059333855467, -2.174925636353718161 ) ) ;
#15418=ORIENTED_EDGE ( 'NONE', *, *, #14390, .T. ) ;
#15420=CARTESIAN_POINT ( 'NONE',  ( 79.73837173991832117, 66.20136991484926625, -1.918505602738486138 ) ) ;
#15423=B_SPLINE_CURVE_WITH_KNOTS ( 'NONE', 3,
 ( #40597, #30955, #34261, #2759, #15285, #40391, #37310, #9106, #6032, #18566, #31153, #13826, #25784, #25987 ),
 .UNSPECIFIED., .F., .F.,
 ( 4, 2, 2, 2, 2, 2, 4 ),
 ( 0.000000000000000000, 0.0008966178941042668047, 0.001793235788208533609, 0.002241544735260675957, 0.002689853682312818087, 0.003138162629364960217, 0.003586471576417102347 ),
 .UNSPECIFIED. ) ;
#15427=CARTESIAN_POINT ( 'NONE',  ( -69.46331044089802731, 37.03771852125571229, 8.800414904976364028 ) ) ;
#15428=CARTESIAN_POINT ( 'NONE',  ( 74.86006972221214539, 59.87270642427901635, 3.642458757454619889 ) ) ;
#15438=CARTESIAN_POINT ( 'NONE',  ( 79.78729094670487143, 65.99503481514538805, 2.368810654844614394 ) ) ;
#15441=ORIENTED_EDGE ( 'NONE', *, *, #3264, .F. ) ;
#15451=DIRECTION ( 'NONE',  ( -0.5171480877355195682, 0.2439873919671761981, 0.8203828422831326295 ) ) ;
#15453=VERTEX_POINT ( 'NONE', #28581 ) ;
#15457=CARTESIAN_POINT ( 'NONE',  ( 66.74698822326750758, 57.80221319398844315, -3.998057522770657624 ) ) ;
#15461=TOROIDAL_SURFACE ( 'NONE', #20714, 67.42751648247021024, 3.000000000000000000 ) ;
#15462=CARTESIAN_POINT ( 'NONE',  ( -55.43956553351903693, 30.97124788692904218, 1.442063311134026637 ) ) ;
#15464=CARTESIAN_POINT ( 'NONE',  ( 74.91345620096926439, 63.41934653362798713, 3.016809678508692194 ) ) ;
#15467=VERTEX_POINT ( 'NONE', #6759 ) ;
#15470=CARTESIAN_POINT ( 'NONE',  ( 79.32563386639210989, 66.29995228605847046, -1.174937739208586907 ) ) ;
#15471=CARTESIAN_POINT ( 'NONE',  ( 78.64144163184205638, 66.02383098553904972, 1.235082213173782195 ) ) ;
#15474=CARTESIAN_POINT ( 'NONE',  ( 77.45380151126717294, 63.20247531706575472, -3.748203062644118067 ) ) ;
#15478=CARTESIAN_POINT ( 'NONE',  ( 79.45632949585312588, 65.80330994668889844, -2.596981798947360254 ) ) ;
#15479=CARTESIAN_POINT ( 'NONE',  ( 78.06740453511714861, 61.95427634543516149, 3.748203062644153150 ) ) ;
#15485=CARTESIAN_POINT ( 'NONE',  ( -57.44572001938779238, 32.97690117809874977, 4.025720541963821120 ) ) ;
#15486=CARTESIAN_POINT ( 'NONE',  ( 80.49077247797930568, 66.09228938494877070, 1.971256063808053627 ) ) ;
#15493=CARTESIAN_POINT ( 'NONE',  ( -64.17177837788707961, 36.63861034030102815, 5.251833000746531255 ) ) ;
#15495=DIRECTION ( 'NONE',  ( -0.9267318687906771491, 0.3757233601570964532, 0.000000000000000000 ) ) ;
#15503=CARTESIAN_POINT ( 'NONE',  ( 81.16957891225059996, 61.30398062001309256, -1.000000000000000000 ) ) ;
#15517=CARTESIAN_POINT ( 'NONE',  ( 69.55412262724962602, 59.60600320152340004, -3.916752429509892774 ) ) ;
#15528=AXIS2_PLACEMENT_3D ( 'NONE', #3510, #38258, #410 ) ;
#15531=CARTESIAN_POINT ( 'NONE',  ( 78.83212471655066622, 64.69929012837440041, -3.375657603866064616 ) ) ;
#15534=CARTESIAN_POINT ( 'NONE',  ( 81.10335266982598057, 65.07249684831452896, -2.967158453529146644 ) ) ;
#15535=CARTESIAN_POINT ( 'NONE',  ( 79.38338525671692025, 64.07937768075930762, 3.690346394509879335 ) ) ;
#15539=CARTESIAN_POINT ( 'NONE',  ( 80.03496335128151884, 66.36160760684386162, 1.000000000000000000 ) ) ;
#15563=CARTESIAN_POINT ( 'NONE',  ( 67.00793363329040631, 57.99808316372624972, 3.999354069328931782 ) ) ;
#15580=CARTESIAN_POINT ( 'NONE',  ( 78.59417545055856635, 65.93066236947775849, -1.724274471760826488 ) ) ;
#15582=CARTESIAN_POINT ( 'NONE',  ( 80.77881921633029094, 62.12902493665696824, 3.041370705153006337 ) ) ;
#15589=CARTESIAN_POINT ( 'NONE',  ( -64.08758708074093136, 38.34280096101419844, -3.014656224624829850 ) ) ;
#15595=VECTOR ( 'NONE', #9870, 1000.000000000000000 ) ;
#15599=CARTESIAN_POINT ( 'NONE',  ( 81.24747667583794453, 63.59436251574997101, 3.343039074470570693 ) ) ;
#15614=CARTESIAN_POINT ( 'NONE',  ( 80.31657930512767507, 64.64970693426512582, -3.487490852634256733 ) ) ;
#15628=CARTESIAN_POINT ( 'NONE',  ( 79.73292928667240176, 64.66788176856890402, -3.497296750721717196 ) ) ;
#15634=CARTESIAN_POINT ( 'NONE',  ( 81.23963933823222305, 65.14454330635804524, -2.817575383041753589 ) ) ;
#15641=CARTESIAN_POINT ( 'NONE',  ( 72.96153509227066536, 61.08495594734687018, 3.864208391313482149 ) ) ;
#15651=CARTESIAN_POINT ( 'NONE',  ( 80.60418185334565067, 65.53338749785490336, 2.819252638153800117 ) ) ;
#15667=CARTESIAN_POINT ( 'NONE',  ( 66.69400287465482791, 57.94980623640483230, -3.999076693785756920 ) ) ;
#15672=CARTESIAN_POINT ( 'NONE',  ( -57.29470892912325297, 33.22074752690817689, 3.999999999999999112 ) ) ;
#15679=ORIENTED_EDGE ( 'NONE', *, *, #22196, .F. ) ;
#15681=CARTESIAN_POINT ( 'NONE',  ( 78.99269976270092286, 66.20980237122185486, -1.093381982072927361 ) ) ;
#15682=CARTESIAN_POINT ( 'NONE',  ( 79.44161963160776452, 65.18980684700308359, 3.197674131580388490 ) ) ;
#15684=CARTESIAN_POINT ( 'NONE',  ( 77.42503339237346438, 60.33561942134753764, -3.121245467013774810 ) ) ;
#15689=CARTESIAN_POINT ( 'NONE',  ( 80.07838786650488316, 65.24465706271045917, -3.189931650267179286 ) ) ;
#15690=CARTESIAN_POINT ( 'NONE',  ( 78.65108613080987254, 60.71083206350697026, 2.889099817377207557 ) ) ;
#15695=CARTESIAN_POINT ( 'NONE',  ( 82.44602376881528016, 63.15227202030956732, 1.728104186157677358 ) ) ;
#15709=CARTESIAN_POINT ( 'NONE',  ( 66.27376694608931018, 57.73522568913554665, -4.000000000000000000 ) ) ;
#15723=CARTESIAN_POINT ( 'NONE',  ( 68.00738522489628224, 58.43930376306189345, -3.995571880668716602 ) ) ;
#15725=ORIENTED_EDGE ( 'NONE', *, *, #8451, .T. ) ;
#15735=ORIENTED_EDGE ( 'NONE', *, *, #17536, .F. ) ;
#15738=CARTESIAN_POINT ( 'NONE',  ( 79.93872656714209768, 63.00306196921508217, -3.690346394509887773 ) ) ;
#15741=CARTESIAN_POINT ( 'NONE',  ( 81.76814852625381036, 62.80907675923850775, -2.758880570191353687 ) ) ;
#15742=CARTESIAN_POINT ( 'NONE',  ( 80.44079772350291080, 62.04115482339161503, 3.140153738741080058 ) ) ;
#15745=CARTESIAN_POINT ( 'NONE',  ( 82.59411735159427792, 63.56171878218358273, 1.000000000000000000 ) ) ;
#15750=VERTEX_POINT ( 'NONE', #29982 ) ;
#15771=CARTESIAN_POINT ( 'NONE',  ( 67.06207392303235792, 57.84849753947618467, 3.994852852620101480 ) ) ;
#15786=ORIENTED_EDGE ( 'NONE', *, *, #10732, .T. ) ;
#15791=CARTESIAN_POINT ( 'NONE',  ( 80.35827824124267238, 62.85331387716615126, -3.547878946066216788 ) ) ;
#15792=CARTESIAN_POINT ( 'NONE',  ( 89.09355779190869384, 24.84364830758654108, -8.800414904976364028 ) ) ;
#15793=CARTESIAN_POINT ( 'NONE',  ( 79.58170130377179419, 64.56493525204571426, 3.531602295408449610 ) ) ;
#15797=CARTESIAN_POINT ( 'NONE',  ( -57.21793255368775988, 30.45183801093173770, 3.625376778041544235 ) ) ;
#15808=CARTESIAN_POINT ( 'NONE',  ( 80.70340038347129052, 64.47061299330751183, 3.456914256421387499 ) ) ;
#15812=FACE_OUTER_BOUND ( 'NONE', #1867, .T. ) ;
#15819=CARTESIAN_POINT ( 'NONE',  ( -54.79610818216033152, 31.51396769785350926, 1.000000000000000000 ) ) ;
#15823=ADVANCED_FACE ( 'NONE', ( #9700 ), #35009, .T. ) ;
#15825=CARTESIAN_POINT ( 'NONE',  ( 79.86111789578113473, 65.11834937465496864, -3.286127602909499235 ) ) ;
#15834=CARTESIAN_POINT ( 'NONE',  ( 80.05321609864766685, 64.11675358990301277, -3.674973878998263110 ) ) ;
#15844=CARTESIAN_POINT ( 'NONE',  ( 74.96893927862336682, 59.62365076172310552, 3.485789274173446639 ) ) ;
#15851=CARTESIAN_POINT ( 'NONE',  ( 78.68741431065086545, 66.05648362737333912, 1.057717897339650159 ) ) ;
#15868=VERTEX_POINT ( 'NONE', #2215 ) ;
#15872=CARTESIAN_POINT ( 'NONE',  ( 66.69105935506532035, 57.95800471661298303, -3.998864354720668146 ) ) ;
#15882=CARTESIAN_POINT ( 'NONE',  ( 79.67387220895490429, 66.32735109421591346, -1.189854999565593818 ) ) ;
#15884=CARTESIAN_POINT ( 'NONE',  ( 80.05321609864766685, 64.11675358990301277, 3.674973878998264443 ) ) ;
#15887=CARTESIAN_POINT ( 'NONE',  ( 77.06614703306246383, 61.11928327932308491, -3.683100983543596385 ) ) ;
#15891=CARTESIAN_POINT ( 'NONE',  ( 81.24880315266030095, 62.88501018724373637, -3.211742283750911753 ) ) ;
#15892=CARTESIAN_POINT ( 'NONE',  ( 79.32401137462350960, 60.77278567581110025, 2.512892981323315844 ) ) ;
#15897=CARTESIAN_POINT ( 'NONE',  ( 81.16398582655347127, 65.83200543430108098, 2.021051955676537393 ) ) ;
#15901=ADVANCED_FACE ( 'NONE', ( #3349 ), #25751, .F. ) ;
#15903=DIRECTION ( 'NONE',  ( 0.000000000000000000, 0.000000000000000000, 1.000000000000000000 ) ) ;
#15905=CARTESIAN_POINT ( 'NONE',  ( -64.08758708074093136, 35.87095250353098663, 3.952250494627216781 ) ) ;
#15907=CARTESIAN_POINT ( 'NONE',  ( -60.14275962559869981, 24.84364830758654108, -9.154021781743367114 ) ) ;
#15920=CARTESIAN_POINT ( 'NONE',  ( 67.85873555399604129, 57.94375731920307260, -3.976226663256417826 ) ) ;
#15933=CARTESIAN_POINT ( 'NONE',  ( 80.71621671784500052, 61.21110637000719379, -1.935054690158737323 ) ) ;
#15936=CARTESIAN_POINT ( 'NONE',  ( 81.32842084066697907, 61.39880091617934710, -1.358900964588043880 ) ) ;
#15937=CARTESIAN_POINT ( 'NONE',  ( 79.84618440311783161, 63.29375160576378079, 3.738478073092017073 ) ) ;
#15964=DIRECTION ( 'NONE',  ( -0.7376613619250370624, -0.6751708784618154491, -0.000000000000000000 ) ) ;
#15967=CARTESIAN_POINT ( 'NONE',  ( -63.08758708074093136, 38.76906266698301806, -4.000000000000000000 ) ) ;
#15969=CARTESIAN_POINT ( 'NONE',  ( 67.22540103859083160, 57.85622601175691671, 3.990981480864019826 ) ) ;
#15975=DIRECTION ( 'NONE',  ( -0.4582725098355649451, 0.8888117386314224877, 0.000000000000000000 ) ) ;
#15982=CARTESIAN_POINT ( 'NONE',  ( 79.40192692649263506, 64.80415203875445229, -3.426353657592664526 ) ) ;
#15984=CARTESIAN_POINT ( 'NONE',  ( 81.02333598550073646, 61.30014629029354722, 1.703597047176645507 ) ) ;
#15986=DIRECTION ( 'NONE',  ( 0.000000000000000000, 0.000000000000000000, 1.000000000000000000 ) ) ;
#15990=CARTESIAN_POINT ( 'NONE',  ( -57.80310541255629886, 30.11675026092115104, 4.211351614731054127 ) ) ;
#16006=CARTESIAN_POINT ( 'NONE',  ( -69.08758708074091714, 24.84364830758654108, -8.800414904976364028 ) ) ;
#16007=FACE_OUTER_BOUND ( 'NONE', #30252, .T. ) ;
#16008=CARTESIAN_POINT ( 'NONE',  ( 78.77947119303419754, 66.08315628559923027, 1.459100623883111902 ) ) ;
#16014=AXIS2_PLACEMENT_3D ( 'NONE', #3208, #37733, #27869 ) ;
#16021=ORIENTED_EDGE ( 'NONE', *, *, #23744, .T. ) ;
#16022=CARTESIAN_POINT ( 'NONE',  ( 81.14234681338471944, 61.29401378075402818, -1.159471704397073477 ) ) ;
#16032=CARTESIAN_POINT ( 'NONE',  ( 80.50045704793726031, 63.23530725187647050, -3.614403801066807365 ) ) ;
#16037=ORIENTED_EDGE ( 'NONE', *, *, #4609, .T. ) ;
#16038=CARTESIAN_POINT ( 'NONE',  ( 82.07485033897415860, 63.29559580402020913, -2.558871340112543358 ) ) ;
#16044=CARTESIAN_POINT ( 'NONE',  ( 69.67664977695649497, 59.29623187989270150, 3.972683913566358971 ) ) ;
#16048=ORIENTED_EDGE ( 'NONE', *, *, #18786, .F. ) ;
#16053=CARTESIAN_POINT ( 'NONE',  ( 78.85932765206025863, 66.13466208585964523, 1.358900964592133054 ) ) ;
#16066=FACE_OUTER_BOUND ( 'NONE', #3329, .T. ) ;
#16076=EDGE_CURVE ( 'NONE', #4319, #17865, #28527, .T. ) ;
#16077=CARTESIAN_POINT ( 'NONE',  ( 66.27376694609004915, 57.73522568913436004, -4.000000000000000000 ) ) ;
#16085=CARTESIAN_POINT ( 'NONE',  ( 81.46991160412488853, 61.46693516840311133, -1.070820504727074685 ) ) ;
#16087=CARTESIAN_POINT ( 'NONE',  ( 80.99344733541434493, 61.93321701578161509, 2.778975589575234384 ) ) ;
#16092=CARTESIAN_POINT ( 'NONE',  ( 75.57967633106541427, 61.33476069914100748, -3.901127667181007119 ) ) ;
#16094=LINE ( 'NONE', #25569, #32892 ) ;
#16096=CARTESIAN_POINT ( 'NONE',  ( 78.94073822560471854, 66.07870154842751731, -1.754135932968032163 ) ) ;
#16097=CARTESIAN_POINT ( 'NONE',  ( 76.19461364182981811, 62.94386820200828225, 3.683100983535307904 ) ) ;
#16103=CARTESIAN_POINT ( 'NONE',  ( 78.68995612299298159, 66.05828935306207939, 1.022614849746397159 ) ) ;
#16108=CARTESIAN_POINT ( 'NONE',  ( -59.87552183813137674, 24.84364830758654108, 9.800414904976365804 ) ) ;
#16111=CARTESIAN_POINT ( 'NONE',  ( -66.99872204295122913, 28.48507918597134037, -46.17089178453873188 ) ) ;
#16127=CARTESIAN_POINT ( 'NONE',  ( 68.66337269546751543, 58.46565884629779930, -3.990501929453247332 ) ) ;
#16128=TOROIDAL_SURFACE ( 'NONE', #33840, 6.999999999999986677, 1.000000000000000000 ) ;
#16140=CARTESIAN_POINT ( 'NONE',  ( -81.07947155388369254, 30.81399289130168384, -46.17089178453873188 ) ) ;
#16141=CARTESIAN_POINT ( 'NONE',  ( 81.23686708412715518, 61.78859655676697571, 2.419967184825709161 ) ) ;
#16144=CARTESIAN_POINT ( 'NONE',  ( 78.20000946334697289, 65.71092203236408125, -1.748505333477076817 ) ) ;
#16147=CARTESIAN_POINT ( 'NONE',  ( 81.46069228693599484, 61.55470069442471015, -1.644402879615779689 ) ) ;
#16148=CARTESIAN_POINT ( 'NONE',  ( 80.23310653198076636, 61.53645999506316144, 2.845586111146968467 ) ) ;
#16151=CARTESIAN_POINT ( 'NONE',  ( -63.63077514377983590, 43.97264056304742752, 2.477143415600858933 ) ) ;
#16172=CARTESIAN_POINT ( 'NONE',  ( 66.71461092208421917, 57.89240490252945648, 3.999756211082519552 ) ) ;
#16174=VECTOR ( 'NONE', #37770, 1000.000000000000000 ) ;
#16189=CARTESIAN_POINT ( 'NONE',  ( 79.12326768591945836, 65.24646460380061797, -3.052025427726081652 ) ) ;
#16192=CARTESIAN_POINT ( 'NONE',  ( 78.59417545055856635, 65.93066236947775849, 1.724274471760826488 ) ) ;
#16195=ORIENTED_EDGE ( 'NONE', *, *, #36863, .F. ) ;
#16207=CARTESIAN_POINT ( 'NONE',  ( 79.58096101840206416, 65.58481148403340910, 2.850064543546717566 ) ) ;
#16223=CARTESIAN_POINT ( 'NONE',  ( 81.02539575022784391, 62.78269734341446195, -3.300462285847916899 ) ) ;
#16236=CARTESIAN_POINT ( 'NONE',  ( 81.04163241827636455, 61.94641952267326701, -2.758686562281577270 ) ) ;
#16247=CARTESIAN_POINT ( 'NONE',  ( 69.70139497306261944, 59.23354404394888917, 3.977789803233246158 ) ) ;
#16248=ORIENTED_EDGE ( 'NONE', *, *, #6318, .T. ) ;
#16255=CARTESIAN_POINT ( 'NONE',  ( 80.14223387229885986, 65.61881967978085584, 2.852119850618825669 ) ) ;
#16265=DIRECTION ( 'NONE',  ( 1.000000000000000000, 0.000000000000000000, 0.000000000000000000 ) ) ;
#16267=AXIS2_PLACEMENT_3D ( 'NONE', #17172, #33045, #26266 ) ;
#16274=CARTESIAN_POINT ( 'NONE',  ( 66.55613647995218685, 57.87265654107390844, -3.999745625243888547 ) ) ;
#16285=CARTESIAN_POINT ( 'NONE',  ( 81.92984576605157088, 61.94483778347744618, -1.306649493517271221 ) ) ;
#16290=CARTESIAN_POINT ( 'NONE',  ( 76.19819836466999163, 59.97076997751577210, -3.322260703561257245 ) ) ;
#16294=CARTESIAN_POINT ( 'NONE',  ( 76.31287196683638285, 61.24236878174156828, 3.825872951957600243 ) ) ;
#16301=CARTESIAN_POINT ( 'NONE',  ( 79.53094818655506515, 66.25005786596111079, 1.601045042264325646 ) ) ;
#16315=LINE ( 'NONE', #28883, #9533 ) ;
#16319=CARTESIAN_POINT ( 'NONE',  ( 68.42229528291726126, 59.10113456467039583, -3.941639393089740651 ) ) ;
#16323=CARTESIAN_POINT ( 'NONE',  ( -64.08758708074094557, 37.77509509994077774, 3.093168342234559276 ) ) ;
#16331=CARTESIAN_POINT ( 'NONE',  ( 79.42059605865688354, 65.48104909687435793, 2.923497156821689646 ) ) ;
#16335=CARTESIAN_POINT ( 'NONE',  ( 78.41725481636187567, 64.09006905928654874, -3.590127757398426489 ) ) ;
#16340=CARTESIAN_POINT ( 'NONE',  ( 80.85068185327205015, 64.93836743323436167, -3.187395722549116961 ) ) ;
#16341=CARTESIAN_POINT ( 'NONE',  ( 79.72787136111028872, 62.61980214589643623, 3.627744115730415775 ) ) ;
#16344=CARTESIAN_POINT ( 'NONE',  ( 79.33205627562975337, 66.30342423254383277, 1.132734665583299272 ) ) ;
#16345=CARTESIAN_POINT ( 'NONE',  ( -64.08758708074093136, 44.09647858371769047, 1.000000000000000000 ) ) ;
#16355=CARTESIAN_POINT ( 'NONE',  ( 66.27376694608931018, 57.73522568913554665, -4.000000000000000000 ) ) ;
#16363=CARTESIAN_POINT ( 'NONE',  ( -59.87552183813137674, 24.84364830758654108, -9.800414904976365804 ) ) ;
#16372=CARTESIAN_POINT ( 'NONE',  ( 66.85741207324237223, 57.95599960577073517, 3.999594749380519954 ) ) ;
#16380=TOROIDAL_SURFACE ( 'NONE', #36118, 80.68529983683480111, 3.000000000000000000 ) ;
#16384=CARTESIAN_POINT ( 'NONE',  ( 78.69934701664531929, 65.67047266146688855, -2.368006059521097217 ) ) ;
#16386=CARTESIAN_POINT ( 'NONE',  ( 80.80742440666425352, 61.88848183320469332, 2.854164747637849775 ) ) ;
#16404=CARTESIAN_POINT ( 'NONE',  ( 80.58645273467570291, 64.40825618792595719, 3.509897338574980541 ) ) ;
#16410=EDGE_CURVE ( 'NONE', #23047, #30342, #40373, .T. ) ;
#16415=CARTESIAN_POINT ( 'NONE',  ( -59.93345510331042902, 24.73247967741478703, -46.17089178453873188 ) ) ;
#16417=CARTESIAN_POINT ( 'NONE',  ( 68.45414103466679023, 59.01732383939346249, 3.957896739784462881 ) ) ;
#16419=CARTESIAN_POINT ( 'NONE',  ( -64.08758708074093136, 43.50509228255777572, -1.592748443927769486 ) ) ;
#16423=CARTESIAN_POINT ( 'NONE',  ( 80.79424907316142423, 63.37012793878832184, -3.540619799101249576 ) ) ;
#16431=CARTESIAN_POINT ( 'NONE',  ( 81.12912465015324415, 61.32884242822650833, -1.592560325354577255 ) ) ;
#16443=CARTESIAN_POINT ( 'NONE',  ( 71.70339147920792300, 60.88422586754656152, 3.784404822148339953 ) ) ;
#16454=CARTESIAN_POINT ( 'NONE',  ( 81.52287143523093960, 61.74508502528568954, 1.930361577756008806 ) ) ;
#16475=CARTESIAN_POINT ( 'NONE',  ( 66.58744840590414071, 57.78483400379950297, -3.999444518112384106 ) ) ;
#16478=AXIS2_PLACEMENT_3D ( 'NONE', #21441, #34017, #3539 ) ;
#16485=CARTESIAN_POINT ( 'NONE',  ( 82.07520363809490505, 62.17599436785806688, -1.599335268229508111 ) ) ;
#16486=CARTESIAN_POINT ( 'NONE',  ( 27.60344192425479193, 81.15229837709949834, 4.000000000000000000 ) ) ;
#16488=CARTESIAN_POINT ( 'NONE',  ( 75.50377651103727317, 61.49872921062497255, -3.901127667181019110 ) ) ;
#16492=CARTESIAN_POINT ( 'NONE',  ( 77.35950424652857293, 60.48040194676344328, 3.253266109310522847 ) ) ;
#16496=CARTESIAN_POINT ( 'NONE',  ( 81.61324681686122062, 61.62795767120283585, 1.465632304122483465 ) ) ;
#16503=DIRECTION ( 'NONE',  ( -0.000000000000000000, -0.000000000000000000, -1.000000000000000000 ) ) ;
#16519=CARTESIAN_POINT ( 'NONE',  ( 67.83896914621323049, 57.99724189137371155, -3.982857479566772607 ) ) ;
#16527=CARTESIAN_POINT ( 'NONE',  ( -64.08758708074093136, 43.61223004741322740, -1.000000000000000000 ) ) ;
#16530=CARTESIAN_POINT ( 'NONE',  ( 81.74784679736075077, 61.69507302169112251, -1.000000000000000000 ) ) ;
#16531=CARTESIAN_POINT ( 'NONE',  ( 79.30685661404396569, 65.70718262327383741, 2.676159939830902168 ) ) ;
#16535=CARTESIAN_POINT ( 'NONE',  ( 80.24754081275330009, 61.06584331557482415, -2.177161688561031649 ) ) ;
#16538=CARTESIAN_POINT ( 'NONE',  ( 81.48777377604515948, 63.71638886501444432, -3.187395722549115185 ) ) ;
#16539=CARTESIAN_POINT ( 'NONE',  ( 80.56990227295247564, 61.62418804268437356, 2.732428818688230621 ) ) ;
#16542=CARTESIAN_POINT ( 'NONE',  ( 82.54941478318340842, 63.90107490703085347, 1.303631908148715990 ) ) ;
#16543=CARTESIAN_POINT ( 'NONE',  ( -63.60823941500427736, 43.84876827539012822, 2.657415981336364919 ) ) ;
#16563=CARTESIAN_POINT ( 'NONE',  ( 66.73816075044196339, 57.82680446425992926, 3.998864354716218816 ) ) ;
#16577=CARTESIAN_POINT ( 'NONE',  ( 79.74463803169643938, 63.93878357801280288, -3.720735635808768649 ) ) ;
#16578=CARTESIAN_POINT ( 'NONE',  ( 79.74463803169676623, 63.93878357801307999, 3.720735635808746888 ) ) ;
#16596=CARTESIAN_POINT ( 'NONE',  ( 81.09339258687020902, 63.16289930221481796, 3.352621494407052705 ) ) ;
#16603=FACE_OUTER_BOUND ( 'NONE', #9615, .T. ) ;
#16609=CARTESIAN_POINT ( 'NONE',  ( 81.21586879471323073, 61.61940358760092806, -2.137206601789636728 ) ) ;
#16614=CARTESIAN_POINT ( 'NONE',  ( -61.00670947824507806, 24.84364830758654108, -8.800414904976364028 ) ) ;
#16620=CARTESIAN_POINT ( 'NONE',  ( 81.04529349509148517, 61.25860024526324565, -1.340350474428863459 ) ) ;
#16632=CARTESIAN_POINT ( 'NONE',  ( 72.42208042952545100, 59.16915255968121556, 3.823636340456165073 ) ) ;
#16641=CARTESIAN_POINT ( 'NONE',  ( 81.16407079065473340, 61.30196360636995934, 1.071687152257631004 ) ) ;
#16644=ORIENTED_EDGE ( 'NONE', *, *, #27420, .F. ) ;
#16663=AXIS2_PLACEMENT_3D ( 'NONE', #5558, #30690, #27584 ) ;
#16667=CARTESIAN_POINT ( 'NONE',  ( -64.08758708074094557, 37.43074634368117160, -3.182173495013627562 ) ) ;
#16674=CARTESIAN_POINT ( 'NONE',  ( 81.68900298540734184, 61.66555023304466232, -1.322881339814839352 ) ) ;
#16677=CARTESIAN_POINT ( 'NONE',  ( 76.25423822322979106, 59.84407948384421161, -3.204585025132130394 ) ) ;
#16681=CARTESIAN_POINT ( 'NONE',  ( 77.48353911088555890, 60.20448024992288083, 2.970791854446974689 ) ) ;
#16688=CARTESIAN_POINT ( 'NONE',  ( 82.03714350014182344, 63.99860240201152095, 2.622983904469076144 ) ) ;
#16702=CARTESIAN_POINT ( 'NONE',  ( -63.08758708074093136, 41.04287353446839859, -4.000000000000000000 ) ) ;
#16708=CARTESIAN_POINT ( 'NONE',  ( 67.12475893546654504, 58.13278081555189658, -3.997693602769901045 ) ) ;
#16713=DIRECTION ( 'NONE',  ( 0.4582725098355735494, -0.8888117386314181578, 0.000000000000000000 ) ) ;
#16717=CARTESIAN_POINT ( 'NONE',  ( -55.39244940828790220, 31.07786128219255062, 1.730094348643131941 ) ) ;
#16719=ORIENTED_EDGE ( 'NONE', *, *, #31118, .T. ) ;
#16723=CARTESIAN_POINT ( 'NONE',  ( 81.11573943753921867, 62.50280337846361789, 3.122598816540627542 ) ) ;
#16727=CARTESIAN_POINT ( 'NONE',  ( 78.15789273364713097, 65.21536350427231810, -2.660685394430948314 ) ) ;
#16730=CARTESIAN_POINT ( 'NONE',  ( 81.53866496495169258, 61.91358381440836922, -2.246767365022170893 ) ) ;
#16732=CARTESIAN_POINT ( 'NONE',  ( 78.15789273364713097, 65.21536350427231810, 2.660685394430948314 ) ) ;
#16735=CARTESIAN_POINT ( 'NONE',  ( 81.96779975749585390, 61.96402392828839822, 1.065376284871803581 ) ) ;
#16736=CARTESIAN_POINT ( 'NONE',  ( -63.44067635386505088, 42.93380570789835105, 3.509169995953163035 ) ) ;
#16740=CARTESIAN_POINT ( 'NONE',  ( -64.20341131561860948, 34.94420666461578406, -4.877756629158676027 ) ) ;
#16744=DIRECTION ( 'NONE',  ( 1.000000000000000000, 0.000000000000000000, 0.000000000000000000 ) ) ;
#16748=VERTEX_POINT ( 'NONE', #32600 ) ;
#16760=VERTEX_POINT ( 'NONE', #4398 ) ;
#16762=CARTESIAN_POINT ( 'NONE',  ( 66.69400287465482791, 57.94980623640483230, 3.999076693785756031 ) ) ;
#16779=CARTESIAN_POINT ( 'NONE',  ( 80.48897389181450990, 62.29924170813984574, -3.301258712451521138 ) ) ;
#16780=CARTESIAN_POINT ( 'NONE',  ( 79.64740672574815505, 64.24900652125759848, 3.657510014241685425 ) ) ;
#16795=CARTESIAN_POINT ( 'NONE',  ( 81.36407395805154863, 61.67455102447422632, 2.043563575549261824 ) ) ;
#16805=CARTESIAN_POINT ( 'NONE',  ( -64.08758708074093136, 40.20283945498818667, -3.000000000000000000 ) ) ;
#16812=AXIS2_PLACEMENT_3D ( 'NONE', #1137, #35318, #7084 ) ;
#16816=CARTESIAN_POINT ( 'NONE',  ( 79.61290006553410592, 65.30841326124827617, -3.134554000843263299 ) ) ;
#16819=CARTESIAN_POINT ( 'NONE',  ( -56.76293260130698570, 30.10808691202729293, 4.002692287617911404 ) ) ;
#16826=CARTESIAN_POINT ( 'NONE',  ( 81.06761308752984974, 61.31222891353763771, -1.660510093083302108 ) ) ;
#16828=CARTESIAN_POINT ( 'NONE',  ( 80.33017967436602191, 63.51919597486899249, 3.679799701112133725 ) ) ;
#16830=VERTEX_POINT ( 'NONE', #27407 ) ;
#16832=CARTESIAN_POINT ( 'NONE',  ( -58.95184776849900743, 28.36361089872152519, -6.321022755279361860 ) ) ;
#16836=CARTESIAN_POINT ( 'NONE',  ( -64.08758708074407195, 44.09647857431092888, -1.198350469763766579 ) ) ;
#16840=CARTESIAN_POINT ( 'NONE',  ( 78.69038500580363404, 66.05859403932464602, -1.000000000000000000 ) ) ;
#16845=CARTESIAN_POINT ( 'NONE',  ( -69.08758708074091714, 24.84364830758654108, 8.800414904976364028 ) ) ;
#16846=CARTESIAN_POINT ( 'NONE',  ( 79.73441168748210828, 65.96538777703865719, 2.410848004515915743 ) ) ;
#16864=ORIENTED_EDGE ( 'NONE', *, *, #27472, .T. ) ;
#16869=CARTESIAN_POINT ( 'NONE',  ( 66.27376694609004915, 57.73522568913436004, -4.000000000000000000 ) ) ;
#16875=EDGE_CURVE ( 'NONE', #22837, #39470, #1355, .T. ) ;
#16876=( NAMED_UNIT ( * ) PLANE_ANGLE_UNIT ( ) SI_UNIT ( $, .RADIAN. ) );
#16880=CARTESIAN_POINT ( 'NONE',  ( 80.56094004998607261, 66.12977872868212614, -1.831286414254869266 ) ) ;
#16883=CARTESIAN_POINT ( 'NONE',  ( 75.30130074865812162, 63.36357894040063599, -3.230144225280407344 ) ) ;
#16887=CARTESIAN_POINT ( 'NONE',  ( 77.66280895473884982, 61.33468559051788560, 3.643081266330365331 ) ) ;
#16889=PLANE ( 'NONE',  #18176 ) ;
#16891=AXIS2_PLACEMENT_3D ( 'NONE', #36758, #24198, #17389 ) ;
#16895=CARTESIAN_POINT ( 'NONE',  ( 81.66247121191638314, 61.65231731326593234, 1.378120381825652219 ) ) ;
#16900=AXIS2_PLACEMENT_3D ( 'NONE', #21888, #27646, #3188 ) ;
#16904=ORIENTED_EDGE ( 'NONE', *, *, #26958, .F. ) ;
#16909=DIRECTION ( 'NONE',  ( 0.9267318687906771491, -0.3757233601570964532, 0.000000000000000000 ) ) ;
#16918=CARTESIAN_POINT ( 'NONE',  ( 67.36017643331848603, 58.39563743223260417, -3.987264345885670913 ) ) ;
#16934=CARTESIAN_POINT ( 'NONE',  ( 79.99568124201523744, 64.83088095446822763, 3.420541042474579907 ) ) ;
#16937=CARTESIAN_POINT ( 'NONE',  ( 78.24346468842466606, 65.07400588416957987, -2.889371261047450457 ) ) ;
#16940=CARTESIAN_POINT ( 'NONE',  ( 80.71310200138587732, 64.86488640221421065, -3.283621700554756995 ) ) ;
#16941=CARTESIAN_POINT ( 'NONE',  ( 80.55759259636404579, 61.16327383424329156, 2.033355767895909327 ) ) ;
#16943=CARTESIAN_POINT ( 'NONE',  ( 81.96245566837731644, 61.96131850323958901, 1.129532193886028102 ) ) ;
#16945=VERTEX_POINT ( 'NONE', #15053 ) ;
#16948=CARTESIAN_POINT ( 'NONE',  ( -64.29080678322935682, 36.57451004496367375, -5.531098403533436070 ) ) ;
#16964=AXIS2_PLACEMENT_3D ( 'NONE', #14749, #12284, #18878 ) ;
#16970=CARTESIAN_POINT ( 'NONE',  ( 66.71166677010936041, 57.90060579507158423, 3.999756211082797996 ) ) ;
#16971=CARTESIAN_POINT ( 'NONE',  ( 71.10141846075379135, 59.08792130574165924, -3.942344351592514951 ) ) ;
#16975=AXIS2_PLACEMENT_3D ( 'NONE', #11466, #24033, #33541 ) ;
#16982=CARTESIAN_POINT ( 'NONE',  ( 80.87649832867062116, 61.25867624111136678, -1.827177995460257387 ) ) ;
#16984=CARTESIAN_POINT ( 'NONE',  ( 80.03393078220602774, 63.38059744715243937, 3.720735635808742447 ) ) ;
#16986=ORIENTED_EDGE ( 'NONE', *, *, #35684, .T. ) ;
#16987=CIRCLE ( 'NONE', #3235, 1.000000000000000000 ) ;
#16995=AXIS2_PLACEMENT_3D ( 'NONE', #30079, #14214, #2092 ) ;
#16998=CARTESIAN_POINT ( 'NONE',  ( 79.86111789578114895, 65.11834937465495443, 3.286127602909497014 ) ) ;
#17002=CARTESIAN_POINT ( 'NONE',  ( -64.85784325972055342, 34.81586596186931359, -6.466735817496061856 ) ) ;
#17009=CARTESIAN_POINT ( 'NONE',  ( 69.41850365747683327, 58.24027689931818230, 3.921432738910689331 ) ) ;
#17011=CARTESIAN_POINT ( 'NONE',  ( -64.08758708074094557, 43.61223004741322740, -1.152033497945007978 ) ) ;
#17013=CARTESIAN_POINT ( 'NONE',  ( 79.92454992231405697, 64.78853304740056274, -3.443978770203974360 ) ) ;
#17016=CARTESIAN_POINT ( 'NONE',  ( -57.86591918990971095, 28.88504657882484850, 4.653542815086530560 ) ) ;
#17025=CARTESIAN_POINT ( 'NONE',  ( 79.64490966524759585, 64.60885719387546544, -3.518158556798105963 ) ) ;
#17027=CARTESIAN_POINT ( 'NONE',  ( 81.09181894009961411, 61.27555711777438319, 1.268354304253239917 ) ) ;
#17033=CARTESIAN_POINT ( 'NONE',  ( -64.08758708074093136, 43.38408792958330906, -2.770133712456854802 ) ) ;
#17043=CARTESIAN_POINT ( 'NONE',  ( 81.59170830165204791, 62.44397035144425701, 2.684801069578921950 ) ) ;
#17068=ORIENTED_EDGE ( 'NONE', *, *, #35541, .T. ) ;
#17069=DIRECTION ( 'NONE',  ( -1.000000000000000000, 0.000000000000000000, 0.000000000000000000 ) ) ;
#17070=SHAPE_REPRESENTATION_RELATIONSHIP ( 'NONE' , 'NONE' ,  #19830, #22541 ) ;
#17078=CARTESIAN_POINT ( 'NONE',  ( 82.29094429576466041, 64.52076745355560661, -1.905332024691357429 ) ) ;
#17086=CARTESIAN_POINT ( 'NONE',  ( 75.94307401167466764, 60.53934701228696014, 3.685888554891455282 ) ) ;
#17093=CARTESIAN_POINT ( 'NONE',  ( -62.74296742027563312, 35.98356920342448717, 5.167220874066855707 ) ) ;
#17095=CARTESIAN_POINT ( 'NONE',  ( 81.16810052477266879, 61.30343919788879248, 1.037317649801912323 ) ) ;
#17116=CARTESIAN_POINT ( 'NONE',  ( 67.11291460916432072, 58.16531518584054794, -3.996350724342223604 ) ) ;
#17120=DIRECTION ( 'NONE',  ( 0.02975940812527386875, -0.9995570907297058882, 0.000000000000000000 ) ) ;
#17122=CARTESIAN_POINT ( 'NONE',  ( 78.67056111734979140, 66.04450893328514383, 1.166167023198347641 ) ) ;
#17129=CARTESIAN_POINT ( 'NONE',  ( 78.82816376705464734, 65.99584493362826265, 1.862141363775771108 ) ) ;
#17132=CARTESIAN_POINT ( 'NONE',  ( 79.47877296666170821, 61.98342160143342738, -3.470679136763286543 ) ) ;
#17138=CARTESIAN_POINT ( 'NONE',  ( 81.49447160051741434, 61.73183938760860912, -1.953285432042047853 ) ) ;
#17139=CARTESIAN_POINT ( 'NONE',  ( 79.14505932034367675, 62.66850290118684796, 3.750642650174859760 ) ) ;
#17143=CARTESIAN_POINT ( 'NONE',  ( 82.56222392620333039, 63.90769089702598649, 1.153249692834613427 ) ) ;
#17165=CARTESIAN_POINT ( 'NONE',  ( 66.27376694608996388, 57.73522568913447373, 4.000000000000000000 ) ) ;
#17166=CARTESIAN_POINT ( 'NONE',  ( 72.50225525176000474, 58.97572275893025306, -3.745173303611597948 ) ) ;
#17168=EDGE_LOOP ( 'NONE', ( #37662, #23516, #21296, #26619 ) ) ;
#17172=CARTESIAN_POINT ( 'NONE',  ( -81.07947155388369254, 30.81399289130168384, -46.17089178453873188 ) ) ;
#17181=CARTESIAN_POINT ( 'NONE',  ( 79.59524243168472424, 64.21532580903935639, -3.665158340976947038 ) ) ;
#17183=CARTESIAN_POINT ( 'NONE',  ( 79.94486516293738987, 63.68863865526455470, 3.714073935154435624 ) ) ;
#17191=CARTESIAN_POINT ( 'NONE',  ( -62.86576508122315943, 38.67912974266877058, -7.000000000000000000 ) ) ;
#17200=CARTESIAN_POINT ( 'NONE',  ( 80.03809576917893764, 64.85583152007151853, 3.406228740995816295 ) ) ;
#17210=CARTESIAN_POINT ( 'NONE',  ( 68.15116243724637002, 58.05457144382717871, 3.974537232972704892 ) ) ;
#17214=CARTESIAN_POINT ( 'NONE',  ( 80.45813098276144615, 63.95641783144333203, -3.614389211669655655 ) ) ;
#17218=ORIENTED_EDGE ( 'NONE', *, *, #6829, .T. ) ;
#17224=CARTESIAN_POINT ( 'NONE',  ( 80.17861389908763670, 63.81053541282437180, -3.679799701112256294 ) ) ;
#17226=CARTESIAN_POINT ( 'NONE',  ( 79.39546522070097012, 65.15502244391696252, 3.213872034465147909 ) ) ;
#17230=EDGE_CURVE ( 'NONE', #34912, #1373, #32504, .T. ) ;
#17231=EDGE_CURVE ( 'NONE', #9551, #30327, #27314, .T. ) ;
#17237=DIRECTION ( 'NONE',  ( -0.8888117386314180468, -0.4582725098355734938, 0.000000000000000000 ) ) ;
#17245=CARTESIAN_POINT ( 'NONE',  ( 79.58537830805853730, 65.88021587146288027, 2.518708746844645407 ) ) ;
#17266=CARTESIAN_POINT ( 'NONE',  ( 66.27376694609004915, 57.73522568913436004, -4.000000000000000000 ) ) ;
#17270=CARTESIAN_POINT ( 'NONE',  ( -56.24615026952713492, 30.21122693717869367, -1.618048866027542498 ) ) ;
#17274=ORIENTED_EDGE ( 'NONE', *, *, #14222, .F. ) ;
#17276=CARTESIAN_POINT ( 'NONE',  ( 81.88210331175112344, 61.92077230045136105, -1.461108304022173732 ) ) ;
#17284=CARTESIAN_POINT ( 'NONE',  ( 75.27909492816711179, 60.48191808705185224, 3.786335567263138469 ) ) ;
#17290=CARTESIAN_POINT ( 'NONE',  ( -62.78665125536710434, 35.69261095098032399, 5.591393777931260800 ) ) ;
#17292=CARTESIAN_POINT ( 'NONE',  ( 79.16788024942142954, 66.21349342525120107, 1.524764441711115914 ) ) ;
#17311=CARTESIAN_POINT ( 'NONE',  ( 67.47105843325410035, 58.09313517554802075, -3.997566301760142160 ) ) ;
#17317=CARTESIAN_POINT ( 'NONE',  ( -60.05933043039491537, 24.84364830758654108, 9.240995299818667519 ) ) ;
#17324=CARTESIAN_POINT ( 'NONE',  ( 79.89688848262225918, 64.77169266163326711, 3.452358620554652813 ) ) ;
#17328=ORIENTED_EDGE ( 'NONE', *, *, #29288, .T. ) ;
#17329=CARTESIAN_POINT ( 'NONE',  ( 78.16578481971130543, 61.75018358139118391, -3.687756614093558039 ) ) ;
#17332=CARTESIAN_POINT ( 'NONE',  ( 81.53696963055698177, 62.69563756174608926, -2.920975158733595034 ) ) ;
#17333=CARTESIAN_POINT ( 'NONE',  ( 78.94057287092958575, 63.80484286357250312, 3.729426069516721398 ) ) ;
#17336=CARTESIAN_POINT ( 'NONE',  ( 82.47129118679434612, 63.86074534520110291, 1.718006205139013698 ) ) ;
#17339=CARTESIAN_POINT ( 'NONE',  ( -63.02437332573797590, 35.53684452423017603, -6.244480380085997595 ) ) ;
#17350=CARTESIAN_POINT ( 'NONE',  ( -64.85784325972055342, 34.81586596186931359, -6.466735817496061856 ) ) ;
#17352=CARTESIAN_POINT ( 'NONE',  ( -66.99872204295122913, 28.48507918597134037, -46.17089178453873188 ) ) ;
#17359=CARTESIAN_POINT ( 'NONE',  ( 66.58940539569050543, 57.77934511969053943, 3.999344142514785538 ) ) ;
#17360=EDGE_CURVE ( 'NONE', #27566, #38693, #14341, .T. ) ;
#17361=CARTESIAN_POINT ( 'NONE',  ( 71.03485184658521234, 59.25305893485334963, -3.963404584535439312 ) ) ;
#17367=DIRECTION ( 'NONE',  ( -1.000000000000000000, -2.192388006395421260E-15, 0.000000000000000000 ) ) ;
#17374=CARTESIAN_POINT ( 'NONE',  ( 80.23208661909926320, 62.50324886901235999, -3.482780605906225624 ) ) ;
#17376=CARTESIAN_POINT ( 'NONE',  ( 80.63281215842032168, 62.09153919268370458, 3.087291694836661549 ) ) ;
#17389=DIRECTION ( 'NONE',  ( -1.000000000000000000, 0.000000000000000000, 0.000000000000000000 ) ) ;
#17391=CARTESIAN_POINT ( 'NONE',  ( 81.30779604900573077, 61.65202803940792364, 2.079311677127710478 ) ) ;
#17398=CARTESIAN_POINT ( 'NONE',  ( -64.16905995053024014, 35.05897458415617507, 4.706112250371591088 ) ) ;
#17401=CARTESIAN_POINT ( 'NONE',  ( 67.64019463258649978, 58.53452770292938112, 3.982857479566666914 ) ) ;
#17403=EDGE_CURVE ( 'NONE', #38693, #31247, #3465, .T. ) ;
#17408=CARTESIAN_POINT ( 'NONE',  ( 80.38808068765766279, 63.91986139366765940, -3.633989118465184021 ) ) ;
#17411=CARTESIAN_POINT ( 'NONE',  ( -58.37631287976132199, 28.09510535829622668, 3.265447219236210952 ) ) ;
#17416=CARTESIAN_POINT ( 'NONE',  ( 81.07747211222714157, 61.58128768033695621, -2.227525437860508273 ) ) ;
#17418=CARTESIAN_POINT ( 'NONE',  ( 80.00358288781701788, 64.08847832824501722, 3.683925914261491741 ) ) ;
#17420=CARTESIAN_POINT ( 'NONE',  ( -59.00110696496997775, 28.68040728033253473, 6.999999999999999112 ) ) ;
#17424=CARTESIAN_POINT ( 'NONE',  ( -63.08758708074093136, 38.76906266698303227, -4.000000000000000000 ) ) ;
#17425=CARTESIAN_POINT ( 'NONE',  ( -63.71197174466732349, 35.78007194159061299, -7.175960652854968203 ) ) ;
#17435=CARTESIAN_POINT ( 'NONE',  ( -72.95330471031414277, 33.71485196875532608, -46.17089178453873188 ) ) ;
#17436=CARTESIAN_POINT ( 'NONE',  ( 79.64807995744904190, 65.91648781524679634, 2.476693319890303613 ) ) ;
#17439=ORIENTED_EDGE ( 'NONE', *, *, #14666, .F. ) ;
#17449=EDGE_LOOP ( 'NONE', ( #7077, #5896, #19940, #14741 ) ) ;
#17457=EDGE_LOOP ( 'NONE', ( #3220, #34909, #29586, #20058, #15725 ) ) ;
#17460=CARTESIAN_POINT ( 'NONE',  ( 66.27376694609004915, 57.73522568913436004, -4.000000000000000000 ) ) ;
#17461=ORIENTED_EDGE ( 'NONE', *, *, #22935, .F. ) ;
#17474=CARTESIAN_POINT ( 'NONE',  ( 81.94850308769507308, 64.73378216408549690, -2.360008641315554545 ) ) ;
#17480=CARTESIAN_POINT ( 'NONE',  ( 73.81116006253010653, 62.20691382096256206, 3.564124015814260638 ) ) ;
#17488=CARTESIAN_POINT ( 'NONE',  ( 81.67793621607884802, 64.59267988934881544, 2.776691787112188337 ) ) ;
#17503=DIRECTION ( 'NONE',  ( 0.000000000000000000, 0.000000000000000000, 1.000000000000000000 ) ) ;
#17510=CARTESIAN_POINT ( 'NONE',  ( 67.47898117768387749, 58.07151159967423126, -3.997009152755514272 ) ) ;
#17514=CARTESIAN_POINT ( 'NONE',  ( 77.73224247307464907, 65.38057827825358004, 2.040387096976575609 ) ) ;
#17518=ORIENTED_EDGE ( 'NONE', *, *, #9092, .T. ) ;
#17520=CARTESIAN_POINT ( 'NONE',  ( 81.96245566837727381, 61.96131850323955348, -1.129532193886523261 ) ) ;
#17521=CARTESIAN_POINT ( 'NONE',  ( 81.04779914310620370, 62.47515088512101755, 3.146509185145925258 ) ) ;
#17524=CARTESIAN_POINT ( 'NONE',  ( 78.50009633871027859, 63.24008633025189852, -3.804514705604310709 ) ) ;
#17529=CARTESIAN_POINT ( 'NONE',  ( 81.00465555258324457, 64.24153452434936185, -3.375310687856056813 ) ) ;
#17530=CARTESIAN_POINT ( 'NONE',  ( 77.99157368707381011, 64.87245838797727515, 2.976941560848442858 ) ) ;
#17536=EDGE_CURVE ( 'NONE', #38011, #30864, #35156, .T. ) ;
#17538=CARTESIAN_POINT ( 'NONE',  ( 81.72179206571547638, 61.68197623675726504, 1.214491505233688873 ) ) ;
#17563=CARTESIAN_POINT ( 'NONE',  ( 66.27376694608996388, 57.73522568913447373, 4.000000000000000000 ) ) ;
#17564=CARTESIAN_POINT ( 'NONE',  ( 71.58333764992288195, 61.16654152266917777, -3.647993048544889039 ) ) ;
#17577=CARTESIAN_POINT ( 'NONE',  ( 79.89038670178254620, 63.31421865134938542, -3.734652355492745102 ) ) ;
#17581=CARTESIAN_POINT ( 'NONE',  ( 80.12334914806359620, 63.07862483458217895, 3.671038198312436496 ) ) ;
#17590=EDGE_LOOP ( 'NONE', ( #27635, #22047, #39702, #34126, #16248 ) ) ;
#17597=CARTESIAN_POINT ( 'NONE',  ( 78.90480995596031732, 66.05426212177788159, 1.786209778413370586 ) ) ;
#17609=CARTESIAN_POINT ( 'NONE',  ( 67.99537475662653208, 58.47140781303536983, 3.994255761866590149 ) ) ;
#17625=CARTESIAN_POINT ( 'NONE',  ( 80.94504091708289195, 61.55080574620870237, -2.311104455577556394 ) ) ;
#17627=CARTESIAN_POINT ( 'NONE',  ( 80.97304215327375232, 61.92799980795010839, 2.787474064117264838 ) ) ;
#17631=CARTESIAN_POINT ( 'NONE',  ( 73.62310697524999625, 61.12246817794784448, -3.899931323576832920 ) ) ;
#17638=ADVANCED_FACE ( 'NONE', ( #5138 ), #15461, .T. ) ;
#17649=CARTESIAN_POINT ( 'NONE',  ( 81.16342859510598373, 63.93697670171856373, 3.375310687858766645 ) ) ;
#17676=CARTESIAN_POINT ( 'NONE',  ( 80.94990806105060699, 62.43782317439323037, -3.178394274514594997 ) ) ;
#17684=CARTESIAN_POINT ( 'NONE',  ( 82.01669802222831152, 64.37834105533548268, -2.512558077908312537 ) ) ;
#17693=CARTESIAN_POINT ( 'NONE',  ( 75.40715271138134312, 60.19559828969859439, 3.661998389317127511 ) ) ;
#17701=CARTESIAN_POINT ( 'NONE',  ( 81.68772813446398118, 64.20773789716577085, 2.952528780688829624 ) ) ;
#17727=ORIENTED_EDGE ( 'NONE', *, *, #20824, .F. ) ;
#17729=CARTESIAN_POINT ( 'NONE',  ( 81.35706873939176376, 65.93413826765579699, -1.000000000000000000 ) ) ;
#17730=CARTESIAN_POINT ( 'NONE',  ( 80.41878079785790590, 63.93588341273047604, 3.625945587094184130 ) ) ;
#17733=CARTESIAN_POINT ( 'NONE',  ( 78.55649010480105687, 62.41317512920502963, -3.780406938340844736 ) ) ;
#17736=CARTESIAN_POINT ( 'NONE',  ( 79.18807306865505780, 66.05665914930281701, -1.983726836935526761 ) ) ;
#17738=CARTESIAN_POINT ( 'NONE',  ( 79.99044059672593221, 61.67469478680249750, 3.091829831932955575 ) ) ;
#17742=CIRCLE ( 'NONE', #38, 2.999999999999998668 ) ;
#17746=ORIENTED_EDGE ( 'NONE', *, *, #11125, .F. ) ;
#17747=CARTESIAN_POINT ( 'NONE',  ( 79.32563386639218095, 66.29995228605849888, 1.174937739208267606 ) ) ;
#17771=ORIENTED_EDGE ( 'NONE', *, *, #19410, .F. ) ;
#17772=CARTESIAN_POINT ( 'NONE',  ( 66.57962043698374544, 57.80678959376348303, 3.999745625240549440 ) ) ;
#17773=CARTESIAN_POINT ( 'NONE',  ( 69.50581201620700256, 59.72791825745761685, -3.883859131414829413 ) ) ;
#17779=PRODUCT_DEFINITION_SHAPE ( 'NONE', 'NONE',  #32149 ) ;
#17789=CARTESIAN_POINT ( 'NONE',  ( 79.04765299714190974, 64.87162515256788708, -3.322373183921396578 ) ) ;
#17792=CARTESIAN_POINT ( 'NONE',  ( 81.67965074903506206, 61.82017115420519104, -1.781440269582274416 ) ) ;
#17793=CARTESIAN_POINT ( 'NONE',  ( 80.80054865964804378, 61.51733283104051964, 2.392122129321804902 ) ) ;
#17801=CIRCLE ( 'NONE', #13888, 5.681288188914806803 ) ;
#17815=PLANE ( 'NONE',  #6308 ) ;
#17818=CARTESIAN_POINT ( 'NONE',  ( 67.80923286766689273, 58.07768331974902765, 3.990378031984522789 ) ) ;
#17831=CARTESIAN_POINT ( 'NONE',  ( 79.73288524454797255, 64.30401648905855438, -3.644176963625960664 ) ) ;
#17833=CARTESIAN_POINT ( 'NONE',  ( 81.09158065085932776, 61.31869227828926938, 1.634613895560438124 ) ) ;
#17837=CARTESIAN_POINT ( 'NONE',  ( 74.36844136632052482, 60.98005461696732254, -3.924711207976818717 ) ) ;
#17853=CARTESIAN_POINT ( 'NONE',  ( 80.25728969398844015, 65.34460247849791870, 3.089171411838283809 ) ) ;
#17855=DIRECTION ( 'NONE',  ( 0.8831583674550994578, -0.4690749385695672791, 0.000000000000000000 ) ) ;
#17865=VERTEX_POINT ( 'NONE', #22630 ) ;
#17870=CARTESIAN_POINT ( 'NONE',  ( 81.02128870047407361, 63.12856183665077481, -3.380792992375200701 ) ) ;
#17884=CARTESIAN_POINT ( 'NONE',  ( 81.02339296473685692, 62.20010510126473235, -2.956864960647744844 ) ) ;
#17890=ORIENTED_EDGE ( 'NONE', *, *, #10159, .T. ) ;
#17892=CARTESIAN_POINT ( 'NONE',  ( 82.10888692569052694, 64.42619117010471541, -2.360008641315554545 ) ) ;
#17893=CYLINDRICAL_SURFACE ( 'NONE', #945, 2.681419499219045655 ) ;
#17899=CARTESIAN_POINT ( 'NONE',  ( 75.87451422959399849, 60.69085731309660758, 3.756674307851894490 ) ) ;
#17903=CARTESIAN_POINT ( 'NONE',  ( -73.07498068578524908, 39.58105274722134226, -9.800414904976365804 ) ) ;
#17906=CARTESIAN_POINT ( 'NONE',  ( 81.89445579901088479, 62.31310441928819444, 2.222430037835991801 ) ) ;
#17912=EDGE_CURVE ( 'NONE', #21175, #25652, #13944, .T. ) ;
#17913=LINE ( 'NONE', #37061, #25750 ) ;
#17926=CARTESIAN_POINT ( 'NONE',  ( 67.02763120020985355, 57.94366503926806899, -3.998791315154376136 ) ) ;
#17927=EDGE_CURVE ( 'NONE', #38693, #28971, #2666, .T. ) ;
#17928=CARTESIAN_POINT ( 'NONE',  ( -58.99872204295123623, 28.48507918597136523, -6.834244957304557389 ) ) ;
#17940=CARTESIAN_POINT ( 'NONE',  ( 82.35470118046110599, 62.54510421749741056, -1.000000000000000000 ) ) ;
#17941=CARTESIAN_POINT ( 'NONE',  ( 80.38808068765764858, 63.91986139366765940, 3.633989118465185797 ) ) ;
#17944=CARTESIAN_POINT ( 'NONE',  ( 78.66234234182429930, 62.19549841187283334, -3.710351296122902820 ) ) ;
#17947=CARTESIAN_POINT ( 'NONE',  ( 81.45253739226865264, 61.71286443377192654, -1.983726836935522542 ) ) ;
#17948=CARTESIAN_POINT ( 'NONE',  ( 78.81457101317378999, 64.04164361847183784, 3.641957811749153784 ) ) ;
#17952=CARTESIAN_POINT ( 'NONE',  ( 82.50731566719309740, 63.18365725368109764, 1.509105202934762024 ) ) ;
#17960=CIRCLE ( 'NONE', #5485, 1.000000000000000666 ) ;
#17970=DIRECTION ( 'NONE',  ( -0.000000000000000000, 0.000000000000000000, 1.000000000000000000 ) ) ;
#17979=CARTESIAN_POINT ( 'NONE',  ( 66.57766344320866381, 57.81227849924184881, 3.999802976169922974 ) ) ;
#17980=CARTESIAN_POINT ( 'NONE',  ( 68.95366548541680629, 59.44408286695458798, -3.907754234428187257 ) ) ;
#17998=CARTESIAN_POINT ( 'NONE',  ( 78.47662320409183678, 65.68507013823818852, -2.197205184446134218 ) ) ;
#18001=CARTESIAN_POINT ( 'NONE',  ( 79.40575531231831974, 66.18134094231184861, -1.781440269582275970 ) ) ;
#18002=CARTESIAN_POINT ( 'NONE',  ( 79.22323586724850486, 64.66701280635210480, 3.467090974304451123 ) ) ;
#18026=CARTESIAN_POINT ( 'NONE',  ( 67.73962338513339887, 58.26590004628993569, 3.997461085607390885 ) ) ;
#18039=CARTESIAN_POINT ( 'NONE',  ( 79.43051736299561583, 64.82585401503283151, -3.419027627190938556 ) ) ;
#18041=CARTESIAN_POINT ( 'NONE',  ( 79.20065834867811816, 65.31285345095548678, 3.018898740118463486 ) ) ;
#18043=CARTESIAN_POINT ( 'NONE',  ( -63.99293516169446150, 35.89893413629672381, 7.506047544094577084 ) ) ;
#18046=CARTESIAN_POINT ( 'NONE',  ( 73.75428705932469597, 62.33035115498116596, -3.485789274173696661 ) ) ;
#18052=CARTESIAN_POINT ( 'NONE',  ( 81.62248346935344046, 65.70993096190733240, 1.000000000000000000 ) ) ;
#18059=CARTESIAN_POINT ( 'NONE',  ( 81.41366110773391540, 61.69541933536105915, 2.011547652603478564 ) ) ;
#18064=B_SPLINE_CURVE_WITH_KNOTS ( 'NONE', 3,
 ( #24768, #9112, #24977, #12609, #21687, #34265, #25176, #28052, #6239, #40601, #9308, #31362 ),
 .UNSPECIFIED., .F., .F.,
 ( 4, 2, 2, 2, 2, 4 ),
 ( 1.734723475976807094E-18, 0.0007700302096414094822, 0.001155045314462114494, 0.001540060419282819181, 0.002310090628924224218, 0.003080120838565629255 ),
 .UNSPECIFIED. ) ;
#18080=CARTESIAN_POINT ( 'NONE',  ( 81.14908696703564317, 61.29647948322620010, -1.137963815189213079 ) ) ;
#18085=ORIENTED_EDGE ( 'NONE', *, *, #25757, .T. ) ;
#18089=CARTESIAN_POINT ( 'NONE',  ( 80.11713744326790732, 64.15277314745162585, -3.661914029440275886 ) ) ;
#18090=CARTESIAN_POINT ( 'NONE',  ( -59.07422214908517333, 27.36241337473656543, -4.461357708502241337 ) ) ;
#18094=CARTESIAN_POINT ( 'NONE',  ( 82.22574661183148237, 63.03983423078044268, -2.217414436011609702 ) ) ;
#18102=CARTESIAN_POINT ( 'NONE',  ( 74.35309583984513893, 59.45637312398173435, 3.556895493431092348 ) ) ;
#18109=CARTESIAN_POINT ( 'NONE',  ( 81.65405438441128183, 61.80769279848060194, 1.809109834152203833 ) ) ;
#18116=DIRECTION ( 'NONE',  ( 0.4582725098355734938, -0.8888117386314180468, 0.000000000000000000 ) ) ;
#18125=VECTOR ( 'NONE', #32305, 1000.000000000000000 ) ;
#18131=CARTESIAN_POINT ( 'NONE',  ( 67.05223802139354916, 57.87567627276845883, -3.996315564296191614 ) ) ;
#18133=CIRCLE ( 'NONE', #32633, 79.54614097552274643 ) ;
#18136=ORIENTED_EDGE ( 'NONE', *, *, #9092, .F. ) ;
#18146=CARTESIAN_POINT ( 'NONE',  ( 82.26973386304365476, 64.90130211351629441, -1.165579324820864571 ) ) ;
#18148=CARTESIAN_POINT ( 'NONE',  ( 79.82480777417542583, 64.72726844050397688, 3.473545878414594945 ) ) ;
#18151=CARTESIAN_POINT ( 'NONE',  ( 77.74023705119593330, 64.68384637002907311, -3.042889847487472377 ) ) ;
#18155=CARTESIAN_POINT ( 'NONE',  ( 79.52751932687164071, 65.84655314362404965, -2.556731990913035268 ) ) ;
#18156=CARTESIAN_POINT ( 'NONE',  ( 76.19453532209956848, 64.30418437363988460, 2.661196496273629641 ) ) ;
#18159=CARTESIAN_POINT ( 'NONE',  ( 82.20671311902191292, 64.86843738523491254, 1.633153239554254732 ) ) ;
#18173=DIRECTION ( 'NONE',  ( 0.000000000000000000, 0.000000000000000000, 1.000000000000000000 ) ) ;
#18176=AXIS2_PLACEMENT_3D ( 'NONE', #13819, #38919, #36058 ) ;
#18187=CARTESIAN_POINT ( 'NONE',  ( 69.92361841086972163, 58.66916198470556765, -3.954846139149859052 ) ) ;
#18192=CARTESIAN_POINT ( 'NONE',  ( 69.97231107847817100, 58.54512925548123548, 3.931953536312681852 ) ) ;
#18198=DIRECTION ( 'NONE',  ( 0.8831583674550981256, -0.4690749385695702767, 0.000000000000000000 ) ) ;
#18202=CARTESIAN_POINT ( 'NONE',  ( 80.79577214038279465, 61.23497056275883921, -1.884339924308600311 ) ) ;
#18204=CARTESIAN_POINT ( 'NONE',  ( 81.76017987128373932, 63.49575590176120699, -2.919551171211517637 ) ) ;
#18205=CARTESIAN_POINT ( 'NONE',  ( 78.63268743221328805, 65.61080103085718918, 2.414331286641656860 ) ) ;
#18213=FACE_OUTER_BOUND ( 'NONE', #39574, .T. ) ;
#18224=( GEOMETRIC_REPRESENTATION_CONTEXT ( 3 ) GLOBAL_UNCERTAINTY_ASSIGNED_CONTEXT ( ( #13100 ) ) GLOBAL_UNIT_ASSIGNED_CONTEXT ( ( #32951, #16876, #32356 ) ) REPRESENTATION_CONTEXT ( 'NONE', 'WORKASPACE' ) );
#18232=CARTESIAN_POINT ( 'NONE',  ( 67.16623404331231484, 58.01883467879599721, 3.998868826385353348 ) ) ;
#18241=DIRECTION ( 'NONE',  ( 0.000000000000000000, 0.000000000000000000, 1.000000000000000000 ) ) ;
#18246=CARTESIAN_POINT ( 'NONE',  ( 81.00792578075066785, 61.24501526813143215, -1.386845825021845835 ) ) ;
#18247=PRODUCT_DEFINITION_FORMATION_WITH_SPECIFIED_SOURCE ( 'ANY', '', #101, .NOT_KNOWN. ) ;
#18250=CARTESIAN_POINT ( 'NONE',  ( 78.96452808758097319, 65.70328965153828449, 2.526545245021019515 ) ) ;
#18253=CARTESIAN_POINT ( 'NONE',  ( 73.91602183453733232, 60.46016365699546924, -3.923277237800833817 ) ) ;
#18259=ORIENTED_EDGE ( 'NONE', *, *, #19865, .F. ) ;
#18265=CARTESIAN_POINT ( 'NONE',  ( 81.15996319168235118, 61.30045982539699168, 1.094381639753812863 ) ) ;
#18285=CARTESIAN_POINT ( 'NONE',  ( 80.10206815703587324, 64.89240018571257451, -3.380792992375218908 ) ) ;
#18292=EDGE_LOOP ( 'NONE', ( #19971, #32360, #9251, #28273 ) ) ;
#18295=CARTESIAN_POINT ( 'NONE',  ( 80.72665634072043872, 62.99526239489093626, -3.473545878414585175 ) ) ;
#18296=AXIS2_PLACEMENT_3D ( 'NONE', #10375, #35320, #10162 ) ;
#18302=CARTESIAN_POINT ( 'NONE',  ( 79.25820086742456283, 66.26332994521369812, -1.378120381825871599 ) ) ;
#18303=CARTESIAN_POINT ( 'NONE',  ( -58.99872204295125755, 28.26327478256369119, 6.631997745856873294 ) ) ;
#18308=CARTESIAN_POINT ( 'NONE',  ( 73.01418189060618147, 60.96508932706621664, 3.894134109168990499 ) ) ;
#18313=CARTESIAN_POINT ( 'NONE',  ( -58.49085810542278807, 30.53062561304904676, -5.010110517852434775 ) ) ;
#18316=CARTESIAN_POINT ( 'NONE',  ( 80.65441534633353626, 65.56043466500607053, 2.771525467261984232 ) ) ;
#18328=CARTESIAN_POINT ( 'NONE',  ( -74.03402466285142225, 19.33157623370700051, -8.800414904976364028 ) ) ;
#18335=CARTESIAN_POINT ( 'NONE',  ( 67.01778322055632486, 57.97087264248310134, -3.999241514195644775 ) ) ;
#18349=CARTESIAN_POINT ( 'NONE',  ( 82.59411735159429213, 63.56171878218356852, -1.145133701562419226 ) ) ;
#18352=CARTESIAN_POINT ( 'NONE',  ( 79.98933190693155382, 64.46315002137730232, 3.592474444481858153 ) ) ;
#18356=CARTESIAN_POINT ( 'NONE',  ( 77.90315483005265662, 60.81789388943194297, -3.308002540436226990 ) ) ;
#18359=CARTESIAN_POINT ( 'NONE',  ( -63.96695182803187407, 19.27020452292898867, -9.800414904976365804 ) ) ;
#18360=CARTESIAN_POINT ( 'NONE',  ( 81.24747667584206567, 63.59436251575137078, -3.343039074468323157 ) ) ;
#18361=CARTESIAN_POINT ( 'NONE',  ( 77.25343114543986189, 63.60010822905029215, 3.597602401604568012 ) ) ;
#18367=CARTESIAN_POINT ( 'NONE',  ( 82.29094429576495884, 64.52076745355572029, 1.905332024690495007 ) ) ;
#18373=CARTESIAN_POINT ( 'NONE',  ( -62.76544114002936681, 35.76323014769233311, 5.464922856233965121 ) ) ;
#18386=LINE ( 'NONE', #28266, #28623 ) ;
#18394=CARTESIAN_POINT ( 'NONE',  ( 70.83363217041421933, 59.75074159095914439, -3.963404584535426434 ) ) ;
#18406=AXIS2_PLACEMENT_3D ( 'NONE', #10007, #28961, #29361 ) ;
#18409=CARTESIAN_POINT ( 'NONE',  ( 80.39537321288027272, 61.58102678004055264, -2.797036776683079040 ) ) ;
#18411=CARTESIAN_POINT ( 'NONE',  ( 81.16673370561979084, 65.10603640127597203, -2.903340743335492302 ) ) ;
#18412=CARTESIAN_POINT ( 'NONE',  ( 80.76403243373638929, 61.15693784680268408, 1.612955153530313268 ) ) ;
#18427=CARTESIAN_POINT ( 'NONE',  ( -69.08758708074093136, 36.88538962427716683, -8.800414904976364028 ) ) ;
#18428=CARTESIAN_POINT ( 'NONE',  ( -75.45330471031414277, 33.71485196875532608, 8.800414904976364028 ) ) ;
#18434=EDGE_LOOP ( 'NONE', ( #21393, #15263, #33431, #25736, #25373, #15786, #27159, #29301 ) ) ;
#18435=CARTESIAN_POINT ( 'NONE',  ( 67.18400333313441308, 57.97000644093014188, 3.997693602769901045 ) ) ;
#18442=CIRCLE ( 'NONE', #26972, 1.000000000000005551 ) ;
#18454=CARTESIAN_POINT ( 'NONE',  ( 79.01373585440697411, 65.47072129778472060, -2.830664096605183033 ) ) ;
#18456=CARTESIAN_POINT ( 'NONE',  ( 80.36115745751311579, 63.17601289530517761, 3.638935937159312850 ) ) ;
#18464=CARTESIAN_POINT ( 'NONE',  ( -54.79610818216033152, 31.51396769785350926, 1.000000000000000000 ) ) ;
#18469=DIRECTION ( 'NONE',  ( 0.02975940812527386875, -0.9995570907297058882, 0.000000000000000000 ) ) ;
#18471=CARTESIAN_POINT ( 'NONE',  ( 81.38674634791392748, 61.68395714348712033, 2.028924249969739080 ) ) ;
#18475=CARTESIAN_POINT ( 'NONE',  ( -64.16206517525715469, 35.04753771064019929, -4.696770012396532579 ) ) ;
#18479=FACE_OUTER_BOUND ( 'NONE', #32044, .T. ) ;
#18485=CARTESIAN_POINT ( 'NONE',  ( 79.08570711028920641, 65.99300539798551313, -2.058202901128790785 ) ) ;
#18486=CARTESIAN_POINT ( 'NONE',  ( -63.99293516169446150, 35.89893413629672381, 7.506047544094577084 ) ) ;
#18498=CIRCLE ( 'NONE', #23761, 7.999999999999992895 ) ;
#18501=CARTESIAN_POINT ( 'NONE',  ( 80.46181058475264081, 63.58258928487767037, -3.654032574946328271 ) ) ;
#18502=CARTESIAN_POINT ( 'NONE',  ( -59.46024017484872815, 26.94883531126003007, -5.502890977078439327 ) ) ;
#18507=CARTESIAN_POINT ( 'NONE',  ( 81.98137654593473655, 62.63634409986672580, -2.334361474589122132 ) ) ;
#18513=CARTESIAN_POINT ( 'NONE',  ( 73.91602183453733232, 60.46016365699546924, 3.923277237800832928 ) ) ;
#18515=ORIENTED_EDGE ( 'NONE', *, *, #24126, .T. ) ;
#18521=CARTESIAN_POINT ( 'NONE',  ( -54.79610818216088575, 31.51396769785300123, -1.028983900456674538 ) ) ;
#18522=CARTESIAN_POINT ( 'NONE',  ( 81.77617677873431035, 62.02699640077097598, 2.046910133536369969 ) ) ;
#18525=CARTESIAN_POINT ( 'NONE',  ( -64.08758708074093136, 38.34299140179469134, 3.014629887202059155 ) ) ;
#18531=DIRECTION ( 'NONE',  ( 0.4690749385695657803, 0.8831583674551003460, -0.000000000000000000 ) ) ;
#18540=CARTESIAN_POINT ( 'NONE',  ( 66.81418162778464875, 58.07599004166701206, -3.996206253860483226 ) ) ;
#18542=CARTESIAN_POINT ( 'NONE',  ( -55.42153689335682998, 31.50958069423711549, 3.999999999999998668 ) ) ;
#18551=CARTESIAN_POINT ( 'NONE',  ( 81.30214557805295783, 65.90511036421341373, -1.555014038483378158 ) ) ;
#18552=CARTESIAN_POINT ( 'NONE',  ( 80.91556171499748018, 62.42588715431494961, 3.188730975143402091 ) ) ;
#18554=VERTEX_POINT ( 'NONE', #10303 ) ;
#18555=CARTESIAN_POINT ( 'NONE',  ( 76.63461511614536903, 62.03359853006622870, -3.872369636031699258 ) ) ;
#18559=CARTESIAN_POINT ( 'NONE',  ( 79.15160802321746303, 66.03480532732676522, -2.011547652602700076 ) ) ;
#18560=CARTESIAN_POINT ( 'NONE',  ( 77.67868059383667401, 64.13990294438296758, 3.401348408886265329 ) ) ;
#18561=CIRCLE ( 'NONE', #23811, 1.000000000000000000 ) ;
#18562=ORIENTED_EDGE ( 'NONE', *, *, #31254, .F. ) ;
#18565=CARTESIAN_POINT ( 'NONE',  ( 81.44533364721146995, 61.45470812716254727, 1.173033592341437004 ) ) ;
#18566=CARTESIAN_POINT ( 'NONE',  ( -64.08758708074094557, 43.44410442557501995, 1.728127058819059814 ) ) ;
#18572=CARTESIAN_POINT ( 'NONE',  ( -64.43126815475770286, 34.69310041339028317, 5.627269573384544366 ) ) ;
#18575=FACE_OUTER_BOUND ( 'NONE', #18723, .T. ) ;
#18590=EDGE_LOOP ( 'NONE', ( #31539, #7314, #12782, #26386 ) ) ;
#18592=CARTESIAN_POINT ( 'NONE',  ( 69.82526079983220768, 58.91932963963509451, -3.982895692900140894 ) ) ;
#18597=ADVANCED_FACE ( 'NONE', ( #10501 ), #11025, .T. ) ;
#18605=CARTESIAN_POINT ( 'NONE',  ( 80.57587054825803818, 61.08954103313657669, -1.748505333477117452 ) ) ;
#18607=CARTESIAN_POINT ( 'NONE',  ( 79.63061436091753365, 66.14207560456340218, -2.046910133536484100 ) ) ;
#18608=CARTESIAN_POINT ( 'NONE',  ( 78.47662320409183678, 65.68507013823818852, 2.197205184446135107 ) ) ;
#18616=ORIENTED_EDGE ( 'NONE', *, *, #26909, .T. ) ;
#18628=ADVANCED_FACE ( 'NONE', ( #36637 ), #31981, .T. ) ;
#18638=CARTESIAN_POINT ( 'NONE',  ( 67.13068300324758297, 58.11650739856835202, 3.998197261021420701 ) ) ;
#18649=LINE ( 'NONE', #9186, #27225 ) ;
#18653=CARTESIAN_POINT ( 'NONE',  ( 80.78018476400323777, 61.88220158024270035, -2.864416008774563593 ) ) ;
#18656=CARTESIAN_POINT ( 'NONE',  ( 78.99045122244679362, 65.44959329978490814, 2.843122152733565056 ) ) ;
#18659=EDGE_CURVE ( 'NONE', #33117, #12043, #21446, .T. ) ;
#18677=CARTESIAN_POINT ( 'NONE',  ( 79.92917477698721029, 65.49944209122678274, 2.989933650883223493 ) ) ;
#18695=VERTEX_POINT ( 'NONE', #19127 ) ;
#18696=CARTESIAN_POINT ( 'NONE',  ( 81.31277617166799132, 62.04138461958081763, -2.639511535887550053 ) ) ;
#18700=DIRECTION ( 'NONE',  ( -0.000000000000000000, -0.000000000000000000, -1.000000000000000000 ) ) ;
#18707=CARTESIAN_POINT ( 'NONE',  ( 80.35739993109717716, 63.53218113005920742, -3.674973878998262222 ) ) ;
#18713=CARTESIAN_POINT ( 'NONE',  ( 81.56984355495252714, 61.60674381500905383, -1.524764441711166763 ) ) ;
#18720=CARTESIAN_POINT ( 'NONE',  ( -64.08758708074093136, 41.34482390022287035, -2.999999996405878111 ) ) ;
#18721=CARTESIAN_POINT ( 'NONE',  ( 73.64144479846403613, 59.51803038729781292, 3.736020861036525531 ) ) ;
#18723=EDGE_LOOP ( 'NONE', ( #603, #29706, #30631, #8479, #2689, #22870 ) ) ;
#18728=CARTESIAN_POINT ( 'NONE',  ( -58.94581694272203265, 28.88139188076748454, -6.382668916716455421 ) ) ;
#18731=CARTESIAN_POINT ( 'NONE',  ( 81.81391746733756065, 63.52311930392516359, 2.869341960395463520 ) ) ;
#18734=VERTEX_POINT ( 'NONE', #9237 ) ;
#18746=DIRECTION ( 'NONE',  ( 0.3757233601570964532, 0.9267318687906771491, -0.000000000000000000 ) ) ;
#18751=CARTESIAN_POINT ( 'NONE',  ( 66.69989039061726999, 57.93340768760646142, -3.999416444362182688 ) ) ;
#18753=CIRCLE ( 'NONE', #26645, 1.000000000000000000 ) ;
#18756=CARTESIAN_POINT ( 'NONE',  ( -56.64002613362055882, 29.83241628681511770, 1.779850828381770445 ) ) ;
#18765=CARTESIAN_POINT ( 'NONE',  ( 81.95295003160654801, 61.95651309483395153, -1.189854999565593818 ) ) ;
#18766=CARTESIAN_POINT ( 'NONE',  ( 79.29422675899259332, 65.38839789421687954, 2.978180346930987099 ) ) ;
#18769=CARTESIAN_POINT ( 'NONE',  ( 75.68803578311077729, 63.95394130778559116, -2.805892758485396765 ) ) ;
#18773=CARTESIAN_POINT ( 'NONE',  ( 81.20101650719858810, 62.86240828450102924, -3.233552917234641555 ) ) ;
#18774=CARTESIAN_POINT ( 'NONE',  ( 78.95923394621949853, 61.57577394195569553, 3.401348408886338159 ) ) ;
#18776=DIRECTION ( 'NONE',  ( -0.9949204587440765302, -0.1006641980670203163, 0.000000000000000000 ) ) ;
#18778=CARTESIAN_POINT ( 'NONE',  ( 82.29984285855105952, 63.07754316838597219, 2.094266784918906943 ) ) ;
#18786=EDGE_CURVE ( 'NONE', #12131, #20345, #11021, .T. ) ;
#18796=CARTESIAN_POINT ( 'NONE',  ( -56.02725819615764635, 27.69325783080268266, -46.17089178453873188 ) ) ;
#18805=CARTESIAN_POINT ( 'NONE',  ( 68.17490759376208587, 57.99096015551094041, -3.964697573200900660 ) ) ;
#18811=B_SPLINE_SURFACE_WITH_KNOTS ( 'NONE', 3, 3, ( 
 ( #10951, #36099, #16530, #29107, #22937, #17940, #8880, #39565, #24330, #5608, #34037, #40179, #24121, #15268, #30521, #27819, #17729, #15064, #11959, #12176, #8673, #36287, #21462, #27215, #24536 ),
 ( #39776, #5810, #2745, #2331, #14852, #11550, #8063, #37091, #18349, #36689, #11753, #14448, #18146, #30939, #30735, #20623, #8469, #27622, #11348, #5197, #23913, #2539, #27418, #40371, #33209 ),
 ( #1925, #30315, #4995, #17520, #30116, #27019, #2126, #21254, #36489, #8261, #20832, #33428, #14643, #21053, #33625, #5400, #36895, #39981, #33825, #25363, #6633, #3558, #31744, #31135, #24955 ),
 ( #3164, #16085, #24746, #18765, #22286, #37491, #28031, #28652, #28855, #37295, #31956, #9089, #19180, #34442, #663, #459, #37900, #9286, #38106, #56, #12586, #15882, #6828, #25152, #9492 ),
 ( #21665, #3760, #34243, #12997, #6219, #6015, #25562, #9707, #21865, #9910, #37687, #22079, #28441, #19385, #34653, #22490, #18551, #2953, #6424, #18981, #28229, #35054, #15470, #15681, #31544 ),
 ( #40577, #12387, #12787, #16285, #31339, #3367, #249, #34856, #36049, #7629, #32560, #29655, #23087, #10102, #38505, #39108, #23281, #866, #19787, #23482, #1073, #26571, #7421, #22884, #13810 ),
 ( #19979, #32957, #35454, #32764, #1466, #29857, #26378, #13200, #10906, #4156, #14000, #17078, #4553, #25971, #7826, #13604, #35848, #22688, #10307, #20375, #7226, #35651, #20181, #38910, #10505 ),
 ( #4743, #25769, #16674, #17276, #16485, #32361, #13398, #38305, #4359, #35255, #7023, #29258, #19591, #32167, #26176, #3966, #29058, #38709, #16880, #29460, #10702, #1271, #4945, #15016, #24488 ),
 ( #14803, #26971, #2083, #11102, #27579, #33380, #39933, #8627, #40132, #21413, #36240, #17892, #17474, #20786, #21206, #1668, #36439, #11708, #1877, #30065, #11912, #14401, #18302, #36643, #26775 ),
 ( #5761, #14202, #8828, #39313, #36844, #11298, #23674, #18094, #2279, #39517, #37044, #17684, #30265, #33577, #33989, #14596, #33778, #8019, #20572, #27167, #24071, #5149, #33159, #23863, #39724 ),
 ( #11505, #8422, #8212, #20998, #2494, #5355, #30473, #30687, #27371, #24285, #5556, #6782, #37444, #25321, #22029, #9242, #12336, #34401, #12540, #3516, #34196, #18930, #12741, #28604, #34810 ),
 ( #25112, #9865, #24910, #9658, #6586, #30890, #3320, #2702, #16038, #6172, #19132, #31699, #412, #2901, #12953, #31295, #37852, #40327, #27980, #25516, #15420, #34603, #38062, #28396, #28183 ),
 ( #22437, #15220, #18713, #35007, #5962, #40528, #18507, #27774, #31496, #12120, #24697, #3118, #37248, #9039, #15634, #21617, #31091, #13347, #11204, #25921, #27078, #31906, #10258, #39623, #22839 ),
 ( #19739, #13554, #8731, #17792, #34305, #40037, #5873, #15326, #21722, #28091, #2182, #24596, #11609, #27487, #18411, #31194, #30999, #20895, #11810, #27881, #24188, #18001, #36744, #2802, #27679 ),
 ( #36952, #30587, #30796, #40642, #37150, #40426, #40235, #14700, #27269, #8529, #39840, #2394, #21315, #3014, #15534, #6074, #21523, #33680, #33887, #30378, #18607, #24393, #12237, #24811, #12445 ),
 ( #21112, #5460, #5667, #8939, #25012, #14919, #8321, #2604, #33481, #18204, #37352, #15123, #12019, #5252, #34098, #9146, #37750, #37551, #34501, #19239, #3225, #13255, #19647, #32218, #34712 ),
 ( #3823, #9346, #21927, #9766, #31805, #313, #10157, #15741, #28501, #34916, #22547, #12850, #3620, #31396, #19040, #38360, #6275, #28710, #25824, #18824, #28293, #6691, #13456, #3425, #32016 ),
 ( #31602, #15936, #16147, #22746, #114, #25617, #6887, #35313, #717, #25419, #16538, #522, #29115, #37959, #16340, #7081, #12646, #9966, #25220, #4020, #22346, #921, #9555, #28911, #22139 ),
 ( #13055, #38160, #35109, #6488, #19441, #23729, #1329, #1521, #4210, #26629, #39368, #26237, #1935, #20235, #10370, #10756, #20433, #35905, #1133, #11158, #23336, #38769, #10565, #26028, #22946 ),
 ( #36295, #13866, #26434, #17138, #8072, #38961, #33014, #38560, #35508, #32818, #4607, #29518, #20631, #32415, #16940, #29711, #10959, #14054, #39163, #19844, #7482, #26827, #7280, #23542, #1725 ),
 ( #4801, #36107, #14256, #7883, #16730, #23139, #33218, #17332, #13665, #32620, #5003, #29910, #17529, #30123, #35706, #29316, #20039, #4416, #8477, #27223, #8888, #31144, #27828, #33834, #11760 ),
 ( #2133, #15277, #5408, #17947, #40380, #21676, #36903, #21262, #30530, #14456, #18360, #12185, #2339, #30746, #33435, #24544, #37303, #37101, #27027, #14861, #34047, #17736, #24132, #14651, #21470 ),
 ( #27430, #39989, #36696, #8680, #34252, #2547, #5821, #5615, #20841, #5205, #39788, #30325, #21060, #24339, #9099, #6025, #24755, #27630, #11558, #18155, #23924, #18559, #15073, #11968, #30948 ),
 ( #33632, #40187, #2753, #39572, #11356, #36498, #8269, #21874, #25371, #6641, #38115, #28662, #22087, #19393, #3375, #6836, #15689, #3567, #468, #3768, #9715, #2962, #9918, #37696, #13008 ),
 ( #31347, #22499, #34661, #19188, #12397, #28240, #25571, #65, #15891, #31754, #22294, #31552, #258, #12596, #25161, #28451, #12798, #35062, #31966, #15478, #37909, #37501, #16096, #6434, #18991 ),
 ( #34451, #9504, #24965, #28040, #6228, #40588, #34865, #9296, #18773, #3175, #12317, #21803, #2883, #11490, #24893, #11688, #40312, #21395, #33970, #12101, #21601, #18485, #5947, #5336, #39914 ),
 ( #18080, #31075, #39703, #33759, #37228, #24266, #2261, #15404, #3098, #24053, #6156, #36622, #34182, #8610, #15614, #27964, #24679, #36828, #37429, #15000, #27560, #30876, #34381, #40117, #40507 ),
 ( #5743, #33560, #27355, #9022, #9224, #18696, #8408, #31278, #20981, #17870, #30454, #27758, #14786, #21188, #5539, #18285, #30668, #2477, #11895, #2682, #24468, #8809, #37025, #15205, #13328 ),
 ( #16022, #797, #22421, #37837, #28797, #3910, #19317, #22222, #189, #22625, #4096, #25904, #6766, #25498, #13142, #6363, #15825, #28995, #19115, #31682, #38441, #35394, #9847, #34991, #3499 ),
 ( #12726, #31891, #10044, #25700, #38046, #3702, #9640, #34792, #16223, #38243, #16423, #10245, #28167, #12936, #9424, #35193, #28589, #398, #6569, #6965, #7165, #19524, #32105, #22824, #34588 ),
 ( #19726, #32298, #31480, #24854, #12522, #25096, #37625, #18912, #25302, #3304, #28379, #10839, #17214, #39242, #36176, #23610, #23023, #16816, #19918, #20114, #29785, #29990, #29395, #33302, #23415 ),
 ( #20717, #29193, #23799, #16609, #11032, #26311, #1005, #33088, #1600, #1213, #1805, #32693, #4493, #7760, #39444, #17013, #7956, #13540, #26113, #29590, #39038, #1405, #14330, #35589, #7559 ),
 ( #38644, #10442, #7360, #4680, #26901, #13748, #20504, #35979, #38846, #11234, #4873, #20308, #17408, #26508, #32489, #10640, #36374, #26708, #4289, #23217, #8145, #32893, #35781, #14131, #13938 ),
 ( #21408, #12330, #11499, #21610, #31084, #12111, #20778, #34191, #20992, #8822, #30679, #2489, #33981, #30884, #27768, #15214, #14589, #8417, #24064, #11701, #5756, #5956, #33569, #24903, #15010 ),
 ( #40321, #8204, #33372, #15413, #5142, #2696, #17884, #17676, #24691, #18295, #5348, #18501, #24279, #36839, #40126, #2895, #8619, #37240, #30258, #2077, #21199, #27573, #33773, #27972, #27161 ),
 ( #9033, #39716, #36636, #30466, #37036, #40520, #2273, #14795, #11906, #27365, #39927, #5550, #24481, #18089, #6580, #34395, #22024, #22636, #6777, #25106, #3314, #6975, #25315, #10054, #31693 ),
 ( #37846, #16431, #3508, #29005, #18922, #16236, #13151, #13342, #9857, #37437, #35203, #28389, #25711, #609, #28807, #9439, #19534, #9650, #19330, #6166, #34598, #38257, #6373, #19126, #31901 ),
 ( #3711, #32116, #3919, #9235, #198, #808, #2, #31490, #37635, #21813, #16032, #18707, #31288, #15834, #3106, #15628, #12736, #12946, #28177, #12533, #22235, #34801, #28599, #409, #25511 ),
 ( #38057, #22433, #35003, #17416, #39252, #38655, #20515, #32309, #7369, #22832, #20320, #19735, #17224, #19926, #39050, #30001, #29205, #11046, #7965, #29797, #38450, #23621, #10452, #26517, #7571 ),
 ( #23424, #32902, #36185, #4885, #4106, #1415, #1017, #4304, #4691, #25916, #32502, #35990, #26123, #13549, #1610, #1817, #10253, #33100, #35403, #14145, #35599, #7176, #26718, #10849, #23034 ),
 ( #16620, #16826, #29408, #29600, #7772, #1224, #13758, #32706, #26322, #38859, #10650, #23229, #35795, #20126, #4503, #17025, #13951, #11243, #2440, #27721, #14538, #8771, #8572, #36588, #37192 ),
 ( #30836, #24226, #23807, #39662, #40276, #24433, #2022, #20937, #24641, #2221, #12060, #21150, #24011, #14960, #2646, #5496, #8363, #27112, #21357, #31040, #8982, #33717, #11649, #40079, #33312 ),
 ( #18246, #5706, #11445, #21567, #14742, #36989, #36383, #33523, #15163, #5292, #8155, #20727, #27527, #34146, #17831, #33932, #18039, #30414, #5914, #18454, #30632, #14339, #36787, #5091, #27313 ),
 ( #39874, #11857, #26911, #17625, #39455, #30203, #565, #6731, #31444, #22587, #37797, #35154, #25059, #22389, #19281, #19489, #15982, #2847, #16189, #34550, #31848, #3662, #34954, #15580, #13103 ),
 ( #9603, #6324, #15367, #28755, #25662, #18871, #19080, #21766, #12897, #38204, #25462, #27924, #3266, #10004, #6119, #12492, #31242, #38007, #22185, #6926, #40470, #28134, #12279, #9191, #37593 ),
 ( #37397, #24853, #9390, #28549, #34349, #18653, #3063, #40687, #21975, #15791, #28342, #156, #3464, #25265, #34757, #359, #9809, #12689, #6533, #31648, #32264, #35355, #35554, #32661, #4648 ),
 ( #29554, #4062, #7127, #23377, #36145, #3868, #39209, #32063, #26473, #966, #7925, #7727, #4459, #16577, #17181, #7322, #19881, #23178, #14094, #32453, #39001, #16384, #28958, #4253, #13711 ),
 ( #29750, #16982, #761, #1374, #13292, #35748, #26673, #16779, #10799, #25865, #38405, #29358, #26278, #1178, #1564, #10205, #22988, #38811, #13905, #10604, #7522, #22788, #13503, #32859, #19688 ),
 ( #26075, #10997, #35945, #20083, #20274, #23581, #29157, #38608, #10412, #30584, #8111, #27076, #30793, #8319, #33885, #14698, #30161, #21110, #36950, #11607, #14501, #33265, #14917, #37149, #5665 ),
 ( #20474, #18202, #11402, #8729, #24390, #11807, #5048, #2602, #20893, #2392, #29955, #17577, #21313, #1981, #2180, #27484, #33677, #17789, #39838, #39620, #23968, #27267, #30376, #15121, #27677 ),
 ( #40035, #24186, #12017, #40233, #36543, #24594, #26867, #33479, #17374, #33056, #14298, #4843, #5250, #5458, #1768, #23768, #39411, #11202, #36343, #20680, #36742, #8527, #17998, #31393, #3221 ),
 ( #28498, #15933, #15324, #9144, #12235, #12442, #9552, #22343, #21720, #25614, #15738, #34095, #34498, #3422, #18820, #24809, #34913, #6272, #34303, #6072, #8937, #5871, #28290, #27878, #25415 ),
 ( #18605, #3616, #40424, #31192, #18409, #310, #2800, #12847, #3012, #22133, #13051, #37350, #6687, #31802, #37956, #21521, #19235, #15531, #34708, #110, #12643, #6484, #31599, #9763, #16144 ),
 ( #25216, #28088, #40639, #28706, #30997, #25008, #19037, #37548, #9343, #519, #21924, #37747, #4604, #38157, #32617, #7078, #14051, #13863, #38766, #10154, #10754, #13452, #26025, #29313, #20232 ),
 ( #29515, #16535, #4207, #32012, #25821, #10561, #23333, #23136, #1518, #35703, #19437, #35106, #6884, #26232, #35902, #38358, #4412, #32412, #19644, #32816, #16937, #16727, #26431, #7277, #3820 ),
 ( #32215, #29112, #19841, #7682, #714, #7478, #20035, #17132, #1324, #38556, #29707, #1129, #9963, #4017, #38958, #22544, #16335, #28908, #13252, #22743, #918, #35308, #10366, #22943, #35505 ),
 ( #13662, #33432, #30120, #26626, #30527, #24336, #1930, #2130, #4797, #36693, #8677, #8474, #39160, #17524, #5405, #29907, #36292, #14252, #21057, #5202, #18151, #39986, #33009, #14453, #23919 ),
 ( #23539, #36104, #14648, #11757, #26824, #33629, #20837, #8067, #21259, #17944, #17733, #2336, #36495, #7880, #11155, #36899, #14856, #39365, #33215, #33831, #27023, #5612, #30321, #20628, #27220 ),
 ( #39782, #30740, #4999, #27425, #2544, #10955, #11555, #20430, #17329, #39569, #1721, #23725, #11353, #8266, #24128, #15474, #25157, #24540, #12181, #31548, #40376, #37495, #37692, #28235, #12392 ),
 ( #9498, #27626, #6020, #34657, #18356, #24750, #2749, #22083, #34446, #6637, #28446, #27823, #9711, #21466, #37299, #11964, #6429, #8884, #18986, #9096, #61, #19184, #30944, #254, #37905 ),
 ( #12794, #21670, #15684, #9292, #21870, #12590, #3371, #15887, #25366, #34042, #15272, #34248, #18555, #22290, #34861, #31139, #31750, #6224, #40183, #40581, #15070, #24961, #2958, #37097, #18769 ),
 ( #5815, #28036, #31343, #3170, #19983, #26918, #39461, #667, #7230, #13608, #35655, #22693, #10310, #38111, #31962, #4160, #38509, #28658, #29062, #38714, #13401, #19389, #16883, #869, #3764 ),
 ( #32566, #16677, #16290, #30008, #19596, #32170, #35458, #11249, #3969, #10510, #3562, #16092, #16488, #25976, #7028, #1827, #9914, #35259, #22889, #29263, #19791, #32364, #22495, #25772, #4363 ),
 ( #1076, #38309, #23814, #23090, #26180, #14348, #7425, #464, #28860, #36390, #8163, #13204, #10106, #20733, #13003, #25567, #35058, #6832, #27532, #30842, #30638, #30421, #20945, #21363, #5920 ),
 ( #40084, #33318, #40281, #39882, #2651, #15169, #27727, #33529, #24647, #24232, #8777, #2029, #17837, #12070, #5302, #5503, #33937, #24438, #33724, #2446, #2229, #14750, #18046, #14970, #37198 ),
 ( #8372, #5711, #11862, #5100, #8987, #27320, #21573, #11453, #11658, #14545, #18253, #39668, #34151, #36794, #36998, #17631, #8579, #30213, #27120, #24020, #21157, #36594, #1360, #29938, #10987 ),
 ( #26855, #36328, #1968, #8303, #22620, #4830, #32647, #7713, #8098, #28791, #23365, #39397, #35933, #11185, #29544, #4445, #20665, #33468, #597, #36529, #13138, #23758, #38988, #5236, #5034 ),
 ( #14486, #4636, #17166, #20461, #11387, #29735, #33250, #25696, #38239, #1550, #23567, #32847, #27059, #35735, #20261, #26660, #14286, #14081, #36131, #7508, #10787, #30150, #10040, #33040, #17564 ),
 ( #39605, #7912, #23952, #39194, #20071, #13895, #20879, #16971, #26459, #17361, #1755, #5650, #31178, #12001, #27465, #18394, #34288, #8920, #11791, #30567, #12220, #34482, #2999, #37132, #15104 ),
 ( #8715, #6057, #21707, #9133, #2377, #28072, #18187, #27864, #27254, #14896, #18592, #40020, #40219, #40414, #30980, #27663, #21504, #24373, #36933, #24581, #34083, #15517, #40625, #17773, #2583 ),
 ( #9328, #12430, #21294, #24998, #24172, #33868, #14686, #24793, #11591, #37533, #30779, #2786, #21907, #21092, #30360, #2165, #39823, #36728, #8512, #5857, #15312, #37338, #33663, #5440, #17980 ),
 ( #12627, #6471, #9537, #9748, #6869, #19626, #31378, #31785, #701, #16127, #22120, #32201, #3600, #19021, #31583, #6260, #3204, #28691, #25197, #22726, #29095, #897, #3408, #9945, #16319 ),
 ( #18805, #19221, #501, #22327, #4001, #37728, #37940, #13037, #31995, #34896, #25598, #95, #28483, #7059, #15723, #38143, #35291, #28276, #34693, #22527, #22920, #12830, #13237, #35093, #25402 ),
 ( #15920, #6670, #16519, #19423, #13433, #3799, #289, #28894, #26011, #25802, #38339, #10137, #38541, #10348, #8050, #14033, #32798, #20413, #13643, #23118, #36276, #26413, #38942, #20609, #1913 ),
 ( #10737, #35488, #39346, #33194, #23316, #10940, #26215, #4777, #17510, #17311, #7259, #35886, #14236, #38747, #4396, #35688, #29888, #26607, #27005, #4982, #7461, #30104, #1112, #16918, #32398 ),
 ( #10541, #20016, #32599, #29498, #1307, #7664, #14434, #39551, #11335, #7864, #13844, #20215, #4191, #19823, #4588, #32992, #1705, #16708, #29298, #17116, #23519, #29688, #1500, #26808, #39144 ),
 ( #36086, #11138, #23709, #18131, #33612, #24524, #40362, #15051, #17926, #36672, #18335, #40565, #37284, #2527, #21237, #8864, #2113, #11538, #24733, #14838, #27406, #9077, #31125, #5591, #30722 ),
 ( #12159, #8455, #27610, #5797, #37074, #40168, #11948, #5386, #30509, #21450, #34026, #21653, #6004, #23901, #8660, #5185, #30925, #24316, #11738, #2315, #2732, #2941, #15256, #27808, #18540 ),
 ( #39968, #15457, #28016, #27204, #36473, #8248, #20818, #33414, #30299, #21039, #14630, #39760, #24108, #12989, #35042, #31943, #19374, #18751, #12574, #15667, #15872, #25554, #25756, #25143, #29047 ),
 ( #28215, #3751, #16475, #24946, #19581, #12377, #6820, #22066, #37479, #28847, #38095, #37674, #38295, #28430, #237, #3548, #35243, #12777, #16274, #9277, #21853, #25348, #34842, #37889, #10096 ),
 ( #34429, #9897, #6208, #31329, #3151, #447, #22680, #9477, #654, #6619, #34640, #7015, #13190, #31734, #32157, #22275, #45, #6413, #3955, #22475, #18964, #31529, #3355, #9698, #19168 ),
 ( #16077, #28640, #35840, #10493, #1455, #17266, #32752, #35642, #13593, #36037, #17460, #14190, #20169, #38899, #26560, #19777, #29250, #1655, #32547, #4347, #26762, #8005, #23273, #7614, #16869 ) ),
 .UNSPECIFIED., .F., .F., .F.,
 ( 4, 3, 3, 3, 3, 3, 3, 3, 3, 3, 3, 3, 3, 3, 3, 3, 3, 3, 3, 3, 3, 3, 3, 3, 3, 3, 3, 4 ),
 ( 4, 3, 3, 3, 3, 3, 3, 3, 4 ),
 ( -2.249698332083740343E-17, 9.220626685372613810E-07, 1.844125337097019745E-06, 3.688250674216536686E-06, 5.532376011336053626E-06, 7.376501348455570566E-06, 1.106475202269460445E-05, 1.475300269693363833E-05, 2.212950404541170609E-05, 2.950600539388977385E-05, 4.425900809084590937E-05, 5.901201078780204490E-05, 8.851801618171431594E-05, 0.0001180240215756265870, 0.0001770360323634511291, 0.0002360480431512756712, 0.0003540720647269247554, 0.0004720960863025738395, 0.0009441921726051701221, 0.001888384345210362796, 0.003776768690420748142, 0.005665153035631133489, 0.007553537380841518836, 0.01133030607126228953, 0.01321869041647267401, 0.01416288258907786798, 0.01463497867538046324, 0.01510707476168306022 ),
 ( 0.000000000000000000, 0.1250000000000000000, 0.2500000000000000000, 0.3750000000000000000, 0.5000000000000000000, 0.6250000000000000000, 0.7500000000000000000, 0.8750000000000000000, 1.000000000000000000 ),
 .UNSPECIFIED. ) ;
#18820=CARTESIAN_POINT ( 'NONE',  ( 79.38338525671692025, 64.07937768075929341, -3.690346394509879335 ) ) ;
#18823=AXIS2_PLACEMENT_3D ( 'NONE', #2178, #37951, #28286 ) ;
#18824=CARTESIAN_POINT ( 'NONE',  ( 79.78729094670478617, 65.99503481514534542, -2.368810654844697439 ) ) ;
#18825=CARTESIAN_POINT ( 'NONE',  ( 80.48656635915796187, 62.05344631111049836, 3.128253119413327177 ) ) ;
#18831=ORIENTED_EDGE ( 'NONE', *, *, #21627, .F. ) ;
#18855=CARTESIAN_POINT ( 'NONE',  ( 67.14845837397145090, 58.06767444754134289, 3.999036733496184048 ) ) ;
#18871=CARTESIAN_POINT ( 'NONE',  ( 80.80742440666386983, 61.88848183320471463, -2.854164747638210820 ) ) ;
#18874=CARTESIAN_POINT ( 'NONE',  ( 81.00146336277434500, 61.29413404061270398, 1.724274471760811167 ) ) ;
#18878=DIRECTION ( 'NONE',  ( -1.000000000000000000, -5.325537380878540815E-15, 0.000000000000000000 ) ) ;
#18880=TOROIDAL_SURFACE ( 'NONE', #16891, 5.681288188914805026, 1.000000000000000000 ) ;
#18895=DIRECTION ( 'NONE',  ( -1.000000000000000000, 0.000000000000000000, 0.000000000000000000 ) ) ;
#18896=CARTESIAN_POINT ( 'NONE',  ( 81.15394892944381411, 63.54712375394903745, 3.396356880840902370 ) ) ;
#18912=CARTESIAN_POINT ( 'NONE',  ( 81.08176929032271119, 62.48897713179231772, -3.134554000843273514 ) ) ;
#18917=EDGE_LOOP ( 'NONE', ( #5290, #2830, #23070, #21938, #39343, #37597 ) ) ;
#18922=CARTESIAN_POINT ( 'NONE',  ( 81.09335400879909628, 61.74513338965305564, -2.494286432550476995 ) ) ;
#18925=EDGE_CURVE ( 'NONE', #16760, #9551, #13700, .T. ) ;
#18930=CARTESIAN_POINT ( 'NONE',  ( 79.49585004866908378, 66.23094581382571278, -1.662695954554820554 ) ) ;
#18937=CARTESIAN_POINT ( 'NONE',  ( 74.80267162900737787, 60.00335986791986898, 3.708893976703238948 ) ) ;
#18943=CARTESIAN_POINT ( 'NONE',  ( -57.44564769468265553, 32.97701904356408420, -4.025706866804887873 ) ) ;
#18946=CARTESIAN_POINT ( 'NONE',  ( 81.90837201943169532, 62.87926165960877256, 2.626729253126739216 ) ) ;
#18948=EDGE_LOOP ( 'NONE', ( #31742, #13257, #17727, #16986 ) ) ;
#18964=CARTESIAN_POINT ( 'NONE',  ( 66.41505992881675979, 57.81052748253004125, -4.000000000000023093 ) ) ;
#18981=CARTESIAN_POINT ( 'NONE',  ( 80.34788146105260864, 66.29920961842009319, -1.394285451510165252 ) ) ;
#18982=AXIS2_PLACEMENT_3D ( 'NONE', #32034, #9575, #22156 ) ;
#18983=CARTESIAN_POINT ( 'NONE',  ( 79.02959213847955766, 65.76024385718582721, 2.482170738714648550 ) ) ;
#18985=ORIENTED_EDGE ( 'NONE', *, *, #5785, .F. ) ;
#18986=CARTESIAN_POINT ( 'NONE',  ( 76.63893934653984275, 63.44172143924971152, -3.539370024148525307 ) ) ;
#18991=CARTESIAN_POINT ( 'NONE',  ( 78.67710717883703353, 66.04916176178686271, -1.122020883098632904 ) ) ;
#18992=CARTESIAN_POINT ( 'NONE',  ( 78.66234234182425666, 62.19549841187289019, 3.710351296122935683 ) ) ;
#18997=CARTESIAN_POINT ( 'NONE',  ( 81.57551674523639917, 65.32158946912302611, 2.325514254128254965 ) ) ;
#19006=DIRECTION ( 'NONE',  ( -1.000000000000000000, 0.000000000000000000, 0.000000000000000000 ) ) ;
#19015=CARTESIAN_POINT ( 'NONE',  ( -64.08758708074093136, 36.76354445449491948, -3.435823087746522120 ) ) ;
#19021=CARTESIAN_POINT ( 'NONE',  ( 68.59886892412534110, 58.63590986220410173, -3.993768376023888234 ) ) ;
#19037=CARTESIAN_POINT ( 'NONE',  ( 80.05518365985739138, 61.93129665380739368, -3.228498513792977587 ) ) ;
#19040=CARTESIAN_POINT ( 'NONE',  ( 80.93493477626104493, 64.98323193449208190, -3.125232205748941006 ) ) ;
#19041=CARTESIAN_POINT ( 'NONE',  ( 79.60839748543872929, 63.85977214187242623, 3.734652355492746434 ) ) ;
#19043=CARTESIAN_POINT ( 'NONE',  ( 81.04763707098177861, 66.10603528134694784, 1.000000000000000000 ) ) ;
#19062=DIRECTION ( 'NONE',  ( -1.000000000000000000, 0.000000000000000000, 0.000000000000000000 ) ) ;
#19064=ORIENTED_EDGE ( 'NONE', *, *, #35951, .T. ) ;
#19065=CARTESIAN_POINT ( 'NONE',  ( 67.47105843325410035, 58.09313517554802075, 3.997566301760142160 ) ) ;
#19080=CARTESIAN_POINT ( 'NONE',  ( 80.71678001510446165, 62.11300466482757088, -3.061371641637534502 ) ) ;
#19082=CARTESIAN_POINT ( 'NONE',  ( 80.98641699598172750, 61.40056178693504307, 2.031354376635673198 ) ) ;
#19088=CARTESIAN_POINT ( 'NONE',  ( -54.89797088024758409, 31.42847739604817647, 1.178388813972039983 ) ) ;
#19091=CARTESIAN_POINT ( 'NONE',  ( -64.66796849410253856, 36.23110552202045653, -6.165526157072432234 ) ) ;
#19092=VECTOR ( 'NONE', #28784, 1000.000000000000000 ) ;
#19094=CARTESIAN_POINT ( 'NONE',  ( -68.71186372058383540, 37.81212149306785619, 9.800414904976364028 ) ) ;
#19097=CARTESIAN_POINT ( 'NONE',  ( -75.45330471031414277, 33.71485196875532608, -46.17089178453873188 ) ) ;
#19098=CARTESIAN_POINT ( 'NONE',  ( 79.83674225097152544, 65.44563770485291343, 3.036434590848153370 ) ) ;
#19115=CARTESIAN_POINT ( 'NONE',  ( 79.50768156050780533, 65.53910429656815495, -2.885071930847946664 ) ) ;
#19126=CARTESIAN_POINT ( 'NONE',  ( 78.69119446862563905, 66.01295734309310603, -1.592560325354585915 ) ) ;
#19127=CARTESIAN_POINT ( 'NONE',  ( -81.07947155388369254, 30.81399289130168029, -12.49999999999999645 ) ) ;
#19132=CARTESIAN_POINT ( 'NONE',  ( 81.95280109346356312, 63.95510859576435081, -2.731810022748015321 ) ) ;
#19135=CARTESIAN_POINT ( 'NONE',  ( -58.05766836353178917, 29.90785475872966259, -4.511249903221973945 ) ) ;
#19137=DIRECTION ( 'NONE',  ( -0.000000000000000000, -0.000000000000000000, -1.000000000000000000 ) ) ;
#19139=CARTESIAN_POINT ( 'NONE',  ( 69.55412262724962602, 59.60600320152340004, 3.916752429509892774 ) ) ;
#19142=ORIENTED_EDGE ( 'NONE', *, *, #26785, .F. ) ;
#19146=CARTESIAN_POINT ( 'NONE',  ( -54.79610818216033152, 31.51396769785350926, -1.000000000000000000 ) ) ;
#19147=CARTESIAN_POINT ( 'NONE',  ( 81.58578928044241252, 61.77466459011640865, 1.878604182848663262 ) ) ;
#19152=VERTEX_POINT ( 'NONE', #38791 ) ;
#19161=ADVANCED_FACE ( 'NONE', ( #28935 ), #13689, .T. ) ;
#19168=CARTESIAN_POINT ( 'NONE',  ( 66.41110252083150556, 57.82170748331512300, -4.000000000000026645 ) ) ;
#19170=CARTESIAN_POINT ( 'NONE',  ( -55.16208421294562925, 31.22611435454062345, 1.446432346866579621 ) ) ;
#19180=CARTESIAN_POINT ( 'NONE',  ( 82.23130663822949771, 64.88126268290422161, -1.480606629406893804 ) ) ;
#19181=CARTESIAN_POINT ( 'NONE',  ( 79.55117250774245008, 64.91534908514034896, 3.386558198656119512 ) ) ;
#19184=CARTESIAN_POINT ( 'NONE',  ( 76.39468346684414257, 63.92226846272791363, -3.160174624570336821 ) ) ;
#19188=CARTESIAN_POINT ( 'NONE',  ( 81.36407395805152021, 61.67455102447421211, -2.043563575549276479 ) ) ;
#19189=CARTESIAN_POINT ( 'NONE',  ( 77.19967638839703739, 62.30393748795762576, 3.856837490695280923 ) ) ;
#19196=CARTESIAN_POINT ( 'NONE',  ( -58.88327606466311437, 29.11203654247168870, 6.075279880813873490 ) ) ;
#19197=CARTESIAN_POINT ( 'NONE',  ( 79.25820086742470494, 66.26332994521376918, 1.378120381825653551 ) ) ;
#19201=CARTESIAN_POINT ( 'NONE',  ( -64.29080678322934261, 36.57451004496311953, 5.531098403533500907 ) ) ;
#19206=EDGE_CURVE ( 'NONE', #32421, #10601, #8874, .T. ) ;
#19221=CARTESIAN_POINT ( 'NONE',  ( 68.16305384742138074, 58.02271910793402299, -3.969942683317755350 ) ) ;
#19231=CARTESIAN_POINT ( 'NONE',  ( 80.87203728266233327, 63.05930952086730201, 3.432259906339284683 ) ) ;
#19235=CARTESIAN_POINT ( 'NONE',  ( 78.95999731999182814, 64.46943033386044419, -3.516968106976288588 ) ) ;
#19239=CARTESIAN_POINT ( 'NONE',  ( 79.85781052176623973, 66.03394566247139608, -2.299173245602593507 ) ) ;
#19240=CARTESIAN_POINT ( 'NONE',  ( 80.15282788578683437, 62.77883523856217352, 3.578491385641962452 ) ) ;
#19241=ADVANCED_FACE ( 'NONE', ( #5432 ), #2158, .T. ) ;
#19242=CARTESIAN_POINT ( 'NONE',  ( 82.45631153319118312, 62.87735296625318426, 1.000000000000000000 ) ) ;
#19243=CARTESIAN_POINT ( 'NONE',  ( -64.08758708074093136, 43.90699456340107787, 1.959021792961942898 ) ) ;
#19269=CARTESIAN_POINT ( 'NONE',  ( 66.72933079118084265, 57.85140187965895819, 3.999416444359401357 ) ) ;
#19273=ORIENTED_EDGE ( 'NONE', *, *, #18786, .T. ) ;
#19281=CARTESIAN_POINT ( 'NONE',  ( 79.70130230958179141, 64.28379252955068068, -3.649417990092605368 ) ) ;
#19283=CARTESIAN_POINT ( 'NONE',  ( 81.00792578075066785, 61.24501526813143215, 1.386845825021845835 ) ) ;
#19293=CARTESIAN_POINT ( 'NONE',  ( -63.71117060422339051, 35.77969396829408311, -7.174848616057552420 ) ) ;
#19301=CARTESIAN_POINT ( 'NONE',  ( 79.06971639787835215, 65.98240043192649296, 2.069468987430128415 ) ) ;
#19303=CARTESIAN_POINT ( 'NONE',  ( -81.07947155388369254, 30.81399289130168384, -46.17089178453873188 ) ) ;
#19313=CARTESIAN_POINT ( 'NONE',  ( 68.63113683135277654, 58.55076364936792288, 3.993768376023898448 ) ) ;
#19317=CARTESIAN_POINT ( 'NONE',  ( 81.21077662890941440, 62.27078576854650294, -2.885071930847909805 ) ) ;
#19318=DIRECTION ( 'NONE',  ( -1.000000000000000000, 0.000000000000000000, 0.000000000000000000 ) ) ;
#19324=ORIENTED_EDGE ( 'NONE', *, *, #910, .F. ) ;
#19330=CARTESIAN_POINT ( 'NONE',  ( 79.29422675899260753, 65.38839789421687954, -2.978180346930986211 ) ) ;
#19336=DIRECTION ( 'NONE',  ( 0.000000000000000000, 0.000000000000000000, 1.000000000000000000 ) ) ;
#19341=CARTESIAN_POINT ( 'NONE',  ( -64.08758708074093136, 41.42070492151870553, -3.928592456684763423 ) ) ;
#19342=CARTESIAN_POINT ( 'NONE',  ( 71.23183612236115891, 58.76351790733232860, 3.862811858476256965 ) ) ;
#19350=CARTESIAN_POINT ( 'NONE',  ( -64.01189449551647215, 34.81586596186931359, -7.000000000000003553 ) ) ;
#19351=CARTESIAN_POINT ( 'NONE',  ( 81.65270467917663666, 63.44102909743362773, 3.019969592843123607 ) ) ;
#19368=FACE_OUTER_BOUND ( 'NONE', #1974, .T. ) ;
#19371=ORIENTED_EDGE ( 'NONE', *, *, #35205, .T. ) ;
#19374=CARTESIAN_POINT ( 'NONE',  ( 66.70283438698932343, 57.92520761901871396, -3.999543855873471276 ) ) ;
#19385=CARTESIAN_POINT ( 'NONE',  ( 82.04611962119285806, 65.17642557464525055, -1.633153239555407144 ) ) ;
#19389=CARTESIAN_POINT ( 'NONE',  ( 75.36936014427639918, 63.22485534106652949, -3.346357594022706827 ) ) ;
#19393=CARTESIAN_POINT ( 'NONE',  ( 80.63945418285945266, 64.43655742540512676, -3.486376426170564979 ) ) ;
#19394=CARTESIAN_POINT ( 'NONE',  ( 77.74497067125921035, 61.15868661831857622, 3.539370024157653116 ) ) ;
#19400=CARTESIAN_POINT ( 'NONE',  ( 80.36115181822172815, 66.02274906846037084, 2.190303691588294743 ) ) ;
#19408=CARTESIAN_POINT ( 'NONE',  ( 77.27679392923256785, 60.01025453254077036, 2.873255474974654167 ) ) ;
#19410=EDGE_CURVE ( 'NONE', #11154, #23165, #18386, .T. ) ;
#19416=VECTOR ( 'NONE', #36023, 1000.000000000000000 ) ;
#19423=CARTESIAN_POINT ( 'NONE',  ( 67.82906190410768943, 58.02404379074640417, -3.985511447369935123 ) ) ;
#19434=CARTESIAN_POINT ( 'NONE',  ( 81.24801795318221309, 61.46771992710468169, 1.817988788077155249 ) ) ;
#19437=CARTESIAN_POINT ( 'NONE',  ( 79.45360044721715553, 62.79974527947164376, -3.729426069516725839 ) ) ;
#19441=CARTESIAN_POINT ( 'NONE',  ( 81.60486409339017655, 61.94451848016240092, -2.198649373785569239 ) ) ;
#19442=CARTESIAN_POINT ( 'NONE',  ( 79.21623058866053668, 63.63573840405092596, 3.765547211956732809 ) ) ;
#19443=EDGE_CURVE ( 'NONE', #20708, #12131, #10841, .T. ) ;
#19447=CARTESIAN_POINT ( 'NONE',  ( 82.10909544300281482, 65.20937546977818045, 1.165579324820864571 ) ) ;
#19448=CARTESIAN_POINT ( 'NONE',  ( -64.08758708074093136, 43.61223004741322740, 1.000000000000000000 ) ) ;
#19472=CARTESIAN_POINT ( 'NONE',  ( 66.55613647995218685, 57.87265654107390844, 3.999745625243888547 ) ) ;
#19484=DIRECTION ( 'NONE',  ( -0.000000000000000000, -0.000000000000000000, -1.000000000000000000 ) ) ;
#19489=CARTESIAN_POINT ( 'NONE',  ( 79.55161461803720613, 64.54397228415257359, -3.537885823842634725 ) ) ;
#19491=CARTESIAN_POINT ( 'NONE',  ( 80.97051285240280549, 61.23143294393114644, 1.429680343938458664 ) ) ;
#19509=CARTESIAN_POINT ( 'NONE',  ( 80.17140661427384885, 64.93185644258201705, 3.352621494407050484 ) ) ;
#19518=CARTESIAN_POINT ( 'NONE',  ( 68.74365607523500898, 58.25355655637604713, 3.970924506823473532 ) ) ;
#19524=CARTESIAN_POINT ( 'NONE',  ( 79.00945943828583040, 65.94065490460722856, -2.112861953993757425 ) ) ;
#19534=CARTESIAN_POINT ( 'NONE',  ( 79.60112097352363492, 64.95058993122677293, -3.372125408468116703 ) ) ;
#19535=VECTOR ( 'NONE', #36536, 1000.000000000000000 ) ;
#19540=ORIENTED_EDGE ( 'NONE', *, *, #404, .T. ) ;
#19550=DIRECTION ( 'NONE',  ( 0.000000000000000000, 0.000000000000000000, 1.000000000000000000 ) ) ;
#19551=CARTESIAN_POINT ( 'NONE',  ( -63.70768058868310391, 44.39675795731058372, -0.9999999999999904521 ) ) ;
#19552=CARTESIAN_POINT ( 'NONE',  ( 71.91282362819097784, 60.38839763785598080, 3.929231508849752252 ) ) ;
#19561=CARTESIAN_POINT ( 'NONE',  ( 81.74528107327201099, 62.23958694028463867, 2.368810654844612174 ) ) ;
#19572=CARTESIAN_POINT ( 'NONE',  ( -73.07498068578524908, 39.58105274722134226, -12.49999999999999645 ) ) ;
#19581=CARTESIAN_POINT ( 'NONE',  ( 66.58353442343859285, 57.79581178809598896, -3.999616584010542208 ) ) ;
#19586=AXIS2_PLACEMENT_3D ( 'NONE', #13301, #23385, #10809 ) ;
#19591=CARTESIAN_POINT ( 'NONE',  ( 82.04814969336703712, 64.78574761690806838, -2.164558651854042282 ) ) ;
#19596=CARTESIAN_POINT ( 'NONE',  ( 76.07689452438883393, 60.24265224227303150, -3.527522301306114105 ) ) ;
#19601=CARTESIAN_POINT ( 'NONE',  ( 75.88202180556031351, 63.57356190189720735, 3.253266109296548247 ) ) ;
#19606=CARTESIAN_POINT ( 'NONE',  ( 82.15073535245181802, 63.33429545135121685, 2.460680857248572551 ) ) ;
#19618=CIRCLE ( 'NONE', #19586, 1.000000000000003109 ) ;
#19626=CARTESIAN_POINT ( 'NONE',  ( 68.72765198451649837, 58.29585788764496357, -3.976359261632543163 ) ) ;
#19638=FACE_OUTER_BOUND ( 'NONE', #31479, .T. ) ;
#19639=CARTESIAN_POINT ( 'NONE',  ( 81.21077662890941440, 62.27078576854649583, 2.885071930847908028 ) ) ;
#19642=EDGE_CURVE ( 'NONE', #24852, #15453, #16315, .T. ) ;
#19644=CARTESIAN_POINT ( 'NONE',  ( 78.45565513354563336, 64.70068626995113448, -3.258123098320685695 ) ) ;
#19647=CARTESIAN_POINT ( 'NONE',  ( 79.11601629524606949, 66.18432715369988273, -1.588372325568319754 ) ) ;
#19649=CARTESIAN_POINT ( 'NONE',  ( 80.29582733418162377, 61.38465067277563492, 2.608847861177660210 ) ) ;
#19651=CARTESIAN_POINT ( 'NONE',  ( 82.35470118046110599, 62.54510421749742477, 1.103079483641125069 ) ) ;
#19652=CARTESIAN_POINT ( 'NONE',  ( -63.70768058868310391, 44.39675795731061214, 1.000000000000000000 ) ) ;
#19655=CARTESIAN_POINT ( 'NONE',  ( -64.58420500176733015, 36.29544061437565716, -5.991211914497585944 ) ) ;
#19668=CARTESIAN_POINT ( 'NONE',  ( -60.14275962559869981, 24.84364830758654108, -9.154021781743367114 ) ) ;
#19672=AXIS2_PLACEMENT_3D ( 'NONE', #24024, #30216, #4700 ) ;
#19676=CARTESIAN_POINT ( 'NONE',  ( 66.68517307240369973, 57.97439930951417608, 3.998354769216140525 ) ) ;
#19685=DIRECTION ( 'NONE',  ( -1.000000000000000000, 0.000000000000000000, 0.000000000000000000 ) ) ;
#19688=CARTESIAN_POINT ( 'NONE',  ( 78.44852601586514140, 65.88695166727248420, -1.521414672925273770 ) ) ;
#19689=CARTESIAN_POINT ( 'NONE',  ( 78.90889979212963112, 65.37513451817271459, 2.884918531047065748 ) ) ;
#19707=CARTESIAN_POINT ( 'NONE',  ( 80.53345128649188212, 64.37995495044675920, 3.533418250979424968 ) ) ;
#19720=CARTESIAN_POINT ( 'NONE',  ( 68.48614864092384380, 58.93304109727553453, 3.970924506823388711 ) ) ;
#19726=CARTESIAN_POINT ( 'NONE',  ( 81.13325097526887930, 61.29068799862991312, -1.183438861787473151 ) ) ;
#19735=CARTESIAN_POINT ( 'NONE',  ( 80.33017967436555296, 63.51919597486878644, -3.679799701112255850 ) ) ;
#19739=CARTESIAN_POINT ( 'NONE',  ( 81.16688244586958945, 61.30299313749268464, -1.050153991572639667 ) ) ;
#19744=CARTESIAN_POINT ( 'NONE',  ( -64.08758708074094557, 42.81038502649571598, -3.275296300469149546 ) ) ;
#19745=CARTESIAN_POINT ( 'NONE',  ( 70.96793116520528599, 59.41887718710786714, 3.976054184260645386 ) ) ;
#19754=CARTESIAN_POINT ( 'NONE',  ( 78.68583465488319462, 66.05536144407729182, 1.071687152257635667 ) ) ;
#19757=ORIENTED_EDGE ( 'NONE', *, *, #2396, .F. ) ;
#19765=DIRECTION ( 'NONE',  ( 0.000000000000000000, -0.000000000000000000, -1.000000000000000000 ) ) ;
#19777=CARTESIAN_POINT ( 'NONE',  ( 66.27376694609004915, 57.73522568913436004, -4.000000000000000000 ) ) ;
#19780=CIRCLE ( 'NONE', #31634, 1.000000000000003997 ) ;
#19784=CARTESIAN_POINT ( 'NONE',  ( -58.07367359896441172, 31.71941035118960883, -4.399945119674323557 ) ) ;
#19787=CARTESIAN_POINT ( 'NONE',  ( 80.64785791202326948, 66.17610879001705371, -1.553473047276890284 ) ) ;
#19791=CARTESIAN_POINT ( 'NONE',  ( 74.91689101425367880, 62.74844471888589226, -3.527522301306301511 ) ) ;
#19795=CARTESIAN_POINT ( 'NONE',  ( 77.22142874756848130, 60.78359660874929915, 3.498861892161886811 ) ) ;
#19796=ORIENTED_EDGE ( 'NONE', *, *, #39824, .F. ) ;
#19797=ORIENTED_EDGE ( 'NONE', *, *, #40713, .F. ) ;
#19803=CARTESIAN_POINT ( 'NONE',  ( 81.69611827519081260, 64.99316753419206805, 2.512558077907662391 ) ) ;
#19808=CARTESIAN_POINT ( 'NONE',  ( -63.96695182803194513, 19.27020452292901709, 8.800414904976364028 ) ) ;
#19815=CARTESIAN_POINT ( 'NONE',  ( -63.48446588846724836, 43.17223388165376718, -3.327560541823090023 ) ) ;
#19823=CARTESIAN_POINT ( 'NONE',  ( 67.14845837397145090, 58.06767444754134289, -3.999036733496184048 ) ) ;
#19830=SHAPE_REPRESENTATION ( 'Press Handle', ( #30744 ), #18224 ) ;
#19837=CARTESIAN_POINT ( 'NONE',  ( 80.75501959326771839, 63.35152955421530407, 3.552238747020031617 ) ) ;
#19841=CARTESIAN_POINT ( 'NONE',  ( 79.88607388276625443, 61.09294650314146935, -2.551779361026688342 ) ) ;
#19844=CARTESIAN_POINT ( 'NONE',  ( 79.64807995745978531, 65.91648781525297807, -2.476693319882547151 ) ) ;
#19846=CARTESIAN_POINT ( 'NONE',  ( 78.07232077886961008, 65.35672112437505632, 2.431999527814446171 ) ) ;
#19847=CARTESIAN_POINT ( 'NONE',  ( 82.07069543531883937, 65.18928443706822407, 1.480606629405690544 ) ) ;
#19860=DIRECTION ( 'NONE',  ( 1.000000000000000000, 0.000000000000000000, 0.000000000000000000 ) ) ;
#19865=EDGE_CURVE ( 'NONE', #36812, #28074, #36419, .T. ) ;
#19869=CARTESIAN_POINT ( 'NONE',  ( 66.55222248544532704, 57.88363434508141125, 3.999616584014993759 ) ) ;
#19881=CARTESIAN_POINT ( 'NONE',  ( 79.30508931962887686, 64.72973333162801168, -3.449595662144194108 ) ) ;
#19889=EDGE_CURVE ( 'NONE', #30246, #30686, #39218, .T. ) ;
#19893=CARTESIAN_POINT ( 'NONE',  ( -57.16504416091206053, 33.41445838748276742, 4.000000000000000000 ) ) ;
#19901=CARTESIAN_POINT ( 'NONE',  ( 79.79486853628225163, 65.42109455898983583, 3.057227112800002367 ) ) ;
#19913=CARTESIAN_POINT ( 'NONE',  ( 69.05402862303502332, 59.18504256499077343, 3.962610901733955693 ) ) ;
#19916=DIRECTION ( 'NONE',  ( 0.9267318687906771491, -0.3757233601570964532, -0.000000000000000000 ) ) ;
#19918=CARTESIAN_POINT ( 'NONE',  ( 79.44789965344524774, 65.49939714349790165, -2.911438267503722699 ) ) ;
#19920=CARTESIAN_POINT ( 'NONE',  ( -63.08758708074093136, 38.13199975834722011, -3.043809435734137647 ) ) ;
#19926=CARTESIAN_POINT ( 'NONE',  ( 80.02704812380972044, 64.10187485077996428, -3.679799701112256738 ) ) ;
#19928=CARTESIAN_POINT ( 'NONE',  ( 80.74944977059911366, 62.67191958473371471, 3.380189700376619921 ) ) ;
#19937=CARTESIAN_POINT ( 'NONE',  ( -63.53001610672649946, 43.42049052265932829, -3.126256110287076062 ) ) ;
#19938=CARTESIAN_POINT ( 'NONE',  ( 72.33948634203015615, 59.36795819651598549, 3.882941974771883853 ) ) ;
#19940=ORIENTED_EDGE ( 'NONE', *, *, #2688, .T. ) ;
#19946=CARTESIAN_POINT ( 'NONE',  ( 79.06287735989729981, 66.15384612319691371, 1.644402879622035574 ) ) ;
#19971=ORIENTED_EDGE ( 'NONE', *, *, #3566, .T. ) ;
#19975=CARTESIAN_POINT ( 'NONE',  ( -58.37631287976133621, 28.09510535829620537, -3.265447219236182974 ) ) ;
#19979=CARTESIAN_POINT ( 'NONE',  ( 81.16926347961613430, 61.30386509772021242, -1.017094602978584117 ) ) ;
#19983=CARTESIAN_POINT ( 'NONE',  ( 76.68479537131440793, 60.43247505492704619, -3.462570962778662942 ) ) ;
#19987=CARTESIAN_POINT ( 'NONE',  ( 75.23821009641450530, 63.49083772021887739, 3.097219288951023053 ) ) ;
#19988=EDGE_LOOP ( 'NONE', ( #33094, #26277, #499, #16644 ) ) ;
#19989=CARTESIAN_POINT ( 'NONE',  ( -62.81463675898083210, 36.67811266762162603, 4.600311178732274797 ) ) ;
#19996=CARTESIAN_POINT ( 'NONE',  ( 81.97757951650707753, 62.12693032551453598, 1.780213741554580453 ) ) ;
#20010=CARTESIAN_POINT ( 'NONE',  ( -63.63850063552979464, 44.01514332744383040, -2.406330881576853820 ) ) ;
#20015=CARTESIAN_POINT ( 'NONE',  ( -64.08758708074093136, 38.76906266698302517, -3.000000000000000000 ) ) ;
#20016=CARTESIAN_POINT ( 'NONE',  ( 67.21949607617069944, 57.87245792367627928, -3.992323350375291291 ) ) ;
#20032=CARTESIAN_POINT ( 'NONE',  ( 80.30248525907988721, 64.25517361537380623, 3.614389211669656543 ) ) ;
#20033=CARTESIAN_POINT ( 'NONE',  ( -63.08758708074093136, 41.04287353446839148, 4.000000000000000000 ) ) ;
#20034=EDGE_LOOP ( 'NONE', ( #17890, #7386 ) ) ;
#20035=CARTESIAN_POINT ( 'NONE',  ( 79.57354641881573798, 61.78191946445392091, -3.317372267376139661 ) ) ;
#20039=CARTESIAN_POINT ( 'NONE',  ( 80.25728969399251866, 65.34460247849949610, -3.089171411835852865 ) ) ;
#20040=CARTESIAN_POINT ( 'NONE',  ( 80.18735707129573598, 62.48858554017570555, 3.489618106120242036 ) ) ;
#20045=ORIENTED_EDGE ( 'NONE', *, *, #3905, .T. ) ;
#20046=CARTESIAN_POINT ( 'NONE',  ( 82.25590015743745198, 64.89408798057375805, 1.328060019257126356 ) ) ;
#20047=CARTESIAN_POINT ( 'NONE',  ( -64.08758708074095978, 44.07191801957395683, 1.393174556440925249 ) ) ;
#20048=ORIENTED_EDGE ( 'NONE', *, *, #26551, .T. ) ;
#20050=DIRECTION ( 'NONE',  ( -0.9267318687906771491, 0.3757233601570964532, 0.000000000000000000 ) ) ;
#20056=CIRCLE ( 'NONE', #2320, 1.000000000000000888 ) ;
#20058=ORIENTED_EDGE ( 'NONE', *, *, #35541, .F. ) ;
#20063=CARTESIAN_POINT ( 'NONE',  ( -64.94969918204330384, 34.86787045525706219, -6.612452343231766783 ) ) ;
#20064=DIRECTION ( 'NONE',  ( 0.000000000000000000, -0.000000000000000000, -1.000000000000000000 ) ) ;
#20070=CARTESIAN_POINT ( 'NONE',  ( 66.87706763805377363, 57.90143666482605056, 3.999241724014405364 ) ) ;
#20071=CARTESIAN_POINT ( 'NONE',  ( 71.19973236181560594, 58.84349373463830091, -3.887826097256417146 ) ) ;
#20083=CARTESIAN_POINT ( 'NONE',  ( 80.75607764207482830, 61.50646045904603199, -2.414331286641652419 ) ) ;
#20085=CARTESIAN_POINT ( 'NONE',  ( 79.20958446297085231, 65.00485465208082303, 3.275607309966509284 ) ) ;
#20094=CYLINDRICAL_SURFACE ( 'NONE', #27398, 1.000000000000000000 ) ;
#20098=CARTESIAN_POINT ( 'NONE',  ( 80.61469348477540109, 64.03810969304559819, 3.562450064734659527 ) ) ;
#20105=CARTESIAN_POINT ( 'NONE',  ( -64.12095013931764242, 35.34012592920250739, 4.384900748508816726 ) ) ;
#20112=CARTESIAN_POINT ( 'NONE',  ( -64.08758708074093136, 43.61223004741322740, -1.000000000000000000 ) ) ;
#20114=CARTESIAN_POINT ( 'NONE',  ( 79.28289924135638955, 65.69038102574751292, -2.688322534164182542 ) ) ;
#20117=CARTESIAN_POINT ( 'NONE',  ( -58.98400447371446376, 28.74159977738611715, 6.613141227606677219 ) ) ;
#20126=CARTESIAN_POINT ( 'NONE',  ( 79.95665241583039062, 64.06168528317456889, -3.692178340560190897 ) ) ;
#20128=CARTESIAN_POINT ( 'NONE',  ( 80.78100857081943786, 62.68361397997274054, 3.372125408468113594 ) ) ;
#20137=CARTESIAN_POINT ( 'NONE',  ( -64.08758708074093136, 42.48851732723078811, -2.660621165554523326 ) ) ;
#20147=CARTESIAN_POINT ( 'NONE',  ( 81.55137728095093053, 62.42468454963330515, 2.710336141772879959 ) ) ;
#20150=ORIENTED_EDGE ( 'NONE', *, *, #24932, .F. ) ;
#20151=ADVANCED_FACE ( 'NONE', ( #35517 ), #23434, .T. ) ;
#20167=CIRCLE ( 'NONE', #21511, 0.9999999999999996669 ) ;
#20168=ADVANCED_FACE ( 'NONE', ( #10573 ), #23147, .T. ) ;
#20169=CARTESIAN_POINT ( 'NONE',  ( 66.27376694609004915, 57.73522568913436004, -4.000000000000000000 ) ) ;
#20171=ADVANCED_FACE ( 'NONE', ( #11368 ), #24350, .F. ) ;
#20176=CARTESIAN_POINT ( 'NONE',  ( -57.13133194381637736, 29.70675091384814337, -4.151468609674966004 ) ) ;
#20181=CARTESIAN_POINT ( 'NONE',  ( 79.30570723442072278, 66.28915683679505833, -1.250621450094244080 ) ) ;
#20186=CARTESIAN_POINT ( 'NONE',  ( 76.81167355577598244, 60.15069890908834083, 3.230144225296844418 ) ) ;
#20193=CARTESIAN_POINT ( 'NONE',  ( 81.76431320972403682, 64.63772642544205382, 2.665107514500538066 ) ) ;
#20199=CARTESIAN_POINT ( 'NONE',  ( -64.85784325972052500, 34.81586596186941307, 6.466735817496045868 ) ) ;
#20207=CARTESIAN_POINT ( 'NONE',  ( -63.24191987307168006, 41.86289664080484840, -3.933528212093161169 ) ) ;
#20215=CARTESIAN_POINT ( 'NONE',  ( 67.16030903438456789, 58.03511467963866011, -3.999036733496184048 ) ) ;
#20221=CARTESIAN_POINT ( 'NONE',  ( 78.69038500580361983, 66.05859403932463181, 1.083698948140488394 ) ) ;
#20225=CIRCLE ( 'NONE', #10934, 2.500000000000002220 ) ;
#20229=CARTESIAN_POINT ( 'NONE',  ( 78.95300076920055687, 65.89750638847961284, 2.156541836018599501 ) ) ;
#20232=CARTESIAN_POINT ( 'NONE',  ( 78.07544678589873399, 65.62285883043881540, -1.832491541757240494 ) ) ;
#20235=CARTESIAN_POINT ( 'NONE',  ( 80.97210443045602801, 64.61276409570730550, -3.292658836668131084 ) ) ;
#20236=CARTESIAN_POINT ( 'NONE',  ( 78.95339491453125902, 64.13176242216603384, 3.627744115730410002 ) ) ;
#20238=CARTESIAN_POINT ( 'NONE',  ( 82.53033050081238287, 64.25366301186838314, 1.161365684106807850 ) ) ;
#20243=CARTESIAN_POINT ( 'NONE',  ( -64.52806261857494974, 36.37942767234955710, -5.858659361856752845 ) ) ;
#20244=ORIENTED_EDGE ( 'NONE', *, *, #2738, .F. ) ;
#20251=CARTESIAN_POINT ( 'NONE',  ( -63.08379346057678561, 18.80112958435940840, -9.800414904976365804 ) ) ;
#20260=CARTESIAN_POINT ( 'NONE',  ( 66.27376694608996388, 57.73522568913447373, 4.000000000000000000 ) ) ;
#20261=CARTESIAN_POINT ( 'NONE',  ( 71.99851445618389789, 60.18445664521269123, -3.955776929956313470 ) ) ;
#20274=CARTESIAN_POINT ( 'NONE',  ( 80.70428644432419674, 61.65645308977152439, -2.679976076788562089 ) ) ;
#20276=CARTESIAN_POINT ( 'NONE',  ( 79.50008710437312232, 64.50769319364337662, 3.547878946066072015 ) ) ;
#20280=FACE_OUTER_BOUND ( 'NONE', #17590, .T. ) ;
#20285=CARTESIAN_POINT ( 'NONE',  ( 73.85882785809795337, 62.69890035364841907, -3.253129289162608906 ) ) ;
#20291=CARTESIAN_POINT ( 'NONE',  ( 78.67160034737365493, 66.04525015085647510, 1.145133111591879471 ) ) ;
#20302=CARTESIAN_POINT ( 'NONE',  ( 67.76947924466990969, 58.18518750870053680, 3.996132678073308853 ) ) ;
#20308=CARTESIAN_POINT ( 'NONE',  ( 80.54296318544950850, 63.62250603730376497, -3.633989118465182688 ) ) ;
#20317=DIRECTION ( 'NONE',  ( 0.000000000000000000, 0.000000000000000000, 1.000000000000000000 ) ) ;
#20320=CARTESIAN_POINT ( 'NONE',  ( 80.47318323629822601, 63.22351390842185737, -3.619557188109181922 ) ) ;
#20322=CARTESIAN_POINT ( 'NONE',  ( 79.10907727509496112, 65.55534887285796231, 2.778975589575228167 ) ) ;
#20342=CARTESIAN_POINT ( 'NONE',  ( 79.42963897888203917, 66.02853703564775856, 2.226826180281127332 ) ) ;
#20345=VERTEX_POINT ( 'NONE', #40199 ) ;
#20347=DIRECTION ( 'NONE',  ( 1.000000000000000000, 0.000000000000000000, 0.000000000000000000 ) ) ;
#20361=ORIENTED_EDGE ( 'NONE', *, *, #1649, .F. ) ;
#20375=CARTESIAN_POINT ( 'NONE',  ( 80.30118292188586793, 66.27423127454432006, -1.564050819714060792 ) ) ;
#20384=CARTESIAN_POINT ( 'NONE',  ( 74.16083781478751291, 62.90537518464178390, 3.184487947857685519 ) ) ;
#20386=CARTESIAN_POINT ( 'NONE',  ( -62.89172142731288062, 37.18122596373011390, 4.326867315595950281 ) ) ;
#20389=CARTESIAN_POINT ( 'NONE',  ( -62.81463675898083210, 36.67811266762162603, 4.600311178732273021 ) ) ;
#20391=CARTESIAN_POINT ( 'NONE',  ( 82.07485033897428650, 63.29559580402029439, 2.558871340112365278 ) ) ;
#20396=CARTESIAN_POINT ( 'NONE',  ( -63.08758708074094557, 43.61223004741322740, 1.000000000000000000 ) ) ;
#20407=DIRECTION ( 'NONE',  ( -0.3757233601570931225, -0.9267318687906784813, 0.000000000000000000 ) ) ;
#20413=CARTESIAN_POINT ( 'NONE',  ( 67.68985761519660116, 58.40038676363953840, -3.993918888840240822 ) ) ;
#20427=CARTESIAN_POINT ( 'NONE',  ( 78.83705574937599181, 66.00318003113706311, 1.852607187800926036 ) ) ;
#20428=CARTESIAN_POINT ( 'NONE',  ( -63.38847523777653237, 42.65083663216248766, 3.660712078102464684 ) ) ;
#20430=CARTESIAN_POINT ( 'NONE',  ( 78.25991397077976330, 61.55280089391294496, -3.597602401604586220 ) ) ;
#20433=CARTESIAN_POINT ( 'NONE',  ( 80.36688112371665227, 65.40474626848705952, -3.015199126117773964 ) ) ;
#20434=CARTESIAN_POINT ( 'NONE',  ( 78.53692321045886615, 63.86140601108343873, 3.670385203786641348 ) ) ;
#20438=AXIS2_PLACEMENT_3D ( 'NONE', #24563, #34064, #36711 ) ;
#20439=CARTESIAN_POINT ( 'NONE',  ( 82.50386574309253263, 63.87755912629621236, 1.586031901069098193 ) ) ;
#20443=CARTESIAN_POINT ( 'NONE',  ( -64.62035675220391795, 36.25855371424816553, -6.071883532252270399 ) ) ;
#20460=CARTESIAN_POINT ( 'NONE',  ( 66.58157743075884127, 57.80130068828511014, 3.999688274311175906 ) ) ;
#20461=CARTESIAN_POINT ( 'NONE',  ( 72.46216784064273497, 59.07243765930573431, -3.784404822033881288 ) ) ;
#20474=CARTESIAN_POINT ( 'NONE',  ( 80.80164418317316688, 61.17044828488888442, -1.584170212883418305 ) ) ;
#20476=CARTESIAN_POINT ( 'NONE',  ( 78.96152850399714396, 65.10675657659960791, 3.115013800517340670 ) ) ;
#20485=EDGE_CURVE ( 'NONE', #7709, #33117, #18064, .T. ) ;
#20492=CARTESIAN_POINT ( 'NONE',  ( 81.34759249528946157, 61.83023590116508217, 2.361823859647546264 ) ) ;
#20497=CARTESIAN_POINT ( 'NONE',  ( -64.08758708074093136, 36.14363715547680300, 3.800414904976363140 ) ) ;
#20499=DIRECTION ( 'NONE',  ( -0.000000000000000000, 0.000000000000000000, -1.000000000000000000 ) ) ;
#20500=CARTESIAN_POINT ( 'NONE',  ( 67.98336428835678191, 58.50351186300884621, 3.992939643064463695 ) ) ;
#20504=CARTESIAN_POINT ( 'NONE',  ( 81.08836214216864846, 62.22329742272083308, -2.932725070486247532 ) ) ;
#20509=CARTESIAN_POINT ( 'NONE',  ( -59.00096901216079459, 28.68090462335501201, 7.030006629679628638 ) ) ;
#20515=CARTESIAN_POINT ( 'NONE',  ( 80.91173626137313590, 62.16536564854128954, -2.996423812020329258 ) ) ;
#20518=CARTESIAN_POINT ( 'NONE',  ( 79.12626349118839642, 65.57005066984849861, 2.769656700700049878 ) ) ;
#20536=ADVANCED_FACE ( 'NONE', ( #11470 ), #28618, .T. ) ;
#20539=CARTESIAN_POINT ( 'NONE',  ( 80.30538902757352560, 65.37113732873363858, 3.059106349699973304 ) ) ;
#20554=CIRCLE ( 'NONE', #2850, 0.9999999999999976685 ) ;
#20568=CARTESIAN_POINT ( 'NONE',  ( -57.76433750236255804, 32.39122475941741186, -4.160719226838292428 ) ) ;
#20572=CARTESIAN_POINT ( 'NONE',  ( 80.42596214810023980, 66.05751922670441445, -2.080779877698640590 ) ) ;
#20580=CARTESIAN_POINT ( 'NONE',  ( 73.70000790436553473, 62.44749314232890924, 3.395557233589456825 ) ) ;
#20585=CARTESIAN_POINT ( 'NONE',  ( -56.34850605459113382, 30.68671187671608536, -2.749655849400832963 ) ) ;
#20586=DIRECTION ( 'NONE',  ( -1.000000000000000000, 0.000000000000000000, 0.000000000000000000 ) ) ;
#20590=CARTESIAN_POINT ( 'NONE',  ( 78.90307038293786945, 66.16006992971016132, 1.301239782962659852 ) ) ;
#20609=CARTESIAN_POINT ( 'NONE',  ( 67.63028434841179148, 58.56128740577801750, -3.979762160777184477 ) ) ;
#20619=DIRECTION ( 'NONE',  ( 0.000000000000000000, 1.000000000000000000, 0.000000000000000000 ) ) ;
#20623=CARTESIAN_POINT ( 'NONE',  ( 81.62248346935345467, 65.70993096190730398, -1.153249692834613427 ) ) ;
#20625=CARTESIAN_POINT ( 'NONE',  ( 80.57402935197536920, 63.63785766202913408, 3.625945587094185463 ) ) ;
#20628=CARTESIAN_POINT ( 'NONE',  ( 77.25588627614904169, 64.91391695767343606, -2.512892981323163077 ) ) ;
#20631=CARTESIAN_POINT ( 'NONE',  ( 81.06025503660893605, 64.27053461118835287, -3.341858160548295320 ) ) ;
#20633=CARTESIAN_POINT ( 'NONE',  ( 77.50572060368776306, 65.09508644891811002, 2.418543376929332744 ) ) ;
#20639=CARTESIAN_POINT ( 'NONE',  ( 82.29396208789067657, 62.51418980721558682, 1.483157530538788516 ) ) ;
#20641=LINE ( 'NONE', #5212, #28845 ) ;
#20649=FACE_OUTER_BOUND ( 'NONE', #21056, .T. ) ;
#20662=CARTESIAN_POINT ( 'NONE',  ( -69.08758708074093136, 36.88538962427716683, -8.800414904976364028 ) ) ;
#20664=CARTESIAN_POINT ( 'NONE',  ( 66.42891085676512830, 57.77139747978236528, 4.000000000000007994 ) ) ;
#20665=CARTESIAN_POINT ( 'NONE',  ( 73.01418189060618147, 60.96508932706621664, -3.894134109168989610 ) ) ;
#20666=VECTOR ( 'NONE', #38888, 1000.000000000000000 ) ;
#20680=CARTESIAN_POINT ( 'NONE',  ( 78.76746739705249922, 65.24896075961403596, -2.948506306558722478 ) ) ;
#20682=CARTESIAN_POINT ( 'NONE',  ( 78.54017873204453792, 65.73972836631979533, 2.148686496494747633 ) ) ;
#20685=CIRCLE ( 'NONE', #31864, 2.681419499219045655 ) ;
#20686=DIRECTION ( 'NONE',  ( 0.000000000000000000, 0.000000000000000000, -1.000000000000000000 ) ) ;
#20700=CARTESIAN_POINT ( 'NONE',  ( 80.21507364257671213, 64.59331366548808262, 3.526329879082135577 ) ) ;
#20705=CARTESIAN_POINT ( 'NONE',  ( -64.13386656030947108, 35.23920786735105537, 4.488055666952388556 ) ) ;
#20708=VERTEX_POINT ( 'NONE', #34168 ) ;
#20709=CARTESIAN_POINT ( 'NONE',  ( 68.03141654933527604, 58.37504561612195886, 3.996230182412892074 ) ) ;
#20714=AXIS2_PLACEMENT_3D ( 'NONE', #30675, #33565, #8009 ) ;
#20717=CARTESIAN_POINT ( 'NONE',  ( 81.12869333199854793, 61.28902183752150989, -1.194943971655652692 ) ) ;
#20723=ADVANCED_FACE ( 'NONE', ( #31058 ), #21997, .T. ) ;
#20727=CARTESIAN_POINT ( 'NONE',  ( 80.18433095895142060, 63.45046554133029559, -3.702313260098204051 ) ) ;
#20729=CARTESIAN_POINT ( 'NONE',  ( 80.65169068708814848, 62.63775009584345099, 3.403428918328332387 ) ) ;
#20733=CARTESIAN_POINT ( 'NONE',  ( 74.86608108239484238, 61.39286988729297434, -3.912919437578932236 ) ) ;
#20748=CARTESIAN_POINT ( 'NONE',  ( 78.68330935989222041, 66.05356751642948154, 1.089225060639253950 ) ) ;
#20753=TOROIDAL_SURFACE ( 'NONE', #16812, 82.54614097552274643, 3.000000000000000000 ) ;
#20776=EDGE_LOOP ( 'NONE', ( #27384, #31890 ) ) ;
#20778=CARTESIAN_POINT ( 'NONE',  ( 81.06670574969137988, 62.21556664890213284, -2.940771700540079969 ) ) ;
#20786=CARTESIAN_POINT ( 'NONE',  ( 81.78811924969963343, 65.04137315806627839, -2.360008641315554545 ) ) ;
#20792=CARTESIAN_POINT ( 'NONE',  ( 75.58356882164667923, 59.79721036961943526, 3.404024988867351720 ) ) ;
#20798=CARTESIAN_POINT ( 'NONE',  ( -66.90228649915854930, 37.07846761000362790, 9.592188357273904842 ) ) ;
#20800=CARTESIAN_POINT ( 'NONE',  ( 81.31254497084479738, 65.18305021144017530, 2.731810022747817701 ) ) ;
#20807=DIRECTION ( 'NONE',  ( 0.000000000000000000, -1.000000000000000000, 0.000000000000000000 ) ) ;
#20815=ORIENTED_EDGE ( 'NONE', *, *, #5919, .F. ) ;
#20818=CARTESIAN_POINT ( 'NONE',  ( 66.73227421799262515, 57.84320248636868200, -3.999246569070631363 ) ) ;
#20824=EDGE_CURVE ( 'NONE', #18734, #11497, #11879, .T. ) ;
#20832=CARTESIAN_POINT ( 'NONE',  ( 82.51683713915174678, 64.24667231656792410, -1.319711737400975915 ) ) ;
#20833=CARTESIAN_POINT ( 'NONE',  ( 79.55838722571232324, 65.27247487857080444, 3.155412080370055605 ) ) ;
#20837=CARTESIAN_POINT ( 'NONE',  ( 78.95923394621955538, 61.57577394195563159, -3.401348408886269770 ) ) ;
#20841=CARTESIAN_POINT ( 'NONE',  ( 81.35401977073111368, 62.93507997573861701, -3.162824939344917041 ) ) ;
#20842=CARTESIAN_POINT ( 'NONE',  ( 78.65659160455585663, 63.63274296288032161, 3.750642650174855319 ) ) ;
#20848=CARTESIAN_POINT ( 'NONE',  ( 79.30570723442079384, 66.28915683679507254, 1.250621450094003384 ) ) ;
#20850=CARTESIAN_POINT ( 'NONE',  ( -64.08758708074093136, 38.13199975834322686, 3.043809435734686097 ) ) ;
#20866=CARTESIAN_POINT ( 'NONE',  ( -75.45330471031414277, 33.71485196875532608, -8.800414904976364028 ) ) ;
#20871=EDGE_CURVE ( 'NONE', #33155, #22837, #6949, .T. ) ;
#20877=CARTESIAN_POINT ( 'NONE',  ( 66.27376694608996388, 57.73522568913447373, 4.000000000000000000 ) ) ;
#20879=CARTESIAN_POINT ( 'NONE',  ( 71.13429564674895289, 59.00621471515203353, -3.925556587156297628 ) ) ;
#20881=ORIENTED_EDGE ( 'NONE', *, *, #40286, .F. ) ;
#20892=ORIENTED_EDGE ( 'NONE', *, *, #19443, .F. ) ;
#20893=CARTESIAN_POINT ( 'NONE',  ( 80.27814043029276547, 62.51814696698978935, -3.475409704257724997 ) ) ;
#20895=CARTESIAN_POINT ( 'NONE',  ( 80.45692750329149590, 65.79057296784165487, -2.573500632437589086 ) ) ;
#20896=CARTESIAN_POINT ( 'NONE',  ( 79.84106601136197412, 63.63461245521319398, 3.725738571856552550 ) ) ;
#20922=CIRCLE ( 'NONE', #26207, 0.9999999999999994449 ) ;
#20923=CARTESIAN_POINT ( 'NONE',  ( 67.66003928550829016, 58.48093499090138891, 3.988165415173012374 ) ) ;
#20930=LINE ( 'NONE', #40680, #32708 ) ;
#20937=CARTESIAN_POINT ( 'NONE',  ( 80.72421460287552009, 62.36539998118918504, -3.243225924683091232 ) ) ;
#20939=CARTESIAN_POINT ( 'NONE',  ( 78.57229106431512378, 65.97474043420317003, 1.364493914842173306 ) ) ;
#20944=EDGE_CURVE ( 'NONE', #18695, #34099, #25887, .T. ) ;
#20945=CARTESIAN_POINT ( 'NONE',  ( 74.27115401224453706, 62.67359094190467772, -3.404024988867591084 ) ) ;
#20947=CIRCLE ( 'NONE', #16995, 6.329987104167475565 ) ;
#20951=FACE_OUTER_BOUND ( 'NONE', #24709, .T. ) ;
#20956=ADVANCED_FACE ( 'NONE', ( #31875 ), #10227, .T. ) ;
#20962=CARTESIAN_POINT ( 'NONE',  ( 81.16306007146954471, 61.30159356321340169, 1.077711394955742863 ) ) ;
#20981=CARTESIAN_POINT ( 'NONE',  ( 81.13213036240664167, 62.83067685251092627, -3.261148789966863859 ) ) ;
#20992=CARTESIAN_POINT ( 'NONE',  ( 80.89892670780336914, 62.72941125082673608, -3.340002271463665906 ) ) ;
#20998=CARTESIAN_POINT ( 'NONE',  ( 81.77194423968612114, 61.86568514665825802, -1.662695954554818778 ) ) ;
#21006=CARTESIAN_POINT ( 'NONE',  ( 74.72645207833699033, 61.69672356374137223, 3.865308561588414182 ) ) ;
#21015=CARTESIAN_POINT ( 'NONE',  ( -65.62105494222964808, 35.19887319331469655, 7.481751891072599747 ) ) ;
#21017=CARTESIAN_POINT ( 'NONE',  ( 81.96106518217335690, 62.90574382782723717, 2.573500632437473623 ) ) ;
#21039=CARTESIAN_POINT ( 'NONE',  ( 66.72344311391505300, 57.86780257000127392, -3.999628797551961767 ) ) ;
#21053=CARTESIAN_POINT ( 'NONE',  ( 82.09527124944445120, 65.20214329949099863, -1.328060019258380242 ) ) ;
#21054=CARTESIAN_POINT ( 'NONE',  ( 81.18881611591316982, 61.34569122823197773, 1.520709669156496968 ) ) ;
#21056=EDGE_LOOP ( 'NONE', ( #32132, #40060, #38502, #33437 ) ) ;
#21057=CARTESIAN_POINT ( 'NONE',  ( 77.93772202372294089, 64.31926776197542495, -3.361664161258271388 ) ) ;
#21060=CARTESIAN_POINT ( 'NONE',  ( 80.86168855680497813, 64.16696250863120099, -3.456914256419914011 ) ) ;
#21061=CARTESIAN_POINT ( 'NONE',  ( 79.66831987096976775, 61.58041732747442865, 3.164065397988992778 ) ) ;
#21065=CARTESIAN_POINT ( 'NONE',  ( 80.99740051111626826, 66.07939114927827973, 1.509105202934762024 ) ) ;
#21083=CYLINDRICAL_SURFACE ( 'NONE', #36457, 83.68529983683480111 ) ;
#21091=CARTESIAN_POINT ( 'NONE',  ( 66.43286826475038254, 57.76021747899728354, 4.000000000000004441 ) ) ;
#21092=CARTESIAN_POINT ( 'NONE',  ( 69.17602579976487220, 58.86946863987066791, -3.990151341881416514 ) ) ;
#21100=CARTESIAN_POINT ( 'NONE',  ( -75.45330471031414277, 33.71485196875532608, -12.49999999999999645 ) ) ;
#21107=DIRECTION ( 'NONE',  ( -1.000000000000000000, -0.000000000000000000, -0.000000000000000000 ) ) ;
#21108=CIRCLE ( 'NONE', #3393, 10.99999999999998224 ) ;
#21110=CARTESIAN_POINT ( 'NONE',  ( 79.08605325858584933, 64.90301710537214319, -3.311815948186460190 ) ) ;
#21112=CARTESIAN_POINT ( 'NONE',  ( 81.16598293928451824, 61.30266375757629049, -1.057717897339658153 ) ) ;
#21113=CARTESIAN_POINT ( 'NONE',  ( 80.70428644432419674, 61.65645308977151728, 2.679976076788563866 ) ) ;
#21119=DIRECTION ( 'NONE',  ( 0.000000000000000000, 0.000000000000000000, -1.000000000000000000 ) ) ;
#21137=CARTESIAN_POINT ( 'NONE',  ( 68.06744372826909739, 58.27867795456629807, 3.994255761866622123 ) ) ;
#21141=DIRECTION ( 'NONE',  ( -0.000000000000000000, -0.000000000000000000, 1.000000000000000000 ) ) ;
#21150=CARTESIAN_POINT ( 'NONE',  ( 80.21880177947251411, 63.46656020078422955, -3.697630003121159081 ) ) ;
#21153=CARTESIAN_POINT ( 'NONE',  ( 79.30978077413506355, 65.08723789429433282, 3.243225924683099226 ) ) ;
#21156=EDGE_CURVE ( 'NONE', #8770, #25652, #20056, .T. ) ;
#21157=CARTESIAN_POINT ( 'NONE',  ( 73.33958664722344167, 61.75625940721955942, -3.692213121420756305 ) ) ;
#21172=CARTESIAN_POINT ( 'NONE',  ( 81.42004705248814389, 62.63944267392375309, 2.989933650883211502 ) ) ;
#21175=VERTEX_POINT ( 'NONE', #24613 ) ;
#21179=CARTESIAN_POINT ( 'NONE',  ( -67.57960606288774841, 36.15173574121457989, -8.626892781891035256 ) ) ;
#21187=EDGE_LOOP ( 'NONE', ( #5322, #29399, #19540, #12502, #15015, #4111 ) ) ;
#21188=CARTESIAN_POINT ( 'NONE',  ( 80.45774067191287315, 64.33927723362793927, -3.562450064734666189 ) ) ;
#21199=CARTESIAN_POINT ( 'NONE',  ( 79.04990754624076033, 65.77731930041099417, -2.468641556982019480 ) ) ;
#21206=CARTESIAN_POINT ( 'NONE',  ( 81.57551674523598706, 65.32158946912282715, -2.325514254129002367 ) ) ;
#21212=CARTESIAN_POINT ( 'NONE',  ( 74.43259725886051115, 60.83706718145764114, 3.924711207976804950 ) ) ;
#21218=CARTESIAN_POINT ( 'NONE',  ( -68.33309634913140940, 36.51831931741379833, 8.800414904976364028 ) ) ;
#21219=CARTESIAN_POINT ( 'NONE',  ( 82.03499260127753701, 62.66326407617584238, 2.270757614041261530 ) ) ;
#21237=CARTESIAN_POINT ( 'NONE',  ( 66.99808371854801692, 58.02529356684345885, -3.999241514195644331 ) ) ;
#21240=CARTESIAN_POINT ( 'NONE',  ( -59.01947560891952804, 27.90920910948504385, -6.147301388271595890 ) ) ;
#21243=EDGE_CURVE ( 'NONE', #12529, #32500, #20685, .T. ) ;
#21246=DIRECTION ( 'NONE',  ( -1.000000000000000000, 0.000000000000000000, 0.000000000000000000 ) ) ;
#21249=AXIS2_PLACEMENT_3D ( 'NONE', #6012, #3365, #2742 ) ;
#21254=CARTESIAN_POINT ( 'NONE',  ( 82.54681503119213914, 63.20390409618730132, -1.263752851813363609 ) ) ;
#21255=CARTESIAN_POINT ( 'NONE',  ( 79.49612969957790654, 65.22981380272329943, 3.178394274514609208 ) ) ;
#21259=CARTESIAN_POINT ( 'NONE',  ( 78.76819457884754172, 61.97782169454064416, -3.640295653904960904 ) ) ;
#21262=CARTESIAN_POINT ( 'NONE',  ( 81.49799543786826916, 62.67690593247225905, -2.943961322783049450 ) ) ;
#21263=CARTESIAN_POINT ( 'NONE',  ( 78.50009633871025017, 63.24008633025189852, 3.804514705604313374 ) ) ;
#21268=CARTESIAN_POINT ( 'NONE',  ( 81.56437483599492566, 65.67932636690383674, 1.586031901069098193 ) ) ;
#21277=FACE_OUTER_BOUND ( 'NONE', #18434, .T. ) ;
#21294=CARTESIAN_POINT ( 'NONE',  ( 69.39861229970156842, 58.29198505329483027, -3.933428174212718176 ) ) ;
#21296=ORIENTED_EDGE ( 'NONE', *, *, #27472, .F. ) ;
#21299=CARTESIAN_POINT ( 'NONE',  ( 69.99634961962405555, 58.48381665884328839, 3.916752429509930078 ) ) ;
#21305=ORIENTED_EDGE ( 'NONE', *, *, #4609, .F. ) ;
#21307=EDGE_CURVE ( 'NONE', #32308, #16760, #11715, .T. ) ;
#21308=DIRECTION ( 'NONE',  ( -1.000000000000000000, 0.000000000000000000, 0.000000000000000000 ) ) ;
#21309=CIRCLE ( 'NONE', #29209, 5.000000000000000888 ) ;
#21313=CARTESIAN_POINT ( 'NONE',  ( 79.74939209361063774, 63.58699539661090228, -3.734652355492745102 ) ) ;
#21315=CARTESIAN_POINT ( 'NONE',  ( 81.46256558106179568, 64.48035972931448612, -3.017922835037758933 ) ) ;
#21316=CARTESIAN_POINT ( 'NONE',  ( 80.79830692519234958, 61.67796721187822584, 2.640205493567646222 ) ) ;
#21319=VERTEX_POINT ( 'NONE', #33031 ) ;
#21340=CARTESIAN_POINT ( 'NONE',  ( 67.19584252064707641, 57.93747020029492489, 3.996350724342223604 ) ) ;
#21355=EDGE_CURVE ( 'NONE', #10601, #9954, #34526, .T. ) ;
#21357=CARTESIAN_POINT ( 'NONE',  ( 79.17340063025110908, 65.28954359503943294, -3.030715982579950563 ) ) ;
#21359=ADVANCED_FACE ( 'NONE', ( #34070 ), #21083, .T. ) ;
#21360=CARTESIAN_POINT ( 'NONE',  ( 79.92041472187213458, 64.04075560556067614, 3.697630003121161302 ) ) ;
#21363=CARTESIAN_POINT ( 'NONE',  ( 74.21382537490346465, 62.79450482958245772, -3.300071129360916622 ) ) ;
#21367=CARTESIAN_POINT ( 'NONE',  ( -63.58520484588294153, 35.72026407271188475, -6.999999999999999112 ) ) ;
#21373=CARTESIAN_POINT ( 'NONE',  ( 81.51347805233932320, 61.90211215308875836, 2.263370276488428257 ) ) ;
#21382=VECTOR ( 'NONE', #24855, 1000.000000000000000 ) ;
#21385=CARTESIAN_POINT ( 'NONE',  ( -68.71186372058383540, 37.81212149306785619, -9.800414904976365804 ) ) ;
#21393=ORIENTED_EDGE ( 'NONE', *, *, #31254, .T. ) ;
#21395=CARTESIAN_POINT ( 'NONE',  ( 79.79486853628222320, 65.42109455898982162, -3.057227112800017910 ) ) ;
#21400=CARTESIAN_POINT ( 'NONE',  ( -75.45330471031414277, 33.71485196875532608, -46.17089178453873188 ) ) ;
#21403=ORIENTED_EDGE ( 'NONE', *, *, #34802, .F. ) ;
#21408=CARTESIAN_POINT ( 'NONE',  ( 81.11951992695615843, 61.28566998660698317, -1.215327096190472966 ) ) ;
#21409=CARTESIAN_POINT ( 'NONE',  ( -59.00289461565213855, 28.67396232720155780, -6.820567581290490899 ) ) ;
#21413=CARTESIAN_POINT ( 'NONE',  ( 82.26467961622988412, 63.75423115438291433, -2.259066313178065499 ) ) ;
#21415=CARTESIAN_POINT ( 'NONE',  ( -58.99872204295123623, 28.48507918597134037, -12.49999999999999645 ) ) ;
#21420=CARTESIAN_POINT ( 'NONE',  ( 72.85835069609119330, 61.31913755009141909, 3.785151435630688788 ) ) ;
#21430=CARTESIAN_POINT ( 'NONE',  ( 81.46256558106202306, 64.48035972931458559, 3.017922835037552876 ) ) ;
#21433=DIRECTION ( 'NONE',  ( -1.000000000000000000, 0.000000000000000000, 0.000000000000000000 ) ) ;
#21441=CARTESIAN_POINT ( 'NONE',  ( -63.08758708074093136, -21.25669541281728669, -3.000000000000000000 ) ) ;
#21446=CIRCLE ( 'NONE', #15528, 1.000000000000000666 ) ;
#21450=CARTESIAN_POINT ( 'NONE',  ( 66.87313677512783272, 57.91234881663538658, -3.999382933222194847 ) ) ;
#21457=ORIENTED_EDGE ( 'NONE', *, *, #33288, .T. ) ;
#21462=CARTESIAN_POINT ( 'NONE',  ( 79.34209122208885390, 66.30884595491197331, -1.000000000000000000 ) ) ;
#21463=CARTESIAN_POINT ( 'NONE',  ( 80.81256737103976207, 62.69530837521176636, 3.364061116559607267 ) ) ;
#21466=CARTESIAN_POINT ( 'NONE',  ( 77.10371989074776877, 62.50202019409577048, -3.856837490694493997 ) ) ;
#21470=CARTESIAN_POINT ( 'NONE',  ( 78.68244131272051334, 66.05295088176872298, -1.094381639753450930 ) ) ;
#21471=CARTESIAN_POINT ( 'NONE',  ( 76.39468346684418520, 63.92226846272791363, 3.160174624570346147 ) ) ;
#21475=CARTESIAN_POINT ( 'NONE',  ( 82.26850461147290616, 62.50126132183006433, 1.564050819713521223 ) ) ;
#21482=CARTESIAN_POINT ( 'NONE',  ( -64.59661209699966378, 34.69995260619790400, 6.002488439271551179 ) ) ;
#21489=ADVANCED_FACE ( 'NONE', ( #21699 ), #22672, .T. ) ;
#21502=ORIENTED_EDGE ( 'NONE', *, *, #4212, .F. ) ;
#21504=CARTESIAN_POINT ( 'NONE',  ( 69.67664977695649497, 59.29623187989270150, -3.972683913566358083 ) ) ;
#21505=VECTOR ( 'NONE', #8743, 1000.000000000000000 ) ;
#21511=AXIS2_PLACEMENT_3D ( 'NONE', #19920, #29397, #10444 ) ;
#21517=ORIENTED_EDGE ( 'NONE', *, *, #12561, .T. ) ;
#21521=CARTESIAN_POINT ( 'NONE',  ( 79.09261123048416664, 64.22416776617160394, -3.612066323963887715 ) ) ;
#21523=CARTESIAN_POINT ( 'NONE',  ( 80.65441534633333731, 65.56043466500595684, -2.771525467262166753 ) ) ;
#21525=CARTESIAN_POINT ( 'NONE',  ( 79.01107290893718016, 64.84207397985339583, 3.331801170923393673 ) ) ;
#21551=CARTESIAN_POINT ( 'NONE',  ( 67.17808119270118539, 57.98628055940345405, 3.998197261021421589 ) ) ;
#21554=FACE_OUTER_BOUND ( 'NONE', #10674, .T. ) ;
#21567=CARTESIAN_POINT ( 'NONE',  ( 80.97211960314545820, 61.55694294823970836, -2.294512580621450137 ) ) ;
#21570=CARTESIAN_POINT ( 'NONE',  ( 80.93309715666640614, 61.70751139687529729, 2.576318598473983368 ) ) ;
#21573=CARTESIAN_POINT ( 'NONE',  ( 74.14280505202560789, 59.94172787350157705, -3.795548882712136418 ) ) ;
#21574=CARTESIAN_POINT ( 'NONE',  ( -59.00071946683020485, 28.09513742959886784, 6.356270780544043930 ) ) ;
#21577=CARTESIAN_POINT ( 'NONE',  ( -54.85202521353782856, 31.46638146376523792, 1.118005318203281417 ) ) ;
#21584=CARTESIAN_POINT ( 'NONE',  ( 81.40003982928760706, 62.35377290961283592, 2.797238656122803757 ) ) ;
#21592=ADVANCED_FACE ( 'NONE', ( #21896 ), #34474, .F. ) ;
#21598=VECTOR ( 'NONE', #14517, 1000.000000000000000 ) ;
#21601=CARTESIAN_POINT ( 'NONE',  ( 79.24523542244192242, 65.91691524828223692, -2.349509806045104732 ) ) ;
#21610=CARTESIAN_POINT ( 'NONE',  ( 81.18585152890854317, 61.61024096112966220, -2.156541836018578628 ) ) ;
#21611=CARTESIAN_POINT ( 'NONE',  ( -58.56173084424084863, 30.28994157939056819, -5.156891857687778469 ) ) ;
#21612=ORIENTED_EDGE ( 'NONE', *, *, #40218, .T. ) ;
#21617=CARTESIAN_POINT ( 'NONE',  ( 81.00802433895691479, 65.38516391083560109, -2.726953404243311230 ) ) ;
#21619=ORIENTED_EDGE ( 'NONE', *, *, #36300, .T. ) ;
#21624=CARTESIAN_POINT ( 'NONE',  ( 74.74317362787380148, 60.13816936446348649, 3.762445401688810698 ) ) ;
#21627=EDGE_CURVE ( 'NONE', #9954, #1114, #13423, .T. ) ;
#21629=CARTESIAN_POINT ( 'NONE',  ( -57.31082258017699615, 33.19667476323267152, -3.999999999999999112 ) ) ;
#21631=CARTESIAN_POINT ( 'NONE',  ( -54.83720514956231540, 31.47881213581769089, -1.097840624867143733 ) ) ;
#21632=CARTESIAN_POINT ( 'NONE',  ( 78.87111998578922112, 66.14166623576274162, 1.344573736155044053 ) ) ;
#21634=B_SPLINE_CURVE_WITH_KNOTS ( 'NONE', 3,
 ( #34170, #31060, #9625, #5936, #18475, #15394, #37820, #27950, #40493, #12304, #24878, #37416, #34370, #6140 ),
 .UNSPECIFIED., .F., .F.,
 ( 4, 2, 2, 2, 2, 2, 4 ),
 ( 4.336808689942017255E-19, 0.0008516721041744092658, 0.001703344208348818098, 0.002129180260436026959, 0.002555016312523236688, 0.002980852364610445983, 0.003406688416697655278 ),
 .UNSPECIFIED. ) ;
#21637=FACE_OUTER_BOUND ( 'NONE', #21187, .T. ) ;
#21645=DIRECTION ( 'NONE',  ( 0.000000000000000000, 0.000000000000000000, 1.000000000000000000 ) ) ;
#21652=ORIENTED_EDGE ( 'NONE', *, *, #7219, .F. ) ;
#21653=CARTESIAN_POINT ( 'NONE',  ( 66.86527468745164526, 57.93417386730686758, -3.999594749379963066 ) ) ;
#21665=CARTESIAN_POINT ( 'NONE',  ( 81.16944410057618597, 61.30393124705405938, -1.011532654301245060 ) ) ;
#21666=CARTESIAN_POINT ( 'NONE',  ( 79.34351131543186852, 65.42632830064323457, 2.956864960647761720 ) ) ;
#21669=EDGE_LOOP ( 'NONE', ( #31487, #9889, #29859, #25399 ) ) ;
#21670=CARTESIAN_POINT ( 'NONE',  ( 77.48353911088550205, 60.20448024992294478, -2.970791854447082603 ) ) ;
#21676=CARTESIAN_POINT ( 'NONE',  ( 81.53538963105238224, 62.13961868399401567, -2.518708746843058677 ) ) ;
#21677=CARTESIAN_POINT ( 'NONE',  ( 76.63893934653985696, 63.44172143924968310, 3.539370024148535965 ) ) ;
#21682=CARTESIAN_POINT ( 'NONE',  ( 80.87103490326518340, 66.01227193428226769, 1.936735430445677197 ) ) ;
#21687=CARTESIAN_POINT ( 'NONE',  ( -62.99366871073556950, 35.53755692985882320, -6.184786337850739280 ) ) ;
#21688=CARTESIAN_POINT ( 'NONE',  ( -62.74303057475812295, 35.98358351542167100, 5.167368988332134982 ) ) ;
#21690=CIRCLE ( 'NONE', #18406, 2.999999999999998668 ) ;
#21693=CARTESIAN_POINT ( 'NONE',  ( 79.11873141236488038, 60.58998131946810162, 2.372212216456983214 ) ) ;
#21697=CARTESIAN_POINT ( 'NONE',  ( 71.52974698506822904, 58.56680916168235740, -3.757746881545229289 ) ) ;
#21698=CARTESIAN_POINT ( 'NONE',  ( 79.89212576172681679, 63.66154800590240370, -1.000000000000000000 ) ) ;
#21699=FACE_OUTER_BOUND ( 'NONE', #5457, .T. ) ;
#21707=CARTESIAN_POINT ( 'NONE',  ( 70.02038816076994010, 58.42250406220534131, -3.901551322707177416 ) ) ;
#21720=CARTESIAN_POINT ( 'NONE',  ( 80.18735707129573598, 62.48858554017570555, -3.489618106120242036 ) ) ;
#21722=CARTESIAN_POINT ( 'NONE',  ( 81.94287803445135410, 63.22849810396151327, -2.713791510777194382 ) ) ;
#21723=CARTESIAN_POINT ( 'NONE',  ( 79.04765299714190974, 64.87162515256790130, 3.322373183921397466 ) ) ;
#21748=CARTESIAN_POINT ( 'NONE',  ( 67.20767295658653495, 57.90495500903578829, 3.994504660676310159 ) ) ;
#21754=AXIS2_PLACEMENT_3D ( 'NONE', #2931, #21645, #16265 ) ;
#21757=VERTEX_POINT ( 'NONE', #32986 ) ;
#21760=DIRECTION ( 'NONE',  ( -0.8888117386314225987, -0.4582725098355650006, 0.000000000000000000 ) ) ;
#21766=CARTESIAN_POINT ( 'NONE',  ( 80.62613562354505348, 62.33752749645043423, -3.268578535636858629 ) ) ;
#21768=CARTESIAN_POINT ( 'NONE',  ( 80.81138441778081472, 62.13752223189714385, 3.030715982579940793 ) ) ;
#21771=CIRCLE ( 'NONE', #31654, 3.000000000000003997 ) ;
#21783=CARTESIAN_POINT ( 'NONE',  ( -77.95330471031414277, 33.71485196875532608, -12.49999999999999645 ) ) ;
#21788=CARTESIAN_POINT ( 'NONE',  ( 81.44732304147008506, 62.37541782542987789, 2.773332820898644524 ) ) ;
#21797=CARTESIAN_POINT ( 'NONE',  ( -66.22295697852544549, 35.49170696305579753, -7.967283012324265279 ) ) ;
#21799=CARTESIAN_POINT ( 'NONE',  ( -62.99901854238083843, 37.98537211836831062, 4.070195263749428527 ) ) ;
#21803=CARTESIAN_POINT ( 'NONE',  ( 80.84834833306130975, 63.77578157039148721, -3.533418250979444064 ) ) ;
#21813=CARTESIAN_POINT ( 'NONE',  ( 80.62495340926818699, 62.95361341830508906, -3.497296750721713199 ) ) ;
#21826=CARTESIAN_POINT ( 'NONE',  ( 73.06729433089581960, 60.84378783247667144, 3.914122288852233567 ) ) ;
#21837=CARTESIAN_POINT ( 'NONE',  ( 79.85781052176636763, 66.03394566247145292, 2.299173245602477156 ) ) ;
#21853=CARTESIAN_POINT ( 'NONE',  ( 66.55222248544532704, 57.88363434508141125, -3.999616584014993759 ) ) ;
#21859=DIRECTION ( 'NONE',  ( 0.000000000000000000, 0.000000000000000000, 1.000000000000000000 ) ) ;
#21865=CARTESIAN_POINT ( 'NONE',  ( 82.53887461166610251, 63.53329618120191924, -1.555014038483378158 ) ) ;
#21866=CARTESIAN_POINT ( 'NONE',  ( 81.13529310646420356, 61.59586411174932863, 2.189516896894247999 ) ) ;
#21870=CARTESIAN_POINT ( 'NONE',  ( 77.29397510068352517, 60.62518447217949813, -3.385286751607444966 ) ) ;
#21874=CARTESIAN_POINT ( 'NONE',  ( 81.36706168520306903, 62.61468991663324601, -3.015642068896332795 ) ) ;
#21875=CARTESIAN_POINT ( 'NONE',  ( 79.63092111360344916, 60.86998874196343223, 2.418543376929441546 ) ) ;
#21880=CARTESIAN_POINT ( 'NONE',  ( 82.21693166776744022, 64.09145645796296265, 2.325514254128254521 ) ) ;
#21887=CARTESIAN_POINT ( 'NONE',  ( -64.50921092724549055, 36.42665533667680933, 5.809226461016177012 ) ) ;
#21888=CARTESIAN_POINT ( 'NONE',  ( -94.24726447194083789, -65.19654454972992141, -8.800414904976364028 ) ) ;
#21894=CARTESIAN_POINT ( 'NONE',  ( 77.27624361166392930, 60.01008998901625091, -2.873380611938707752 ) ) ;
#21896=FACE_OUTER_BOUND ( 'NONE', #2996, .T. ) ;
#21900=EDGE_CURVE ( 'NONE', #36272, #32421, #31519, .T. ) ;
#21901=CIRCLE ( 'NONE', #8291, 7.999999999999992895 ) ;
#21902=CARTESIAN_POINT ( 'NONE',  ( -62.85296432947374967, 36.91960874151965299, -4.452026683640994520 ) ) ;
#21906=CARTESIAN_POINT ( 'NONE',  ( -59.00110696496997775, 28.68040728033255249, -6.999999999999999112 ) ) ;
#21907=CARTESIAN_POINT ( 'NONE',  ( 69.19640405677364470, 58.81667877646589204, -3.990151341881418290 ) ) ;
#21924=CARTESIAN_POINT ( 'NONE',  ( 79.60787101065389493, 62.86536646861404165, -3.718817779187658434 ) ) ;
#21927=CARTESIAN_POINT ( 'NONE',  ( 81.48469013494968749, 61.56585122427132006, -1.622497907168742648 ) ) ;
#21928=CARTESIAN_POINT ( 'NONE',  ( 80.02751534128088906, 63.03952351013455768, 3.681573067026198576 ) ) ;
#21938=ORIENTED_EDGE ( 'NONE', *, *, #39487, .F. ) ;
#21940=FACE_OUTER_BOUND ( 'NONE', #2642, .T. ) ;
#21953=CIRCLE ( 'NONE', #9435, 34.02204673211314656 ) ;
#21959=CARTESIAN_POINT ( 'NONE',  ( 66.95869957004099149, 58.13407781516350070, 3.995640437668404044 ) ) ;
#21964=DIRECTION ( 'NONE',  ( 0.4690749385695646145, 0.8831583674551010121, 0.000000000000000000 ) ) ;
#21974=ORIENTED_EDGE ( 'NONE', *, *, #26010, .T. ) ;
#21975=CARTESIAN_POINT ( 'NONE',  ( 80.48490785079538057, 62.58389448792956955, -3.438247877890626469 ) ) ;
#21977=CARTESIAN_POINT ( 'NONE',  ( 78.79145472225366120, 65.75511795602321286, 2.294512580621463016 ) ) ;
#21995=CARTESIAN_POINT ( 'NONE',  ( 81.46310422711934507, 61.87916883045102878, 2.296576099417781958 ) ) ;
#21997=CYLINDRICAL_SURFACE ( 'NONE', #35190, 1.000000000000003997 ) ;
#22021=DIRECTION ( 'NONE',  ( 0.000000000000000000, 0.000000000000000000, 1.000000000000000000 ) ) ;
#22024=CARTESIAN_POINT ( 'NONE',  ( 79.62856576210180037, 64.96968976106111882, -3.364061116559609932 ) ) ;
#22029=CARTESIAN_POINT ( 'NONE',  ( 81.39647959751735584, 65.22731470771807949, -2.622983904469595284 ) ) ;
#22035=CARTESIAN_POINT ( 'NONE',  ( 73.28665133690081745, 61.87344754340890773, 3.624554307483654814 ) ) ;
#22044=CARTESIAN_POINT ( 'NONE',  ( 80.87888400807986500, 65.31646575666034948, 2.869341960395464408 ) ) ;
#22047=ORIENTED_EDGE ( 'NONE', *, *, #24072, .F. ) ;
#22066=CARTESIAN_POINT ( 'NONE',  ( 66.57766344320866381, 57.81227849924184881, -3.999802976169922974 ) ) ;
#22076=ORIENTED_EDGE ( 'NONE', *, *, #22140, .T. ) ;
#22079=CARTESIAN_POINT ( 'NONE',  ( 82.36730661685049881, 64.56044919582427610, -1.633153239555407144 ) ) ;
#22080=CARTESIAN_POINT ( 'NONE',  ( 81.14259283377289478, 61.75830469257449096, 2.468641556982001273 ) ) ;
#22082=ORIENTED_EDGE ( 'NONE', *, *, #24418, .F. ) ;
#22083=CARTESIAN_POINT ( 'NONE',  ( 77.66280895473879298, 61.33468559051797087, -3.643081266330417289 ) ) ;
#22087=CARTESIAN_POINT ( 'NONE',  ( 80.79744990009727701, 64.13345242326634832, -3.486376426170565423 ) ) ;
#22088=CARTESIAN_POINT ( 'NONE',  ( 78.44508438210816337, 62.63916802445883292, 3.816136337383057686 ) ) ;
#22092=CARTESIAN_POINT ( 'NONE',  ( 82.35726419014409316, 62.82676667106981938, 1.646077502935599401 ) ) ;
#22098=CARTESIAN_POINT ( 'NONE',  ( -63.39880662924651489, 35.63549842397610945, 6.795986594147001014 ) ) ;
#22104=DIRECTION ( 'NONE',  ( 0.8831583674551003460, -0.4690749385695657803, 0.000000000000000000 ) ) ;
#22107=CARTESIAN_POINT ( 'NONE',  ( 27.60344192425479193, 81.15229837709949834, -1.000000000000000000 ) ) ;
#22120=CARTESIAN_POINT ( 'NONE',  ( 68.64726599134355922, 58.50818873767699557, -3.992679187475168145 ) ) ;
#22133=CARTESIAN_POINT ( 'NONE',  ( 79.88615925706736220, 62.68050235454665398, -3.612066323963901482 ) ) ;
#22139=CARTESIAN_POINT ( 'NONE',  ( 78.68583465488313777, 66.05536144407732024, -1.071687152255760944 ) ) ;
#22140=EDGE_CURVE ( 'NONE', #38621, #10601, #35433, .T. ) ;
#22141=CARTESIAN_POINT ( 'NONE',  ( 80.66846628934483476, 61.48471191768543775, 2.456741006817842354 ) ) ;
#22156=DIRECTION ( 'NONE',  ( 1.000000000000000000, 0.000000000000000000, 0.000000000000000000 ) ) ;
#22157=CARTESIAN_POINT ( 'NONE',  ( 79.89212576172680258, 63.66154800590238949, 1.000000000000000000 ) ) ;
#22169=CARTESIAN_POINT ( 'NONE',  ( 67.11291460916432072, 58.16531518584054794, 3.996350724342222716 ) ) ;
#22171=CIRCLE ( 'NONE', #5071, 3.000000000000003109 ) ;
#22185=CARTESIAN_POINT ( 'NONE',  ( 79.10075812992880628, 65.22691190166780473, -3.061371641637540719 ) ) ;
#22186=DIRECTION ( 'NONE',  ( 0.4690749385695657803, 0.8831583674551003460, 0.000000000000000000 ) ) ;
#22187=CARTESIAN_POINT ( 'NONE',  ( 79.88758398535436811, 64.02175723273455787, 3.702313260098205827 ) ) ;
#22191=AXIS2_PLACEMENT_3D ( 'NONE', #19350, #3334, #12755 ) ;
#22196=EDGE_CURVE ( 'NONE', #35702, #16830, #40167, .T. ) ;
#22203=EDGE_CURVE ( 'NONE', #12529, #30676, #2400, .T. ) ;
#22208=CARTESIAN_POINT ( 'NONE',  ( 80.90189697519826950, 63.80306449575954986, 3.509897338574981429 ) ) ;
#22222=CARTESIAN_POINT ( 'NONE',  ( 81.15583125883576088, 62.51952284974313301, -3.108243619504619915 ) ) ;
#22235=CARTESIAN_POINT ( 'NONE',  ( 78.99368969759478887, 65.72941799158938636, -2.506402126386322760 ) ) ;
#22250=CARTESIAN_POINT ( 'NONE',  ( 70.63497465855112978, 60.23961165191135336, 3.862811858476220550 ) ) ;
#22258=CARTESIAN_POINT ( 'NONE',  ( 78.89436432227896034, 66.15509128278824846, 1.313329331391815513 ) ) ;
#22268=DIRECTION ( 'NONE',  ( -0.000000000000000000, -0.000000000000000000, -1.000000000000000000 ) ) ;
#22275=CARTESIAN_POINT ( 'NONE',  ( 66.42000668879835246, 57.79655248154868730, -4.000000000000018652 ) ) ;
#22286=CARTESIAN_POINT ( 'NONE',  ( 82.16824647341034904, 62.22308028923542622, -1.246975333547555742 ) ) ;
#22288=CARTESIAN_POINT ( 'NONE',  ( 81.13710691025121946, 61.43629694585948187, 1.911132874451712205 ) ) ;
#22290=CARTESIAN_POINT ( 'NONE',  ( 76.54556538389314824, 62.22002718612351657, -3.872369636030850160 ) ) ;
#22294=CARTESIAN_POINT ( 'NONE',  ( 81.03825699591064335, 63.48946937969521542, -3.448515284080294840 ) ) ;
#22295=CARTESIAN_POINT ( 'NONE',  ( 77.10371989074782562, 62.50202019409571363, 3.856837490694489556 ) ) ;
#22297=ADVANCED_FACE ( 'NONE', ( #31129 ), #24950, .T. ) ;
#22302=DIRECTION ( 'NONE',  ( 0.000000000000000000, 0.000000000000000000, -1.000000000000000000 ) ) ;
#22303=CARTESIAN_POINT ( 'NONE',  ( 78.68971998042104588, 66.05812159354533719, 1.027726681410877863 ) ) ;
#22309=CARTESIAN_POINT ( 'NONE',  ( -62.81463675898083210, 36.67811266762163314, 4.600311178732271244 ) ) ;
#22313=CYLINDRICAL_SURFACE ( 'NONE', #30863, 3.000000000000000444 ) ;
#22317=CARTESIAN_POINT ( 'NONE',  ( -63.05049812975200041, 38.43447230638179235, 4.010972415401512059 ) ) ;
#22327=CARTESIAN_POINT ( 'NONE',  ( 68.13924211849639789, 58.08649371134929140, -3.978477839347963840 ) ) ;
#22339=CARTESIAN_POINT ( 'NONE',  ( 78.73750597996149736, 66.05139304066524630, 1.520709669156477428 ) ) ;
#22343=CARTESIAN_POINT ( 'NONE',  ( 80.30053069885687478, 62.24503436470105555, -3.340572457511948201 ) ) ;
#22346=CARTESIAN_POINT ( 'NONE',  ( 79.50049935622257635, 66.06919348782189161, -2.170472567296708011 ) ) ;
#22347=CARTESIAN_POINT ( 'NONE',  ( 78.44523713320049296, 65.65863411530537519, 2.218931858625904585 ) ) ;
#22351=CARTESIAN_POINT ( 'NONE',  ( 81.16957891225079891, 61.30398062001319914, 1.000000000000000000 ) ) ;
#22352=CARTESIAN_POINT ( 'NONE',  ( -64.08758708074093136, 41.34485010641581937, 2.999999996672334746 ) ) ;
#22374=CARTESIAN_POINT ( 'NONE',  ( 66.72049918463439155, 57.87600310258397940, 3.999713739232678034 ) ) ;
#22389=CARTESIAN_POINT ( 'NONE',  ( 79.85475324883658743, 64.00275885990843960, -3.706996517075250352 ) ) ;
#22391=CARTESIAN_POINT ( 'NONE',  ( 78.55684871931622126, 65.96378271911972035, 1.386845825021860490 ) ) ;
#22405=DIRECTION ( 'NONE',  ( -0.000000000000000000, -0.000000000000000000, -1.000000000000000000 ) ) ;
#22406=CARTESIAN_POINT ( 'NONE',  ( 81.31240362382359876, 61.49079461182719797, 1.766895996212472175 ) ) ;
#22421=CARTESIAN_POINT ( 'NONE',  ( 81.26478070948648735, 61.47323240028521241, -1.804401104814721712 ) ) ;
#22433=CARTESIAN_POINT ( 'NONE',  ( 81.10356443252386782, 61.32192396066504614, -1.621665796799206305 ) ) ;
#22437=CARTESIAN_POINT ( 'NONE',  ( 81.16729622508351838, 61.30314466175458676, -1.045986116561645529 ) ) ;
#22442=CARTESIAN_POINT ( 'NONE',  ( -57.80362650821757597, 30.11637991209972753, -4.211916349762224954 ) ) ;
#22446=CARTESIAN_POINT ( 'NONE',  ( 71.00148000485552302, 59.33579794997937995, 3.971832046809253391 ) ) ;
#22448=ORIENTED_EDGE ( 'NONE', *, *, #17927, .F. ) ;
#22453=CARTESIAN_POINT ( 'NONE',  ( 66.27376694608931018, 57.73522568913554665, 4.000000000000000000 ) ) ;
#22454=CARTESIAN_POINT ( 'NONE',  ( 81.29034902430632314, 64.00233822785270377, 3.292658836682930357 ) ) ;
#22468=AXIS2_PLACEMENT_3D ( 'NONE', #4577, #28878, #36072 ) ;
#22475=CARTESIAN_POINT ( 'NONE',  ( 66.41604928081308401, 57.80773248233377615, -4.000000000000022204 ) ) ;
#22482=DIRECTION ( 'NONE',  ( 0.4582725098355734938, -0.8888117386314180468, 0.000000000000000000 ) ) ;
#22490=CARTESIAN_POINT ( 'NONE',  ( 81.56437483599468408, 65.67932636690369463, -1.586031901070164674 ) ) ;
#22491=CARTESIAN_POINT ( 'NONE',  ( 78.61080321328475407, 66.00207709680661594, 1.298998371267750640 ) ) ;
#22494=VERTEX_POINT ( 'NONE', #39507 ) ;
#22495=CARTESIAN_POINT ( 'NONE',  ( 74.78802096516436393, 63.01683072882820369, -3.322260703561485062 ) ) ;
#22496=DIRECTION ( 'NONE',  ( -0.000000000000000000, -0.000000000000000000, -1.000000000000000000 ) ) ;
#22499=CARTESIAN_POINT ( 'NONE',  ( 81.25681022244550888, 61.36874951788873034, -1.439474762807439134 ) ) ;
#22500=CARTESIAN_POINT ( 'NONE',  ( 76.91271350297705567, 62.89131350122330133, 3.776276000685970136 ) ) ;
#22506=CARTESIAN_POINT ( 'NONE',  ( 79.23414132050105252, 66.25012704882071546, 1.421876342974069507 ) ) ;
#22527=CARTESIAN_POINT ( 'NONE',  ( 67.94738262351316394, 58.59965392607728063, -3.985705108533788898 ) ) ;
#22531=EDGE_CURVE ( 'NONE', #3507, #12043, #8705, .T. ) ;
#22540=CARTESIAN_POINT ( 'NONE',  ( 78.85897125043999267, 66.02047811250265852, 1.830101370957687879 ) ) ;
#22541=ADVANCED_BREP_SHAPE_REPRESENTATION ( '', ( #39670, #30744 ), #18224 ) ;
#22542=CARTESIAN_POINT ( 'NONE',  ( -59.93345510331042902, 24.73247967741478703, 12.49999999999999645 ) ) ;
#22544=CARTESIAN_POINT ( 'NONE',  ( 78.53692321045886615, 63.86140601108343873, -3.670385203786640904 ) ) ;
#22547=CARTESIAN_POINT ( 'NONE',  ( 81.57279438772125957, 63.75980975930797712, -3.125232205748940117 ) ) ;
#22548=CARTESIAN_POINT ( 'NONE',  ( 80.21769632236900804, 61.97993766192919907, 3.195657361810719799 ) ) ;
#22550=CARTESIAN_POINT ( 'NONE',  ( 80.71704827558885142, 66.21292280724348700, 1.000000000000000000 ) ) ;
#22554=ORIENTED_EDGE ( 'NONE', *, *, #16875, .T. ) ;
#22558=DIRECTION ( 'NONE',  ( -0.000000000000000000, 1.000000000000000000, 0.000000000000000000 ) ) ;
#22572=CARTESIAN_POINT ( 'NONE',  ( 66.84954949145740954, 57.97782447864501165, 3.999382933223862846 ) ) ;
#22577=EDGE_CURVE ( 'NONE', #5492, #11497, #6261, .T. ) ;
#22580=AXIS2_PLACEMENT_3D ( 'NONE', #13509, #23185, #22593 ) ;
#22587=CARTESIAN_POINT ( 'NONE',  ( 80.41811942164733296, 62.87504864752338563, -3.537885823842629396 ) ) ;
#22589=CARTESIAN_POINT ( 'NONE',  ( 80.11945187304060312, 63.42025125984827838, 3.710743084827279326 ) ) ;
#22593=DIRECTION ( 'NONE',  ( 1.000000000000000000, 0.000000000000000000, -0.000000000000000000 ) ) ;
#22604=CARTESIAN_POINT ( 'NONE',  ( -73.45070404594234503, 38.65432087843067421, -8.800414904976364028 ) ) ;
#22606=CARTESIAN_POINT ( 'NONE',  ( 80.49267809498162762, 64.35807816991642483, 3.549391953833850977 ) ) ;
#22608=DIRECTION ( 'NONE',  ( 0.000000000000000000, 0.000000000000000000, 1.000000000000000000 ) ) ;
#22618=CARTESIAN_POINT ( 'NONE',  ( 68.71160781503239434, 58.33825098880495119, 3.980709302925375503 ) ) ;
#22620=CARTESIAN_POINT ( 'NONE',  ( 73.64144479846403613, 59.51803038729781292, -3.736020861036525531 ) ) ;
#22621=CARTESIAN_POINT ( 'NONE',  ( -64.08758708074093136, 42.07456177364299066, -2.837280265527672540 ) ) ;
#22625=CARTESIAN_POINT ( 'NONE',  ( 80.95462345035979013, 63.09697225074528859, -3.406228740995798532 ) ) ;
#22629=ORIENTED_EDGE ( 'NONE', *, *, #8162, .F. ) ;
#22630=CARTESIAN_POINT ( 'NONE',  ( 10.50357756723356140, 59.39757829809867928, 1.000000000000000000 ) ) ;
#22636=CARTESIAN_POINT ( 'NONE',  ( 79.46693819636867318, 65.20858797830474884, -3.188730975143405200 ) ) ;
#22639=ORIENTED_EDGE ( 'NONE', *, *, #31118, .F. ) ;
#22647=CARTESIAN_POINT ( 'NONE',  ( -63.66761068000498369, 44.17545465894031764, -2.094006737888894687 ) ) ;
#22648=CARTESIAN_POINT ( 'NONE',  ( 72.54144496250529528, 58.88102433069186503, 3.699617110138615939 ) ) ;
#22652=ORIENTED_EDGE ( 'NONE', *, *, #26785, .T. ) ;
#22656=CARTESIAN_POINT ( 'NONE',  ( 80.85068185324867329, 64.93836743322185612, 3.187395722566882750 ) ) ;
#22672=TOROIDAL_SURFACE ( 'NONE', #28567, 31.02204673211315011, 3.000000000000000000 ) ;
#22677=ORIENTED_EDGE ( 'NONE', *, *, #23300, .F. ) ;
#22680=CARTESIAN_POINT ( 'NONE',  ( 66.42891085676521357, 57.77139747978225870, -4.000000000000010658 ) ) ;
#22688=CARTESIAN_POINT ( 'NONE',  ( 80.93658766080253031, 66.04709959793316898, -1.728104186158372579 ) ) ;
#22693=CARTESIAN_POINT ( 'NONE',  ( 76.15169681074901575, 61.58848496619829405, -3.887901781369006660 ) ) ;
#22698=CARTESIAN_POINT ( 'NONE',  ( 77.42503339237353543, 60.33561942134746658, 3.121245467013677111 ) ) ;
#22703=CARTESIAN_POINT ( 'NONE',  ( 82.22574661183178080, 63.03983423078060611, 2.217414436011084788 ) ) ;
#22724=ORIENTED_EDGE ( 'NONE', *, *, #33345, .T. ) ;
#22726=CARTESIAN_POINT ( 'NONE',  ( 68.50220056233268906, 58.89075781393282227, -3.976359261632471220 ) ) ;
#22740=CARTESIAN_POINT ( 'NONE',  ( 80.34143827441934604, 64.27643806731579446, 3.602832836245130288 ) ) ;
#22743=CARTESIAN_POINT ( 'NONE',  ( 78.08876170118931270, 64.69829802809502439, -3.164065397988976791 ) ) ;
#22746=CARTESIAN_POINT ( 'NONE',  ( 81.55127126996082154, 61.75833066297040119, -1.907437723456241185 ) ) ;
#22747=CARTESIAN_POINT ( 'NONE',  ( 79.34756916856697728, 63.37933396398980079, 3.765547211956733697 ) ) ;
#22752=CARTESIAN_POINT ( 'NONE',  ( 79.68325118717130806, 66.33239387230221951, 1.129532193886028102 ) ) ;
#22755=CARTESIAN_POINT ( 'NONE',  ( -62.96789184024967057, 35.54107112332027896, -6.131023528871231143 ) ) ;
#22776=CARTESIAN_POINT ( 'NONE',  ( 66.56983546066652480, 57.83423415266778278, 3.999917672784519596 ) ) ;
#22788=CARTESIAN_POINT ( 'NONE',  ( 78.66571724150243483, 65.64011997358944939, -2.392122129321805790 ) ) ;
#22789=CARTESIAN_POINT ( 'NONE',  ( 80.38728350982691495, 62.86383526565676760, 3.543129918318839611 ) ) ;
#22808=CARTESIAN_POINT ( 'NONE',  ( 80.74417485493698621, 64.10566034184276418, 3.509897338574980985 ) ) ;
#22810=CARTESIAN_POINT ( 'NONE',  ( -43.84925787048184986, -39.21126558444150589, -9.800414904976365804 ) ) ;
#22814=CARTESIAN_POINT ( 'NONE',  ( -65.04873975080082005, 34.92043383559660441, 6.752938550805159146 ) ) ;
#22819=CARTESIAN_POINT ( 'NONE',  ( 68.95366548541680629, 59.44408286695458798, 3.907754234428187257 ) ) ;
#22824=CARTESIAN_POINT ( 'NONE',  ( 78.75316082766835279, 66.06368344870412557, -1.496866203714572574 ) ) ;
#22830=ORIENTED_EDGE ( 'NONE', *, *, #40516, .F. ) ;
#22832=CARTESIAN_POINT ( 'NONE',  ( 80.59816347408047932, 62.94305116675459288, -3.503057693382716664 ) ) ;
#22833=AXIS2_PLACEMENT_3D ( 'NONE', #28997, #800, #13332 ) ;
#22835=VECTOR ( 'NONE', #9358, 1000.000000000000000 ) ;
#22837=VERTEX_POINT ( 'NONE', #4057 ) ;
#22839=CARTESIAN_POINT ( 'NONE',  ( 78.68849923766543952, 66.05725436416432217, -1.045986116561646639 ) ) ;
#22843=CARTESIAN_POINT ( 'NONE',  ( -64.08758708074093136, 43.61223004741319897, -0.9999999999999937828 ) ) ;
#22844=CARTESIAN_POINT ( 'NONE',  ( 69.75093826875801994, 59.10798165618643907, 3.985452289341158139 ) ) ;
#22853=CARTESIAN_POINT ( 'NONE',  ( 81.46069228692957154, 61.55470069442174719, 1.644402879622030911 ) ) ;
#22870=ORIENTED_EDGE ( 'NONE', *, *, #21355, .F. ) ;
#22884=CARTESIAN_POINT ( 'NONE',  ( 78.98807859296742606, 66.20728402696080650, -1.114595100209339495 ) ) ;
#22889=CARTESIAN_POINT ( 'NONE',  ( 75.05654786057638717, 62.45444674818786268, -3.685888554891597835 ) ) ;
#22892=CARTESIAN_POINT ( 'NONE',  ( 76.81831744871803380, 63.08285468194208079, 3.722835383484662142 ) ) ;
#22900=CARTESIAN_POINT ( 'NONE',  ( 81.16877391194421421, 61.30368580354083008, 1.027726681410876308 ) ) ;
#22915=CARTESIAN_POINT ( 'NONE',  ( -63.06901714727352015, 38.60153782280345780, -4.000000000000000888 ) ) ;
#22920=CARTESIAN_POINT ( 'NONE',  ( 67.93540907064681278, 58.63163702635943508, -3.982418445723137967 ) ) ;
#22923=ORIENTED_EDGE ( 'NONE', *, *, #8590, .F. ) ;
#22930=EDGE_CURVE ( 'NONE', #7709, #26563, #29271, .T. ) ;
#22935=EDGE_CURVE ( 'NONE', #20708, #38802, #38200, .T. ) ;
#22937=CARTESIAN_POINT ( 'NONE',  ( 82.18775271763095702, 62.23297483488567394, -1.000000000000000000 ) ) ;
#22939=CARTESIAN_POINT ( 'NONE',  ( 81.14234681338471944, 61.29401378075402818, 1.159471704397071035 ) ) ;
#22943=CARTESIAN_POINT ( 'NONE',  ( 77.75442706423145012, 65.27774734742538953, -2.313798345564205494 ) ) ;
#22946=CARTESIAN_POINT ( 'NONE',  ( 78.68499968550160872, 66.05476829360677016, -1.077711394953983604 ) ) ;
#22947=CARTESIAN_POINT ( 'NONE',  ( 78.00211021922338261, 65.46497694724934036, 2.177161688561012998 ) ) ;
#22950=CARTESIAN_POINT ( 'NONE',  ( 81.16955088369260807, 61.30397035488353197, 1.005837412005772258 ) ) ;
#22967=CYLINDRICAL_SURFACE ( 'NONE', #5929, 5.000000000000000000 ) ;
#22973=( BOUNDED_SURFACE ( )  B_SPLINE_SURFACE ( 3, 2, ( 
 ( #25049, #13696, #1362 ),
 ( #4050, #3649, #38596 ),
 ( #32441, #28945, #35143 ),
 ( #748, #4239, #38989 ) ),
 .UNSPECIFIED., .F., .F., .F. ) 
 B_SPLINE_SURFACE_WITH_KNOTS ( ( 4, 4 ),
 ( 3, 3 ),
 ( 4.564251139902668619, 4.712388980384689674 ),
 ( 0.000000000000000000, 1.000000000000000000 ),
 .UNSPECIFIED. ) 
 GEOMETRIC_REPRESENTATION_ITEM ( )  RATIONAL_B_SPLINE_SURFACE ( (
 ( 1.000000000000000000, 0.6872206705710377506, 1.000000000000000000),
 ( 1.000000000000000000, 0.6938961412926133443, 1.000000000000000000),
 ( 1.000000000000000000, 0.7005474459265356169, 1.000000000000000000),
 ( 1.000000000000000000, 0.7071067811865475727, 1.000000000000000000) ) ) 
 REPRESENTATION_ITEM ( '' )  SURFACE ( )  );
#22975=CARTESIAN_POINT ( 'NONE',  ( 66.55809347730310321, 57.86716763633229021, 3.999802976172706082 ) ) ;
#22983=CARTESIAN_POINT ( 'NONE',  ( -66.99872204295122913, 28.48507918597134037, -6.999999999999999112 ) ) ;
#22984=AXIS2_PLACEMENT_3D ( 'NONE', #2242, #9405, #18469 ) ;
#22985=VERTEX_POINT ( 'NONE', #39833 ) ;
#22988=CARTESIAN_POINT ( 'NONE',  ( 79.26327435592848758, 64.69753611046425590, -3.458772244351173697 ) ) ;
#22990=CARTESIAN_POINT ( 'NONE',  ( 79.16440527908353886, 64.96746831917783993, 3.289664858626308419 ) ) ;
#23000=CARTESIAN_POINT ( 'NONE',  ( 74.91297039797925095, 63.41901279415932891, -3.016929835169668728 ) ) ;
#23006=CARTESIAN_POINT ( 'NONE',  ( 81.32112198246272783, 62.31825444738112907, 2.836177733672701429 ) ) ;
#23011=AXIS2_PLACEMENT_3D ( 'NONE', #32065, #3666, #13715 ) ;
#23019=CARTESIAN_POINT ( 'NONE',  ( -64.08758708074093136, 41.64075302391485423, -2.960467334047197419 ) ) ;
#23023=CARTESIAN_POINT ( 'NONE',  ( 79.78769048662040575, 65.07306089581300057, -3.312281065658527091 ) ) ;
#23034=CARTESIAN_POINT ( 'NONE',  ( 78.60310727342863402, 65.99661392892440404, -1.312782405654899121 ) ) ;
#23040=DIRECTION ( 'NONE',  ( -0.000000000000000000, -0.000000000000000000, -1.000000000000000000 ) ) ;
#23041=CARTESIAN_POINT ( 'NONE',  ( -59.01947560891952804, 27.90920910948504385, -6.147301388271595890 ) ) ;
#23045=CARTESIAN_POINT ( 'NONE',  ( 70.53871541878200446, 60.47550293342311534, 3.775670717450619218 ) ) ;
#23047=VERTEX_POINT ( 'NONE', #8522 ) ;
#23055=CARTESIAN_POINT ( 'NONE',  ( 81.31796987085604655, 61.39415816021645611, 1.370814772368732948 ) ) ;
#23070=ORIENTED_EDGE ( 'NONE', *, *, #11131, .F. ) ;
#23081=CARTESIAN_POINT ( 'NONE',  ( -64.08758708074093136, 36.14363715547680300, -3.800414904976364028 ) ) ;
#23083=CARTESIAN_POINT ( 'NONE',  ( -55.42153689335680156, 31.50958069423707641, -3.999999999999998224 ) ) ;
#23087=CARTESIAN_POINT ( 'NONE',  ( 82.17153865661288137, 64.85009419791096263, -1.775718711110015224 ) ) ;
#23090=CARTESIAN_POINT ( 'NONE',  ( 75.52602547247359155, 59.92744485144773847, -3.494507759123859802 ) ) ;
#23094=CARTESIAN_POINT ( 'NONE',  ( 76.36824339142353324, 62.58715529212010864, 3.801074476319127093 ) ) ;
#23100=CARTESIAN_POINT ( 'NONE',  ( 79.49585004866924010, 66.23094581382579804, 1.662695954554603617 ) ) ;
#23107=CARTESIAN_POINT ( 'NONE',  ( 68.91489483114931147, 58.10232893654896458, 3.936674041830252158 ) ) ;
#23118=CARTESIAN_POINT ( 'NONE',  ( 67.66997365410338716, 58.45410198214950981, -3.990378031984448182 ) ) ;
#23119=B_SPLINE_CURVE_WITH_KNOTS ( 'NONE', 3,
 ( #2721, #27117, #5500, #17420 ),
 .UNSPECIFIED., .F., .F.,
 ( 4, 4 ),
 ( 0.0008960438496711642777, 0.001150058339056989976 ),
 .UNSPECIFIED. ) ;
#23124=ADVANCED_FACE ( 'NONE', ( #5045 ), #16128, .T. ) ;
#23126=CARTESIAN_POINT ( 'NONE',  ( -61.00670947824507806, 24.84364830758654108, -8.800414904976364028 ) ) ;
#23132=CARTESIAN_POINT ( 'NONE',  ( 78.87101214850905251, 66.02979514927503146, 1.817988788077138596 ) ) ;
#23134=CARTESIAN_POINT ( 'NONE',  ( -63.54361195871889834, 43.49475130726206373, 3.057987111335950026 ) ) ;
#23135=ORIENTED_EDGE ( 'NONE', *, *, #23966, .F. ) ;
#23136=CARTESIAN_POINT ( 'NONE',  ( 79.79883522896109582, 62.08831372790998415, -3.424416364708440685 ) ) ;
#23139=CARTESIAN_POINT ( 'NONE',  ( 81.56578493135152996, 62.15373153752272373, -2.499697124808072157 ) ) ;
#23140=CARTESIAN_POINT ( 'NONE',  ( 80.15150095960399312, 61.72183351646653904, 3.055712048904937195 ) ) ;
#23143=CARTESIAN_POINT ( 'NONE',  ( 82.49284700683531923, 64.23424719397920057, 1.468380750527791268 ) ) ;
#23147=CYLINDRICAL_SURFACE ( 'NONE', #33828, 0.9999999999999998890 ) ;
#23165=VERTEX_POINT ( 'NONE', #14696 ) ;
#23166=CARTESIAN_POINT ( 'NONE',  ( 66.88492799900151908, 57.87961537897388808, 3.998747512900713730 ) ) ;
#23178=CARTESIAN_POINT ( 'NONE',  ( 79.16440527908333991, 64.96746831917748466, -3.289664858626429211 ) ) ;
#23180=CARTESIAN_POINT ( 'NONE',  ( 79.23217405491450904, 65.02354781853230747, 3.268578535636609494 ) ) ;
#23181=FACE_OUTER_BOUND ( 'NONE', #29851, .T. ) ;
#23185=DIRECTION ( 'NONE',  ( 0.000000000000000000, 0.000000000000000000, 1.000000000000000000 ) ) ;
#23190=CARTESIAN_POINT ( 'NONE',  ( 77.23450810825278268, 65.03073311407490564, -2.276535451367163621 ) ) ;
#23197=CARTESIAN_POINT ( 'NONE',  ( 80.91044703854151976, 63.42644682079063045, 3.500437194783534434 ) ) ;
#23212=CARTESIAN_POINT ( 'NONE',  ( 68.47014483779531702, 58.97518246833449496, 3.964410623303925796 ) ) ;
#23217=CARTESIAN_POINT ( 'NONE',  ( 79.24015747652954644, 65.65980919716059816, -2.710038060602469656 ) ) ;
#23220=VECTOR ( 'NONE', #26337, 1000.000000000000000 ) ;
#23221=CARTESIAN_POINT ( 'NONE',  ( -58.44033895488189501, 28.22358054771055436, 5.330345403092622725 ) ) ;
#23222=ORIENTED_EDGE ( 'NONE', *, *, #21156, .F. ) ;
#23229=CARTESIAN_POINT ( 'NONE',  ( 80.25680044982675554, 63.48435701671603937, -3.692178340560190009 ) ) ;
#23231=CARTESIAN_POINT ( 'NONE',  ( 80.53350286136132752, 63.24990014040474051, 3.607546830629784207 ) ) ;
#23239=CARTESIAN_POINT ( 'NONE',  ( -64.08758708074093136, 43.59023631735133364, -1.301703137985040781 ) ) ;
#23245=VECTOR ( 'NONE', #8307, 1000.000000000000000 ) ;
#23251=CARTESIAN_POINT ( 'NONE',  ( 78.84958593098259882, 66.12877247161574701, 1.370814772368738055 ) ) ;
#23273=CARTESIAN_POINT ( 'NONE',  ( 66.27376694609004915, 57.73522568913436004, -4.000000000000000000 ) ) ;
#23277=CARTESIAN_POINT ( 'NONE',  ( -64.08758708074094557, 37.77509509994405335, -3.093168342233789225 ) ) ;
#23281=CARTESIAN_POINT ( 'NONE',  ( 81.27149311957269617, 65.88890312491017198, -1.680016503630878066 ) ) ;
#23287=CARTESIAN_POINT ( 'NONE',  ( 74.78802096516436393, 63.01683072882818948, 3.322260703561484618 ) ) ;
#23291=VECTOR ( 'NONE', #39725, 1000.000000000000000 ) ;
#23295=CARTESIAN_POINT ( 'NONE',  ( 78.68916368339945677, 66.05772639262711721, 1.037317649801914321 ) ) ;
#23300=EDGE_CURVE ( 'NONE', #26757, #28218, #8789, .T. ) ;
#23304=FACE_OUTER_BOUND ( 'NONE', #21669, .T. ) ;
#23306=EDGE_CURVE ( 'NONE', #15332, #30342, #32768, .T. ) ;
#23316=CARTESIAN_POINT ( 'NONE',  ( 67.51064039993573829, 57.98508837280776618, -3.992553130659727945 ) ) ;
#23326=DIRECTION ( 'NONE',  ( -0.8888117386314211554, -0.4582725098355677762, 0.000000000000000000 ) ) ;
#23330=CARTESIAN_POINT ( 'NONE',  ( 81.20006484400859392, 61.61449114502521240, 2.147349935851011526 ) ) ;
#23333=CARTESIAN_POINT ( 'NONE',  ( 79.89463791284350691, 61.88150425735624083, -3.258123098320698130 ) ) ;
#23336=CARTESIAN_POINT ( 'NONE',  ( 79.46506916755670602, 66.04886526173737593, -2.198649373785575456 ) ) ;
#23337=CARTESIAN_POINT ( 'NONE',  ( 80.12095330986325337, 62.19218463582610212, 3.375657603866087264 ) ) ;
#23340=CARTESIAN_POINT ( 'NONE',  ( 81.01700449632699019, 66.08979032036411638, 1.386429027373558664 ) ) ;
#23344=VERTEX_POINT ( 'NONE', #668 ) ;
#23364=CARTESIAN_POINT ( 'NONE',  ( 66.42198539279090141, 57.79096248115626366, 4.000000000000014211 ) ) ;
#23365=CARTESIAN_POINT ( 'NONE',  ( 73.33417617461327609, 60.23131181272744072, -3.934110468510652492 ) ) ;
#23377=CARTESIAN_POINT ( 'NONE',  ( 80.84620594802093763, 61.52815374075456845, -2.368006059521087447 ) ) ;
#23379=CARTESIAN_POINT ( 'NONE',  ( 79.67348887277971414, 64.26584687736657031, 3.653685850874071939 ) ) ;
#23383=PLANE ( 'NONE',  #22580 ) ;
#23385=DIRECTION ( 'NONE',  ( 0.4690749385695426321, 0.8831583674551126695, 2.183007799372904676E-14 ) ) ;
#23390=B_SPLINE_CURVE_WITH_KNOTS ( 'NONE', 3,
 ( #38076, #21629, #18943, #12754, #25332, #15234, #31509, #18313, #9052, #6600, #28406, #40342, #37654, #18728, #5979, #214, #12552, #34824 ),
 .UNSPECIFIED., .F., .F.,
 ( 4, 2, 2, 2, 2, 2, 2, 2, 4 ),
 ( 0.000000000000000000, 0.0007758045964606555527, 0.001551609192921311105, 0.003103218385842596624, 0.003879022982303238515, 0.004654827578763879106, 0.005430632175224520131, 0.005818534473454842378, 0.006206436771685162890 ),
 .UNSPECIFIED. ) ;
#23394=ADVANCED_FACE ( 'NONE', ( #870, #13403 ), #25977, .T. ) ;
#23395=CARTESIAN_POINT ( 'NONE',  ( 28.61591789821288145, 47.14532032487838364, -1.000000000000000000 ) ) ;
#23397=CARTESIAN_POINT ( 'NONE',  ( 81.32777602152022212, 61.82240453612693187, 2.372413575842097444 ) ) ;
#23398=LINE ( 'NONE', #1999, #21598 ) ;
#23404=CARTESIAN_POINT ( 'NONE',  ( -64.09292236773265472, 35.65892419719516226, 4.099996682510911761 ) ) ;
#23408=CARTESIAN_POINT ( 'NONE',  ( 68.56660431458814742, 58.72100381882076192, 3.990501929453217134 ) ) ;
#23410=CIRCLE ( 'NONE', #26705, 1.000000000000000888 ) ;
#23415=CARTESIAN_POINT ( 'NONE',  ( 78.66037426029973290, 66.03727662354840788, -1.183438861787455165 ) ) ;
#23424=CARTESIAN_POINT ( 'NONE',  ( 81.06392658325405876, 61.26538850743065012, -1.312782405654895568 ) ) ;
#23428=CARTESIAN_POINT ( 'NONE',  ( 78.86912799350189118, 65.82616116372959425, 2.227525437860354174 ) ) ;
#23434=( BOUNDED_SURFACE ( )  B_SPLINE_SURFACE ( 3, 2, ( 
 ( #35915, #1734, #13874 ),
 ( #26836, #29917, #1338 ),
 ( #23549, #32420, #39173 ),
 ( #29526, #29718, #929 ),
 ( #36114, #16948, #4219 ),
 ( #26245, #38968, #13463 ),
 ( #4811, #14265, #16740 ),
 ( #39376, #35323, #26441 ),
 ( #7891, #13675, #38777 ),
 ( #22755, #4424, #10767 ),
 ( #17339, #7091, #29324 ),
 ( #1141, #7490, #7694 ),
 ( #38571, #20243, #32825 ),
 ( #26037, #19655, #1527 ),
 ( #32227, #20443, #4616 ),
 ( #14062, #4027, #26639 ) ),
 .UNSPECIFIED., .F., .F., .T. ) 
 B_SPLINE_SURFACE_WITH_KNOTS ( ( 4, 2, 2, 2, 2, 2, 2, 4 ),
 ( 3, 3 ),
 ( 7.372574772901430151E-18, 0.0009755768803159638137, 0.001463365320473941980, 0.001951153760631920255, 0.002438942200789898530, 0.002926730640947876588, 0.003414519081105855079, 0.003902307521263833137 ),
 ( 0.000000000000000000, 1.000000000000000000 ),
 .UNSPECIFIED. ) 
 GEOMETRIC_REPRESENTATION_ITEM ( )  RATIONAL_B_SPLINE_SURFACE ( (
 ( 1.000000000000000000, 0.6029302108204159794, 1.000000000000000000),
 ( 1.000000000000000000, 0.5783298881758098808, 1.000000000000000000),
 ( 1.000000000000000000, 0.5522465926627553312, 1.000000000000000000),
 ( 1.000000000000000000, 0.5169885426014493301, 1.000000000000000000),
 ( 1.000000000000000000, 0.5061025709684141560, 1.000000000000000000),
 ( 1.000000000000000000, 0.4881721342722142309, 1.000000000000000000),
 ( 1.000000000000000000, 0.4810711757771862218, 1.000000000000000000),
 ( 1.000000000000000000, 0.4726640060677306798, 1.000000000000000000),
 ( 1.000000000000000000, 0.4715283203431685499, 1.000000000000000000),
 ( 1.000000000000000000, 0.4761415489114428357, 1.000000000000000000),
 ( 1.000000000000000000, 0.4818043763597766316, 1.000000000000000000),
 ( 1.000000000000000000, 0.4989518560459688667, 1.000000000000000000),
 ( 1.000000000000000000, 0.5102645520265423063, 1.000000000000000000),
 ( 1.000000000000000000, 0.5358562791028014249, 1.000000000000000000),
 ( 1.000000000000000000, 0.5501980292661743377, 1.000000000000000000),
 ( 1.000000000000000000, 0.5652620711642698526, 1.000000000000000000) ) ) 
 REPRESENTATION_ITEM ( '' )  SURFACE ( )  );
#23440=ORIENTED_EDGE ( 'NONE', *, *, #1351, .F. ) ;
#23447=CARTESIAN_POINT ( 'NONE',  ( 78.68244131272049913, 66.05295088176870877, 1.094381639753830182 ) ) ;
#23451=CARTESIAN_POINT ( 'NONE',  ( -75.45330471031414277, 33.71485196875532608, 12.49999999999999645 ) ) ;
#23455=CARTESIAN_POINT ( 'NONE',  ( -64.08758708074093136, -65.19654454972992141, 2.999999999999999112 ) ) ;
#23461=LINE ( 'NONE', #35436, #11212 ) ;
#23471=DIRECTION ( 'NONE',  ( 0.000000000000000000, 0.000000000000000000, 1.000000000000000000 ) ) ;
#23477=CARTESIAN_POINT ( 'NONE',  ( -56.31571917568489738, 30.58480147475593114, -3.912689169536864853 ) ) ;
#23482=CARTESIAN_POINT ( 'NONE',  ( 80.32635178447517887, 66.28770415027543095, -1.483157530539362279 ) ) ;
#23489=CARTESIAN_POINT ( 'NONE',  ( 75.80265905884337485, 60.84868533121094458, 3.810661578667723148 ) ) ;
#23496=CARTESIAN_POINT ( 'NONE',  ( -63.58520484588292732, 35.72026407271187765, 6.999999999999999112 ) ) ;
#23498=CARTESIAN_POINT ( 'NONE',  ( 81.94117896397187906, 62.33638752673003580, 2.166533184762200026 ) ) ;
#23501=AXIS2_PLACEMENT_3D ( 'NONE', #21100, #11394, #17367 ) ;
#23511=DIRECTION ( 'NONE',  ( 0.3757233601570931225, 0.9267318687906784813, 0.000000000000000000 ) ) ;
#23516=ORIENTED_EDGE ( 'NONE', *, *, #32881, .F. ) ;
#23519=CARTESIAN_POINT ( 'NONE',  ( 67.10699435067097340, 58.18157613906911507, -3.995511504169226402 ) ) ;
#23535=CARTESIAN_POINT ( 'NONE',  ( 80.77858121287650306, 63.01782502344085657, 3.459421039841293233 ) ) ;
#23539=CARTESIAN_POINT ( 'NONE',  ( 79.36485406729210013, 60.67242113316871155, -2.285396881590245677 ) ) ;
#23542=CARTESIAN_POINT ( 'NONE',  ( 78.83984420990714170, 66.12288285737325566, -1.382728580142345454 ) ) ;
#23543=CARTESIAN_POINT ( 'NONE',  ( 78.08876170118931270, 64.69829802809502439, 3.164065397988977235 ) ) ;
#23546=CARTESIAN_POINT ( 'NONE',  ( 80.32635178447536362, 66.28770415027547358, 1.483157530538789626 ) ) ;
#23549=CARTESIAN_POINT ( 'NONE',  ( -62.75216693000847101, 36.25077706935577027, -4.893820751806843283 ) ) ;
#23551=DIRECTION ( 'NONE',  ( -0.000000000000000000, -0.000000000000000000, 1.000000000000000000 ) ) ;
#23553=DIRECTION ( 'NONE',  ( -1.000000000000000000, 0.000000000000000000, 0.000000000000000000 ) ) ;
#23560=CARTESIAN_POINT ( 'NONE',  ( -65.04872026876938662, 34.92042435966252611, -6.752913741461258113 ) ) ;
#23566=CARTESIAN_POINT ( 'NONE',  ( 66.27376694608996388, 57.73522568913447373, 4.000000000000000000 ) ) ;
#23567=CARTESIAN_POINT ( 'NONE',  ( 72.17048485476517783, 59.77360812419138369, -3.955776929930289398 ) ) ;
#23570=AXIS2_PLACEMENT_3D ( 'NONE', #24359, #18173, #30764 ) ;
#23578=DIRECTION ( 'NONE',  ( 0.000000000000000000, 0.000000000000000000, 1.000000000000000000 ) ) ;
#23581=CARTESIAN_POINT ( 'NONE',  ( 80.62899510017081184, 61.84672251665477205, -2.918211652848216264 ) ) ;
#23583=CARTESIAN_POINT ( 'NONE',  ( 80.32689410753103232, 62.53373119284189130, 3.467090974304449347 ) ) ;
#23592=CARTESIAN_POINT ( 'NONE',  ( 76.21224277836739702, 64.31709241891930162, -2.649705962983377461 ) ) ;
#23597=CARTESIAN_POINT ( 'NONE',  ( 81.02128870047407361, 63.12856183665077481, 3.380792992375197148 ) ) ;
#23606=CARTESIAN_POINT ( 'NONE',  ( 67.77942698303134250, 58.15829091545840157, 3.995247128881094678 ) ) ;
#23610=CARTESIAN_POINT ( 'NONE',  ( 79.96011558216464721, 64.80970700093439518, -3.432259906339275801 ) ) ;
#23613=CARTESIAN_POINT ( 'NONE',  ( -58.93521193748835429, 27.64319143539499279, 6.467610917687007799 ) ) ;
#23621=CARTESIAN_POINT ( 'NONE',  ( 78.86912799350172065, 65.82616116372945214, -2.227525437860510937 ) ) ;
#23623=CARTESIAN_POINT ( 'NONE',  ( 79.41630106684688428, 65.17102571570140412, 3.206617288017371337 ) ) ;
#23637=CARTESIAN_POINT ( 'NONE',  ( 81.49447160051045103, 61.73183938760540457, 1.953285432047543901 ) ) ;
#23657=VERTEX_POINT ( 'NONE', #34608 ) ;
#23663=EDGE_CURVE ( 'NONE', #37345, #9551, #29183, .T. ) ;
#23668=CARTESIAN_POINT ( 'NONE',  ( -57.97698207090199674, 31.94645990616745834, -4.307980060361010999 ) ) ;
#23674=CARTESIAN_POINT ( 'NONE',  ( 82.16223423120655411, 62.72759567084518295, -2.080779877698640146 ) ) ;
#23681=CARTESIAN_POINT ( 'NONE',  ( 74.58877118170933329, 61.99488014651142009, 3.786335567263263702 ) ) ;
#23683=ORIENTED_EDGE ( 'NONE', *, *, #2396, .T. ) ;
#23684=CARTESIAN_POINT ( 'NONE',  ( -62.96463773297387689, 37.71389135159058270, 4.136849086241030982 ) ) ;
#23689=CARTESIAN_POINT ( 'NONE',  ( 82.00886418671287004, 63.26204695399094646, 2.636331425444717436 ) ) ;
#23709=CARTESIAN_POINT ( 'NONE',  ( 67.05715689120697220, 57.86208461462646113, -3.995640437668404932 ) ) ;
#23714=CARTESIAN_POINT ( 'NONE',  ( 77.97569881417399529, 65.55229714878629466, 1.909807370998233722 ) ) ;
#23722=CARTESIAN_POINT ( 'NONE',  ( 81.13619541807486257, 61.97540048441254612, 2.718470589328604081 ) ) ;
#23725=CARTESIAN_POINT ( 'NONE',  ( 77.86640729734752142, 62.36914183036531512, -3.839379600940508119 ) ) ;
#23729=CARTESIAN_POINT ( 'NONE',  ( 81.64588081867499625, 62.19174680642493058, -2.443770662193221810 ) ) ;
#23730=CARTESIAN_POINT ( 'NONE',  ( 78.90238306073098329, 63.15141027621823611, 3.791687334209852267 ) ) ;
#23733=CARTESIAN_POINT ( 'NONE',  ( 82.52706534919268222, 63.19378067493421014, 1.386429027373558664 ) ) ;
#23744=EDGE_CURVE ( 'NONE', #39470, #9255, #4282, .T. ) ;
#23758=CARTESIAN_POINT ( 'NONE',  ( 72.75889805100318597, 61.54370698478811619, -3.677837812371882897 ) ) ;
#23761=AXIS2_PLACEMENT_3D ( 'NONE', #8661, #24317, #36880 ) ;
#23764=LINE ( 'NONE', #11599, #19535 ) ;
#23766=CARTESIAN_POINT ( 'NONE',  ( -66.99872204295122913, 28.48507918597134037, 9.800414904976365804 ) ) ;
#23768=CARTESIAN_POINT ( 'NONE',  ( 79.28407881342867825, 64.35615987108394620, -3.584461231902843714 ) ) ;
#23769=CARTESIAN_POINT ( 'NONE',  ( 79.69769351933607027, 63.91149418591603393, 3.725738571856552994 ) ) ;
#23783=CARTESIAN_POINT ( 'NONE',  ( 79.05590852586873041, 65.97304283769160804, 2.079311677127754887 ) ) ;
#23795=CARTESIAN_POINT ( 'NONE',  ( 67.81915466200213416, 58.05084569011909679, 3.988165415173097195 ) ) ;
#23799=CARTESIAN_POINT ( 'NONE',  ( 81.21856020378540109, 61.45841878490982424, -1.842213953838253815 ) ) ;
#23802=CARTESIAN_POINT ( 'NONE',  ( -57.68674048389794962, 29.08812126441108603, 4.503248736989442058 ) ) ;
#23804=ORIENTED_EDGE ( 'NONE', *, *, #23663, .F. ) ;
#23807=CARTESIAN_POINT ( 'NONE',  ( 81.03586710326727882, 61.41218721227320287, -1.994058748902159950 ) ) ;
#23809=CARTESIAN_POINT ( 'NONE',  ( 78.72772338417267690, 65.90741647005506820, 1.973779052375973064 ) ) ;
#23811=AXIS2_PLACEMENT_3D ( 'NONE', #27415, #20619, #33206 ) ;
#23814=CARTESIAN_POINT ( 'NONE',  ( 75.58356882164667923, 59.79721036961944236, -3.404024988867352164 ) ) ;
#23828=CARTESIAN_POINT ( 'NONE',  ( 79.18807306865346618, 66.05665914930217752, 1.983726836936665183 ) ) ;
#23857=CARTESIAN_POINT ( 'NONE',  ( -58.12241481891157946, 28.59128022406728675, -4.921134609696957263 ) ) ;
#23863=CARTESIAN_POINT ( 'NONE',  ( 78.94658775073214940, 66.18447242754096749, -1.227604746834844107 ) ) ;
#23870=CARTESIAN_POINT ( 'NONE',  ( 74.45643886899652841, 62.27924959144220196, 3.661998389317300706 ) ) ;
#23874=CARTESIAN_POINT ( 'NONE',  ( -62.99925096543677938, 37.98736139490962671, 4.069933184287122252 ) ) ;
#23876=CARTESIAN_POINT ( 'NONE',  ( 9.703489126596464232, 56.50623631086179444, 1.000000000000000000 ) ) ;
#23879=CARTESIAN_POINT ( 'NONE',  ( -67.57960606288301619, 36.15173574121458699, 8.626892781888731321 ) ) ;
#23880=CARTESIAN_POINT ( 'NONE',  ( 78.68815740766761735, 66.05701152551952759, 1.050153991572632561 ) ) ;
#23887=AXIS2_PLACEMENT_3D ( 'NONE', #29930, #1747, #14278 ) ;
#23901=CARTESIAN_POINT ( 'NONE',  ( 66.85741207324237223, 57.95599960577073517, -3.999594749380519954 ) ) ;
#23902=ADVANCED_FACE ( 'NONE', ( #8991 ), #24650, .T. ) ;
#23913=CARTESIAN_POINT ( 'NONE',  ( 80.03496335128151884, 66.36160760684386162, -1.085061034363233201 ) ) ;
#23914=CARTESIAN_POINT ( 'NONE',  ( 80.68504733838216225, 63.31860838049915685, 3.572022490087450652 ) ) ;
#23919=CARTESIAN_POINT ( 'NONE',  ( 77.45101235711661047, 65.18271368322074011, -2.178915381671167939 ) ) ;
#23924=CARTESIAN_POINT ( 'NONE',  ( 79.33055955479225929, 65.97011375961784552, -2.296576099416863581 ) ) ;
#23925=CARTESIAN_POINT ( 'NONE',  ( 78.85022303194003257, 62.54057813906807439, 3.766285651913947596 ) ) ;
#23930=CARTESIAN_POINT ( 'NONE',  ( 79.66449323073867106, 66.32230831612973532, 1.250177805244208296 ) ) ;
#23941=DIRECTION ( 'NONE',  ( -1.000000000000000000, -1.734723475976808672E-15, 0.000000000000000000 ) ) ;
#23951=CARTESIAN_POINT ( 'NONE',  ( 66.58353442343859285, 57.79581178809598896, 3.999616584010542208 ) ) ;
#23952=CARTESIAN_POINT ( 'NONE',  ( 71.26393988290669768, 58.68354208002635630, -3.837797619696095008 ) ) ;
#23966=EDGE_CURVE ( 'NONE', #13498, #5492, #14901, .T. ) ;
#23968=CARTESIAN_POINT ( 'NONE',  ( 78.69113869042872977, 65.45098002628645872, -2.699019001080980473 ) ) ;
#23970=CARTESIAN_POINT ( 'NONE',  ( 80.24949846641645479, 62.81397012663808255, 3.564905221331804430 ) ) ;
#23996=CARTESIAN_POINT ( 'NONE',  ( 67.43935760634008147, 58.17964655298460741, 3.998402061830689025 ) ) ;
#24002=DIRECTION ( 'NONE',  ( -0.3757233601570978965, -0.9267318687906764829, 0.000000000000000000 ) ) ;
#24004=CARTESIAN_POINT ( 'NONE',  ( -58.69259491913187787, 29.82092612118092489, 5.479210374447095688 ) ) ;
#24009=ORIENTED_EDGE ( 'NONE', *, *, #39824, .T. ) ;
#24011=CARTESIAN_POINT ( 'NONE',  ( 80.06960825067233145, 63.75365790317245995, -3.697630003121159969 ) ) ;
#24014=CARTESIAN_POINT ( 'NONE',  ( 81.04529349509155622, 61.25860024526325276, 1.340350474428757099 ) ) ;
#24017=ORIENTED_EDGE ( 'NONE', *, *, #22531, .F. ) ;
#24020=CARTESIAN_POINT ( 'NONE',  ( 73.39456880541679595, 61.63402075718063600, -3.749455561531862546 ) ) ;
#24022=EDGE_CURVE ( 'NONE', #16945, #7860, #17960, .T. ) ;
#24024=CARTESIAN_POINT ( 'NONE',  ( -68.98442902999595105, 21.93515443114010210, -9.800414904976365804 ) ) ;
#24026=CARTESIAN_POINT ( 'NONE',  ( -59.87552183813137674, 24.84364830758654108, -46.17089178453873188 ) ) ;
#24033=DIRECTION ( 'NONE',  ( -0.000000000000000000, -0.000000000000000000, -1.000000000000000000 ) ) ;
#24036=CARTESIAN_POINT ( 'NONE',  ( 80.45827632841071875, 65.09029793562214650, 3.202775791561846663 ) ) ;
#24053=CARTESIAN_POINT ( 'NONE',  ( 81.05462132553121535, 63.14435662960352147, -3.368075118064902007 ) ) ;
#24064=CARTESIAN_POINT ( 'NONE',  ( 79.38068533922456993, 65.45287079212489800, -2.940771700540094624 ) ) ;
#24071=CARTESIAN_POINT ( 'NONE',  ( 79.82775505260887883, 66.24998868310140665, -1.780213741554920626 ) ) ;
#24072=EDGE_CURVE ( 'NONE', #16830, #5157, #26331, .T. ) ;
#24080=CARTESIAN_POINT ( 'NONE',  ( 75.42787669100914627, 61.66269772210893763, 3.901127667181031100 ) ) ;
#24086=CARTESIAN_POINT ( 'NONE',  ( -63.41438759659862257, 35.63967351046427012, 6.822170959111637956 ) ) ;
#24088=CARTESIAN_POINT ( 'NONE',  ( 81.95280109346369102, 63.95510859576443607, 2.731810022747816813 ) ) ;
#24094=CARTESIAN_POINT ( 'NONE',  ( -64.08758708074093136, 36.14363715547680300, 3.800414904976363140 ) ) ;
#24108=CARTESIAN_POINT ( 'NONE',  ( 66.71461092208421917, 57.89240490252945648, -3.999756211082519552 ) ) ;
#24114=CARTESIAN_POINT ( 'NONE',  ( 68.46975562008563543, 59.13163800552559479, 3.939088990506558030 ) ) ;
#24121=CARTESIAN_POINT ( 'NONE',  ( 82.26973386304365476, 64.90130211351629441, -1.000000000000000000 ) ) ;
#24123=CARTESIAN_POINT ( 'NONE',  ( 81.21317738564106037, 61.78038839029203189, 2.432199249741022307 ) ) ;
#24126=EDGE_CURVE ( 'NONE', #6217, #8770, #15356, .T. ) ;
#24128=CARTESIAN_POINT ( 'NONE',  ( 77.55533639035672877, 62.99992453720924601, -3.808649511194682979 ) ) ;
#24132=CARTESIAN_POINT ( 'NONE',  ( 78.99802787997164444, 66.11506539533232285, -1.704083397383983289 ) ) ;
#24133=CARTESIAN_POINT ( 'NONE',  ( 79.68931684371919744, 62.31783030446536742, 3.554489553981594607 ) ) ;
#24139=CARTESIAN_POINT ( 'NONE',  ( 81.16949749213439702, 61.30395080096879212, 1.008685033153497557 ) ) ;
#24156=DIRECTION ( 'NONE',  ( -0.000000000000000000, -0.000000000000000000, 1.000000000000000000 ) ) ;
#24170=CARTESIAN_POINT ( 'NONE',  ( 66.27376694608996388, 57.73522568913447373, 4.000000000000000000 ) ) ;
#24172=CARTESIAN_POINT ( 'NONE',  ( 69.35860043680946774, 58.39594701590269921, -3.954017255840812872 ) ) ;
#24186=CARTESIAN_POINT ( 'NONE',  ( 80.75587274821523920, 61.22306450394816579, -1.910479420724443989 ) ) ;
#24188=CARTESIAN_POINT ( 'NONE',  ( 79.66325760479739415, 66.16013226748967213, -2.011780557866151398 ) ) ;
#24189=CARTESIAN_POINT ( 'NONE',  ( 79.08605325858584933, 64.90301710537215740, 3.311815948186460634 ) ) ;
#24198=DIRECTION ( 'NONE',  ( 0.000000000000000000, 0.000000000000000000, -1.000000000000000000 ) ) ;
#24211=CARTESIAN_POINT ( 'NONE',  ( 67.67991563464998706, 58.42724437289452055, 3.992148460412343614 ) ) ;
#24226=CARTESIAN_POINT ( 'NONE',  ( 81.04520860822712791, 61.30615853997439046, -1.682919622592479625 ) ) ;
#24228=CARTESIAN_POINT ( 'NONE',  ( 78.64443580140854806, 65.97314938607597412, 1.660510093083201744 ) ) ;
#24232=CARTESIAN_POINT ( 'NONE',  ( 74.55930941259208566, 60.55296354997373953, -3.883841728571185481 ) ) ;
#24245=CARTESIAN_POINT ( 'NONE',  ( 81.36706168520311167, 62.61468991663328154, 3.015642068896308370 ) ) ;
#24255=CARTESIAN_POINT ( 'NONE',  ( -65.87013514634764988, 36.66000420377759639, -7.725785790320288449 ) ) ;
#24266=CARTESIAN_POINT ( 'NONE',  ( 81.33630325801044592, 62.05105258569628290, -2.628317182735725677 ) ) ;
#24277=ORIENTED_EDGE ( 'NONE', *, *, #24022, .F. ) ;
#24279=CARTESIAN_POINT ( 'NONE',  ( 80.30796587587548174, 63.87804906342756084, -3.654032574946329603 ) ) ;
#24285=CARTESIAN_POINT ( 'NONE',  ( 82.09393942629647256, 63.66644892668119127, -2.541832380859317286 ) ) ;
#24290=CARTESIAN_POINT ( 'NONE',  ( 73.39456880541679595, 61.63402075718063600, 3.749455561531862546 ) ) ;
#24297=CARTESIAN_POINT ( 'NONE',  ( -65.15514661499976512, 34.97220226750604866, 6.888442104241534913 ) ) ;
#24298=CARTESIAN_POINT ( 'NONE',  ( 81.73829655978381936, 61.84901640042588866, 1.708467252431126626 ) ) ;
#24310=ADVANCED_FACE ( 'NONE', ( #2790 ), #25805, .T. ) ;
#24316=CARTESIAN_POINT ( 'NONE',  ( 66.84168730393145097, 57.99964773888063974, -3.999029912551660182 ) ) ;
#24317=DIRECTION ( 'NONE',  ( -0.000000000000000000, -0.000000000000000000, 1.000000000000000000 ) ) ;
#24325=EDGE_LOOP ( 'NONE', ( #11037, #16048, #20892, #21305, #7335, #21502, #1264 ) ) ;
#24330=CARTESIAN_POINT ( 'NONE',  ( 82.59411735159429213, 63.56171878218356852, -1.000000000000000000 ) ) ;
#24332=CARTESIAN_POINT ( 'NONE',  ( 78.93014367432635936, 65.87924701951081374, 2.174925636353740366 ) ) ;
#24336=CARTESIAN_POINT ( 'NONE',  ( 79.35831483666115105, 61.48221340643407729, -3.218236826935543249 ) ) ;
#24339=CARTESIAN_POINT ( 'NONE',  ( 80.70340038347460165, 64.47061299330862028, -3.456914256419914455 ) ) ;
#24340=CARTESIAN_POINT ( 'NONE',  ( 78.41725481636187567, 64.09006905928654874, 3.590127757398426933 ) ) ;
#24341=ORIENTED_EDGE ( 'NONE', *, *, #21156, .T. ) ;
#24345=CARTESIAN_POINT ( 'NONE',  ( 81.16944410057618597, 61.30393124705405938, 1.011532654301222856 ) ) ;
#24350=PLANE ( 'NONE',  #3603 ) ;
#24359=CARTESIAN_POINT ( 'NONE',  ( -66.99872204295122913, 28.48507918597134037, -46.17089178453873188 ) ) ;
#24365=CARTESIAN_POINT ( 'NONE',  ( -68.98442902999595105, 21.93515443114010210, -12.49999999999999645 ) ) ;
#24373=CARTESIAN_POINT ( 'NONE',  ( 69.65195751129601831, 59.35873293165669651, -3.965028736237012907 ) ) ;
#24377=DIRECTION ( 'NONE',  ( -1.000000000000000000, 0.000000000000000000, 0.000000000000000000 ) ) ;
#24390=CARTESIAN_POINT ( 'NONE',  ( 80.65804582012491153, 61.64568945823260293, -2.699019001080977365 ) ) ;
#24393=CARTESIAN_POINT ( 'NONE',  ( 79.38089166731849389, 66.16750285958211464, -1.809109834152295093 ) ) ;
#24395=CARTESIAN_POINT ( 'NONE',  ( 80.58270521159307975, 62.07868998654234360, 3.101774481621348833 ) ) ;
#24396=ORIENTED_EDGE ( 'NONE', *, *, #25541, .T. ) ;
#24418=EDGE_CURVE ( 'NONE', #7860, #6802, #11018, .T. ) ;
#24420=CARTESIAN_POINT ( 'NONE',  ( 67.18992292689074475, 57.95373832061253694, 3.997022163556062324 ) ) ;
#24431=ORIENTED_EDGE ( 'NONE', *, *, #10732, .F. ) ;
#24433=CARTESIAN_POINT ( 'NONE',  ( 80.89855423268610934, 61.90964448260509556, -2.818206040476792129 ) ) ;
#24435=CARTESIAN_POINT ( 'NONE',  ( 79.61178798950636804, 64.58589821993884073, 3.525318766974264051 ) ) ;
#24438=CARTESIAN_POINT ( 'NONE',  ( 74.04982613775094080, 61.68561850464361385, -3.815996826674513009 ) ) ;
#24441=CARTESIAN_POINT ( 'NONE',  ( -63.06903391669472825, 38.60168910470162018, -4.000000000000000000 ) ) ;
#24452=CARTESIAN_POINT ( 'NONE',  ( 80.45887431248506516, 64.72775385883048216, 3.425340496581062322 ) ) ;
#24454=CARTESIAN_POINT ( 'NONE',  ( -9.439742135462632078, 51.66544268451064426, 4.000000000000000000 ) ) ;
#24456=DIRECTION ( 'NONE',  ( 1.000000000000000000, 0.000000000000000000, 0.000000000000000000 ) ) ;
#24463=ORIENTED_EDGE ( 'NONE', *, *, #23663, .T. ) ;
#24468=CARTESIAN_POINT ( 'NONE',  ( 79.20700709577712928, 65.89182355360532028, -2.372413575842141853 ) ) ;
#24476=ORIENTED_EDGE ( 'NONE', *, *, #30499, .T. ) ;
#24481=CARTESIAN_POINT ( 'NONE',  ( 80.27036958223403929, 63.85842528439429344, -3.661914029440275442 ) ) ;
#24483=ORIENTED_EDGE ( 'NONE', *, *, #12306, .F. ) ;
#24486=ORIENTED_EDGE ( 'NONE', *, *, #19642, .F. ) ;
#24488=CARTESIAN_POINT ( 'NONE',  ( 78.68995612299299580, 66.05828935306207939, -1.022614849746414922 ) ) ;
#24495=CARTESIAN_POINT ( 'NONE',  ( 74.30211141138923381, 59.57442121254392475, 3.624554307378899054 ) ) ;
#24505=CARTESIAN_POINT ( 'NONE',  ( 81.63129934975499680, 61.79668339569253988, 1.832274617051023569 ) ) ;
#24524=CARTESIAN_POINT ( 'NONE',  ( 67.04239844378345481, 57.90286417203066094, -3.997553359131193584 ) ) ;
#24530=CARTESIAN_POINT ( 'NONE',  ( 66.27376694608931018, 57.73522568913554665, 4.000000000000000000 ) ) ;
#24536=CARTESIAN_POINT ( 'NONE',  ( 78.69038500580381879, 66.05859403932473128, -1.000000000000000000 ) ) ;
#24537=CARTESIAN_POINT ( 'NONE',  ( 79.46693819636865896, 65.20858797830474884, 3.188730975143406088 ) ) ;
#24540=CARTESIAN_POINT ( 'NONE',  ( 77.25343114543989032, 63.60010822905027794, -3.597602401604580002 ) ) ;
#24544=CARTESIAN_POINT ( 'NONE',  ( 80.41462361967069228, 65.06645272473211605, -3.228380831070266410 ) ) ;
#24545=CARTESIAN_POINT ( 'NONE',  ( 76.25248298134042102, 64.19605381821563128, 2.844364419910045516 ) ) ;
#24552=CARTESIAN_POINT ( 'NONE',  ( 81.49402754981294095, 65.64225023272291537, 1.838010297257003822 ) ) ;
#24558=DIRECTION ( 'NONE',  ( -0.000000000000000000, 0.000000000000000000, -1.000000000000000000 ) ) ;
#24559=CARTESIAN_POINT ( 'NONE',  ( -64.14095127866887935, 35.19432717188715287, 4.537732464557205248 ) ) ;
#24563=CARTESIAN_POINT ( 'NONE',  ( 27.60344192425479193, 81.15229837709949834, 4.000000000000000000 ) ) ;
#24574=B_SPLINE_CURVE_WITH_KNOTS ( 'NONE', 3,
 ( #40400, #37927, #33852, #12205, #5632, #31163, #24776, #30763, #2566, #37320, #21693, #9118, #26401, #19408, #6655, #32585, #4381, #28678, #13419, #31771, #23107, #7247, #9933, #13022, #1095, #35475, #3786, #3986 ),
 .UNSPECIFIED., .F., .F.,
 ( 4, 2, 2, 2, 2, 2, 2, 2, 2, 2, 2, 2, 2, 4 ),
 ( 1.301042606982605321E-18, 0.0002572729306080222961, 0.0005145458612160432911, 0.001029091722432085281, 0.002058183444864175766, 0.003087275167296266686, 0.004116366889728356737, 0.006174550334592495207, 0.008232733779456637146, 0.01234910066918491062, 0.01440728411404905082, 0.01543637583648112092, 0.01595092169769715337, 0.01646546755891318756 ),
 .UNSPECIFIED. ) ;
#24575=CARTESIAN_POINT ( 'NONE',  ( -64.08758708074093136, 37.77454521956886424, -3.093244392760367667 ) ) ;
#24581=CARTESIAN_POINT ( 'NONE',  ( 69.60281991352538000, 59.48300438377392396, -3.944663542062654571 ) ) ;
#24584=CARTESIAN_POINT ( 'NONE',  ( -11.81496944966682960, -21.25669541281728669, 1.000000000000000000 ) ) ;
#24594=CARTESIAN_POINT ( 'NONE',  ( 80.53617040090057344, 61.82406284986341660, -2.948506306558747347 ) ) ;
#24596=CARTESIAN_POINT ( 'NONE',  ( 81.68772813446383907, 64.20773789716569979, -2.952528780688971288 ) ) ;
#24597=CARTESIAN_POINT ( 'NONE',  ( 78.97528327045988306, 64.81351720955758822, 3.340572457511927773 ) ) ;
#24607=CARTESIAN_POINT ( 'NONE',  ( -94.24726447194083789, -65.19654454972992141, 8.800414904976364028 ) ) ;
#24613=CARTESIAN_POINT ( 'NONE',  ( -64.08758708074093136, 43.61223004741322740, 1.000000000000000000 ) ) ;
#24623=CARTESIAN_POINT ( 'NONE',  ( 67.08924564209870312, 58.23032185317626386, 3.992323350375290403 ) ) ;
#24641=CARTESIAN_POINT ( 'NONE',  ( 80.61389980387333765, 62.62535450461751907, -3.411701596789205926 ) ) ;
#24643=CARTESIAN_POINT ( 'NONE',  ( 81.06165217645977350, 61.41816154915743908, 1.973779052375980392 ) ) ;
#24647=CARTESIAN_POINT ( 'NONE',  ( 74.62207946275562165, 60.41194043352551546, -3.856662941142526169 ) ) ;
#24650=PLANE ( 'NONE',  #8760 ) ;
#24659=CARTESIAN_POINT ( 'NONE',  ( 81.49799543786487277, 62.67690593247113640, 2.943961322784972356 ) ) ;
#24662=ORIENTED_EDGE ( 'NONE', *, *, #33278, .F. ) ;
#24667=VECTOR ( 'NONE', #35796, 1000.000000000000000 ) ;
#24679=CARTESIAN_POINT ( 'NONE',  ( 79.95152939680100701, 65.17166210280107919, -3.248659383495581920 ) ) ;
#24691=CARTESIAN_POINT ( 'NONE',  ( 80.84870020435621996, 62.70902516261515558, -3.354617312347319746 ) ) ;
#24692=CARTESIAN_POINT ( 'NONE',  ( -59.00096901216079459, 28.68090462335501201, -7.030006629679628638 ) ) ;
#24697=CARTESIAN_POINT ( 'NONE',  ( 81.87949262442919007, 63.91736224575971193, -2.817575383041753589 ) ) ;
#24699=VECTOR ( 'NONE', #1393, 1000.000000000000114 ) ;
#24701=FACE_OUTER_BOUND ( 'NONE', #28133, .T. ) ;
#24707=CARTESIAN_POINT ( 'NONE',  ( 73.59222858082205221, 59.63291812028631966, 3.785151435545463183 ) ) ;
#24709=EDGE_LOOP ( 'NONE', ( #7096, #2292, #5511, #16037 ) ) ;
#24714=CARTESIAN_POINT ( 'NONE',  ( 80.82569761265843056, 65.28806468744768665, 2.919551171211351548 ) ) ;
#24716=CARTESIAN_POINT ( 'NONE',  ( -2.954197855305039422, -12.43481156997016157, 4.000000000000000000 ) ) ;
#24733=CARTESIAN_POINT ( 'NONE',  ( 66.97838688114072170, 58.07970146089488850, -3.998003515188802037 ) ) ;
#24746=CARTESIAN_POINT ( 'NONE',  ( 81.73765358980274698, 61.68994590043247683, -1.132734665583632117 ) ) ;
#24747=CARTESIAN_POINT ( 'NONE',  ( 78.69119446862563905, 66.01295734309309182, 1.592560325354587913 ) ) ;
#24748=CARTESIAN_POINT ( 'NONE',  ( -63.96695182803188828, 19.27020452292899222, 8.800414904976364028 ) ) ;
#24750=CARTESIAN_POINT ( 'NONE',  ( 77.82713238777952824, 60.98268764611934500, -3.435658781985014176 ) ) ;
#24751=B_SPLINE_CURVE_WITH_KNOTS ( 'NONE', 3,
 ( #18464, #25472, #37807, #34563, #21577, #19088, #24865, #37405, #40698, #3471 ),
 .UNSPECIFIED., .F., .F.,
 ( 4, 2, 2, 2, 4 ),
 ( 2.168404344971008868E-19, 8.504419282386946875E-05, 0.0001700883856477387207, 0.0003401767712954767908, 0.0006803535425909649657 ),
 .UNSPECIFIED. ) ;
#24755=CARTESIAN_POINT ( 'NONE',  ( 80.13372729538053818, 65.27601544180762971, -3.162824939344919262 ) ) ;
#24756=CARTESIAN_POINT ( 'NONE',  ( 76.46949791074166569, 63.77707083977482228, 3.308002540424330284 ) ) ;
#24760=CARTESIAN_POINT ( 'NONE',  ( -58.72892591012804075, 29.68775822799332076, 5.573531433662443746 ) ) ;
#24761=CARTESIAN_POINT ( 'NONE',  ( 81.23565735523312981, 65.86993722804051288, 1.793694987645560568 ) ) ;
#24768=CARTESIAN_POINT ( 'NONE',  ( -63.58520484588294153, 35.72026407271188475, -6.999999999999999112 ) ) ;
#24776=CARTESIAN_POINT ( 'NONE',  ( 80.71272553023811724, 61.13839519651874355, 1.655401764483099614 ) ) ;
#24779=CARTESIAN_POINT ( 'NONE',  ( 75.38950776596149694, 59.47909021198979218, -3.241469810694041609 ) ) ;
#24793=CARTESIAN_POINT ( 'NONE',  ( 69.29807964942261833, 58.55307042757259950, -3.976370928559293638 ) ) ;
#24798=EDGE_CURVE ( 'NONE', #30864, #34912, #21309, .T. ) ;
#24809=CARTESIAN_POINT ( 'NONE',  ( 79.24578529683977024, 64.32976145010148628, -3.589982250315052692 ) ) ;
#24811=CARTESIAN_POINT ( 'NONE',  ( 78.89436432227893192, 66.15509128278823425, -1.313329331391854371 ) ) ;
#24812=CARTESIAN_POINT ( 'NONE',  ( 79.66447349905094200, 63.54298318056227401, 3.741985197832887522 ) ) ;
#24814=CARTESIAN_POINT ( 'NONE',  ( -64.08758708074093136, 38.13199975834322686, 3.043809435734689206 ) ) ;
#24835=CARTESIAN_POINT ( 'NONE',  ( 67.50273067437429120, 58.00668225682344570, 3.993945454764282310 ) ) ;
#24852=VERTEX_POINT ( 'NONE', #30831 ) ;
#24853=CARTESIAN_POINT ( 'NONE',  ( 80.95922275190012840, 61.28229338972344920, -1.760837461004916893 ) ) ;
#24854=CARTESIAN_POINT ( 'NONE',  ( 81.23507808130548824, 61.62583295638711434, -2.125034277891705070 ) ) ;
#24855=DIRECTION ( 'NONE',  ( -1.000000000000000000, -0.000000000000000000, -0.000000000000000000 ) ) ;
#24856=AXIS2_PLACEMENT_3D ( 'NONE', #37661, #6190, #34626 ) ;
#24857=CARTESIAN_POINT ( 'NONE',  ( 81.03586710326727882, 61.41218721227320998, 1.994058748902159062 ) ) ;
#24861=CARTESIAN_POINT ( 'NONE',  ( -56.59682361629209879, 30.63869417066593925, 3.015094993620162978 ) ) ;
#24865=CARTESIAN_POINT ( 'NONE',  ( -54.93018042890351182, 31.40271527509257865, 1.217153544005994181 ) ) ;
#24873=CARTESIAN_POINT ( 'NONE',  ( 81.15569957775159082, 61.29889919928260156, 1.113695828830617796 ) ) ;
#24878=CARTESIAN_POINT ( 'NONE',  ( -64.58677651244121876, 34.69729445092669806, -5.982681548040577724 ) ) ;
#24893=CARTESIAN_POINT ( 'NONE',  ( 80.35608454708172133, 64.67152608030554006, -3.471690071579495829 ) ) ;
#24903=CARTESIAN_POINT ( 'NONE',  ( 78.72446908900997187, 66.04077733106291248, -1.541060042019481990 ) ) ;
#24910=CARTESIAN_POINT ( 'NONE',  ( 81.59006957456230680, 61.61658442860579044, -1.498428902123934980 ) ) ;
#24916=CARTESIAN_POINT ( 'NONE',  ( 72.61754431144450450, 61.86111285056382059, 3.476886323448412419 ) ) ;
#24925=CARTESIAN_POINT ( 'NONE',  ( 80.71932482181554747, 65.23126254902237520, 3.019969592843124939 ) ) ;
#24932=EDGE_CURVE ( 'NONE', #23657, #9954, #18649, .T. ) ;
#24939=DIRECTION ( 'NONE',  ( -0.9267318687906771491, 0.3757233601570964532, 0.000000000000000000 ) ) ;
#24942=EDGE_LOOP ( 'NONE', ( #34922, #11900 ) ) ;
#24946=CARTESIAN_POINT ( 'NONE',  ( 66.58549141467136678, 57.79032289594774596, -3.999530551061463157 ) ) ;
#24948=ORIENTED_EDGE ( 'NONE', *, *, #3566, .F. ) ;
#24949=CARTESIAN_POINT ( 'NONE',  ( -57.16504416091206053, 33.41445838748276742, 3.999999999999999112 ) ) ;
#24950=CYLINDRICAL_SURFACE ( 'NONE', #12142, 6.681288188914807691 ) ;
#24955=CARTESIAN_POINT ( 'NONE',  ( 78.69036185089562707, 66.05857758962513060, -1.005837412005794906 ) ) ;
#24956=ADVANCED_FACE ( 'NONE', ( #3259 ), #9469, .T. ) ;
#24957=CARTESIAN_POINT ( 'NONE',  ( 79.31717123896756050, 65.40625759565881481, 2.968223699503263369 ) ) ;
#24961=CARTESIAN_POINT ( 'NONE',  ( 75.88202180556027088, 63.57356190189722156, -3.253266109296521602 ) ) ;
#24965=CARTESIAN_POINT ( 'NONE',  ( 81.31240362382358455, 61.49079461182719086, -1.766895996212483722 ) ) ;
#24967=CARTESIAN_POINT ( 'NONE',  ( 77.25588627614904169, 64.91391695767342185, 2.512892981323197716 ) ) ;
#24971=CARTESIAN_POINT ( 'NONE',  ( 82.13040900219787943, 64.82864533757677350, 1.905332024690495007 ) ) ;
#24977=CARTESIAN_POINT ( 'NONE',  ( -63.25792396345003255, 35.57414178363083579, -6.629687970507617045 ) ) ;
#24981=CYLINDRICAL_SURFACE ( 'NONE', #35367, 3.000000000000004885 ) ;
#24987=CARTESIAN_POINT ( 'NONE',  ( 68.91559242293919851, 58.09233434678947816, -3.947612818959274072 ) ) ;
#24992=CARTESIAN_POINT ( 'NONE',  ( -64.08758708074093136, 38.13199975834722011, -3.043809435734137647 ) ) ;
#24998=CARTESIAN_POINT ( 'NONE',  ( 69.37860636825551808, 58.34396603459876474, -3.943722715026765524 ) ) ;
#25003=DIRECTION ( 'NONE',  ( -0.4582725098355704407, 0.8888117386314197121, 0.000000000000000000 ) ) ;
#25008=CARTESIAN_POINT ( 'NONE',  ( 80.15150095960399312, 61.72183351646653193, -3.055712048904937639 ) ) ;
#25012=CARTESIAN_POINT ( 'NONE',  ( 81.74641399446780099, 62.01249025250110947, -2.076176908533885701 ) ) ;
#25013=CARTESIAN_POINT ( 'NONE',  ( 80.71160662450162704, 61.49558808705152302, 2.436540443961503044 ) ) ;
#25018=CARTESIAN_POINT ( 'NONE',  ( 82.43037228308448050, 64.59322875725442259, 1.000000000000000000 ) ) ;
#25032=APPLICATION_CONTEXT ( 'automotive_design' ) ;
#25046=CARTESIAN_POINT ( 'NONE',  ( 67.10699435067097340, 58.18157613906911507, 3.995511504169227290 ) ) ;
#25049=CARTESIAN_POINT ( 'NONE',  ( -63.03213158086114021, 38.26878225442446535, 4.032857076801014351 ) ) ;
#25059=CARTESIAN_POINT ( 'NONE',  ( 80.00230669363345726, 63.71856487089240773, -3.706996517075249464 ) ) ;
#25061=CARTESIAN_POINT ( 'NONE',  ( 80.03595747215288725, 63.73611138703241608, 3.702313260098205383 ) ) ;
#25074=EDGE_CURVE ( 'NONE', #38802, #12078, #11320, .T. ) ;
#25081=CARTESIAN_POINT ( 'NONE',  ( 79.72834705192842364, 65.67299761742502540, 2.773332820898658291 ) ) ;
#25084=ORIENTED_EDGE ( 'NONE', *, *, #31085, .T. ) ;
#25096=CARTESIAN_POINT ( 'NONE',  ( 81.20569604368299110, 61.99964894245921698, -2.688322534164195421 ) ) ;
#25097=DIRECTION ( 'NONE',  ( 0.000000000000000000, 0.000000000000000000, 1.000000000000000000 ) ) ;
#25106=CARTESIAN_POINT ( 'NONE',  ( 79.16740428156647624, 65.60392721301286656, -2.747716423863119761 ) ) ;
#25108=ORIENTED_EDGE ( 'NONE', *, *, #17536, .T. ) ;
#25112=CARTESIAN_POINT ( 'NONE',  ( 81.16771000429746152, 61.30329618601648889, -1.041818241550651614 ) ) ;
#25118=CARTESIAN_POINT ( 'NONE',  ( 73.45088770829859470, 61.50831400533110127, 3.795548882783541522 ) ) ;
#25127=CARTESIAN_POINT ( 'NONE',  ( 81.74641399446790047, 62.01249025250114499, 2.076176908533788446 ) ) ;
#25143=CARTESIAN_POINT ( 'NONE',  ( 66.68223030933245354, 57.98259542220473861, -3.998057522776775841 ) ) ;
#25145=CARTESIAN_POINT ( 'NONE',  ( -56.58158928110407970, 30.30283765713129540, 3.953813256333435611 ) ) ;
#25152=CARTESIAN_POINT ( 'NONE',  ( 78.99593020234610208, 66.21156118037407623, -1.070820504727074685 ) ) ;
#25154=CARTESIAN_POINT ( 'NONE',  ( 81.09687786842310686, 61.96238702813622723, 2.735335646780897800 ) ) ;
#25157=CARTESIAN_POINT ( 'NONE',  ( 77.35226663217761711, 63.40502609692226343, -3.687756614093553154 ) ) ;
#25161=CARTESIAN_POINT ( 'NONE',  ( 80.40747942978335061, 64.69963996956799690, -3.448515284080292620 ) ) ;
#25163=CARTESIAN_POINT ( 'NONE',  ( 77.16059773406418287, 63.78117330919809547, 3.480716904142236334 ) ) ;
#25168=DIRECTION ( 'NONE',  ( 0.000000000000000000, -1.000000000000000000, 0.000000000000000000 ) ) ;
#25170=CARTESIAN_POINT ( 'NONE',  ( 78.97185648144790093, 66.19841638340301415, 1.173033592341439002 ) ) ;
#25176=CARTESIAN_POINT ( 'NONE',  ( -62.84881660470023945, 35.59796388917940391, -5.828906544001253742 ) ) ;
#25177=CARTESIAN_POINT ( 'NONE',  ( -62.75216693000863444, 36.25077706935546473, 4.893820751807268721 ) ) ;
#25197=CARTESIAN_POINT ( 'NONE',  ( 68.51828301517210207, 58.84837915819282728, -3.980709302925311555 ) ) ;
#25216=CARTESIAN_POINT ( 'NONE',  ( 80.42502267531087057, 61.03612496587228975, -1.832491541757258258 ) ) ;
#25220=CARTESIAN_POINT ( 'NONE',  ( 79.96642255696579582, 65.80764937177660556, -2.611089443229511087 ) ) ;
#25221=CARTESIAN_POINT ( 'NONE',  ( 79.18319737856852214, 64.63648950223996792, 3.475409704257728105 ) ) ;
#25223=B_SPLINE_CURVE_WITH_KNOTS ( 'NONE', 3,
 ( #34382, #190, #31683, #18486 ),
 .UNSPECIFIED., .F., .F.,
 ( 4, 4 ),
 ( 2.602085213965210642E-18, 0.0006739815419856422761 ),
 .UNSPECIFIED. ) ;
#25224=CARTESIAN_POINT ( 'NONE',  ( 82.18775271763095702, 62.23297483488567394, 1.000000000000000000 ) ) ;
#25249=CARTESIAN_POINT ( 'NONE',  ( 67.02763120020985355, 57.94366503926806899, 3.998791315154376136 ) ) ;
#25265=CARTESIAN_POINT ( 'NONE',  ( 79.79878548311195630, 63.97024398824578384, -3.714073935154548867 ) ) ;
#25267=CARTESIAN_POINT ( 'NONE',  ( 81.01114204962451026, 61.40637449960412653, 2.012706562768916019 ) ) ;
#25285=CARTESIAN_POINT ( 'NONE',  ( 80.03255827398542976, 65.21842193378448371, 3.211742283750887328 ) ) ;
#25291=EDGE_CURVE ( 'NONE', #15467, #28971, #20554, .T. ) ;
#25302=CARTESIAN_POINT ( 'NONE',  ( 80.98905497205693393, 62.76708948751929995, -3.312281065658535528 ) ) ;
#25308=ADVANCED_FACE ( 'NONE', ( #14294 ), #36337, .F. ) ;
#25315=CARTESIAN_POINT ( 'NONE',  ( 78.79648636889818647, 65.96905942459900984, -1.896863055073860771 ) ) ;
#25321=CARTESIAN_POINT ( 'NONE',  ( 81.60411730068122438, 64.94496191031744559, -2.665107514501070085 ) ) ;
#25327=CARTESIAN_POINT ( 'NONE',  ( 71.62240613637702324, 61.07494268190700382, 3.699617110277040766 ) ) ;
#25332=CARTESIAN_POINT ( 'NONE',  ( -57.80924547062588204, 32.30639590073213441, -4.182592178550135209 ) ) ;
#25334=CARTESIAN_POINT ( 'NONE',  ( 81.40473435056813400, 64.45019880697493875, 3.071899782094677622 ) ) ;
#25348=CARTESIAN_POINT ( 'NONE',  ( 66.55026548882318593, 57.88912323611526034, -3.999530551066472039 ) ) ;
#25353=CARTESIAN_POINT ( 'NONE',  ( -55.71184120586745792, 30.71742687230118207, 1.474814583819915370 ) ) ;
#25363=CARTESIAN_POINT ( 'NONE',  ( 80.37799020243581083, 66.31529150154180741, -1.204231967108630785 ) ) ;
#25364=CARTESIAN_POINT ( 'NONE',  ( 80.02704812381016097, 64.10187485078017744, 3.679799701112132837 ) ) ;
#25366=CARTESIAN_POINT ( 'NONE',  ( 76.98341904138477787, 61.29654188154459860, -3.753756190332446785 ) ) ;
#25371=CARTESIAN_POINT ( 'NONE',  ( 81.29658979812199959, 62.90761208998645060, -3.189931650267181507 ) ) ;
#25372=CARTESIAN_POINT ( 'NONE',  ( 78.21991615976332923, 63.09003589986990335, 3.816136337383044808 ) ) ;
#25373=ORIENTED_EDGE ( 'NONE', *, *, #17231, .T. ) ;
#25376=CARTESIAN_POINT ( 'NONE',  ( 80.56094004998632840, 66.12977872868221141, 1.831286414254332806 ) ) ;
#25383=CARTESIAN_POINT ( 'NONE',  ( -64.09407456991031893, 35.62175799955464583, 4.126536650001270345 ) ) ;
#25390=CARTESIAN_POINT ( 'NONE',  ( 79.42141780276817542, 60.69055068925465690, -2.271081754790353457 ) ) ;
#25399=ORIENTED_EDGE ( 'NONE', *, *, #25760, .F. ) ;
#25402=CARTESIAN_POINT ( 'NONE',  ( 67.88769211468458309, 58.75904380331535037, -3.964697573200774539 ) ) ;
#25415=CARTESIAN_POINT ( 'NONE',  ( 78.32432613507506858, 65.79895565947732905, -1.640065189519639199 ) ) ;
#25419=CARTESIAN_POINT ( 'NONE',  ( 81.57183863170791938, 63.40013557971743552, -3.079343812547459702 ) ) ;
#25420=CARTESIAN_POINT ( 'NONE',  ( 80.27814043029276547, 62.51814696698978935, 3.475409704257726329 ) ) ;
#25422=CARTESIAN_POINT ( 'NONE',  ( 81.74784679736075077, 61.69507302169112251, 1.000000000000000000 ) ) ;
#25423=CARTESIAN_POINT ( 'NONE',  ( -64.08758708073990817, 43.25085652376020562, 2.908220996737135966 ) ) ;
#25438=CARTESIAN_POINT ( 'NONE',  ( -59.99245622168610481, 24.84364830758654463, -9.341017543843770810 ) ) ;
#25447=CARTESIAN_POINT ( 'NONE',  ( 66.89278707744533392, 57.85779714042387667, 3.998112125421894980 ) ) ;
#25462=CARTESIAN_POINT ( 'NONE',  ( 80.26059561567515743, 63.13455243780963144, -3.653685850874238028 ) ) ;
#25464=CARTESIAN_POINT ( 'NONE',  ( 80.89855423268610934, 61.90964448260509556, 2.818206040476791241 ) ) ;
#25468=CARTESIAN_POINT ( 'NONE',  ( -57.66410233176053879, 30.21301966603896361, 4.063147710751544572 ) ) ;
#25472=CARTESIAN_POINT ( 'NONE',  ( -54.79610818216035995, 31.51396769785353058, 1.028877969214415433 ) ) ;
#25481=DIRECTION ( 'NONE',  ( -0.000000000000000000, -0.000000000000000000, 1.000000000000000000 ) ) ;
#25482=CARTESIAN_POINT ( 'NONE',  ( 78.94073822560471854, 66.07870154842754573, 1.754135932968020173 ) ) ;
#25486=CARTESIAN_POINT ( 'NONE',  ( -66.12008681484671513, 35.44165918782573499, 8.117242773420016988 ) ) ;
#25498=CARTESIAN_POINT ( 'NONE',  ( 80.38786582577539264, 64.30167536105096815, -3.588566286536287731 ) ) ;
#25503=AXIS2_PLACEMENT_3D ( 'NONE', #12357, #14824, #21433 ) ;
#25511=CARTESIAN_POINT ( 'NONE',  ( 78.61848929481175219, 66.00753381999014380, -1.284346554836964582 ) ) ;
#25516=CARTESIAN_POINT ( 'NONE',  ( 80.02452723347238361, 66.12521016146372688, -2.110636331688537037 ) ) ;
#25524=CARTESIAN_POINT ( 'NONE',  ( 70.76671532128065678, 59.91573877893261368, 3.942344351592494966 ) ) ;
#25532=CARTESIAN_POINT ( 'NONE',  ( -64.08758708074093136, 41.04287353446839859, -3.000000000000000000 ) ) ;
#25534=CARTESIAN_POINT ( 'NONE',  ( 79.96642255694898438, 65.80764937176724061, 2.611089443243009178 ) ) ;
#25541=EDGE_CURVE ( 'NONE', #34099, #19152, #29103, .T. ) ;
#25552=CIRCLE ( 'NONE', #22984, 3.000000000000002220 ) ;
#25554=CARTESIAN_POINT ( 'NONE',  ( 66.68811621373450294, 57.96620201306357956, -3.998609561968404336 ) ) ;
#25555=ORIENTED_EDGE ( 'NONE', *, *, #910, .T. ) ;
#25562=CARTESIAN_POINT ( 'NONE',  ( 82.41151909044420165, 62.85445852417072388, -1.451695327222927379 ) ) ;
#25563=CARTESIAN_POINT ( 'NONE',  ( 80.59816347408094828, 62.94305116675476341, 3.503057693382590099 ) ) ;
#25567=CARTESIAN_POINT ( 'NONE',  ( 74.72645207833699033, 61.69672356374137223, -3.865308561588413738 ) ) ;
#25568=DIRECTION ( 'NONE',  ( 0.4582725098355704407, -0.8888117386314197121, 3.083685177455368914E-15 ) ) ;
#25569=CARTESIAN_POINT ( 'NONE',  ( -59.01947560891952804, 27.90920910948504385, -46.17089178453873188 ) ) ;
#25571=CARTESIAN_POINT ( 'NONE',  ( 81.36058090587512481, 62.33601367849696118, -2.816708194897771911 ) ) ;
#25572=CARTESIAN_POINT ( 'NONE',  ( 77.53347081925228679, 60.09046002684877408, 2.805892758502874340 ) ) ;
#25577=CARTESIAN_POINT ( 'NONE',  ( 78.94658775073220625, 66.18447242754098170, 1.227604746834740856 ) ) ;
#25598=CARTESIAN_POINT ( 'NONE',  ( 68.05544300132015678, 58.31078564718745127, -3.995571880668737474 ) ) ;
#25610=CARTESIAN_POINT ( 'NONE',  ( 79.25894186866877078, 65.67357942822117423, 2.700485128497465137 ) ) ;
#25614=CARTESIAN_POINT ( 'NONE',  ( 80.06304181921890972, 62.74582375469539386, -3.589982250315065127 ) ) ;
#25617=CARTESIAN_POINT ( 'NONE',  ( 81.69067057342168425, 62.21317191938595670, -2.410848004503902242 ) ) ;
#25618=CARTESIAN_POINT ( 'NONE',  ( 80.68211079047073042, 61.32331416546044522, 2.218931858625937004 ) ) ;
#25623=CARTESIAN_POINT ( 'NONE',  ( -63.53025880882105980, 43.42181481381274466, 3.125110315362289892 ) ) ;
#25634=EDGE_CURVE ( 'NONE', #2581, #2062, #32130, .T. ) ;
#25639=CARTESIAN_POINT ( 'NONE',  ( -75.45330471031414277, 33.71485196875532608, 8.800414904976364028 ) ) ;
#25646=ORIENTED_EDGE ( 'NONE', *, *, #20824, .T. ) ;
#25647=CARTESIAN_POINT ( 'NONE',  ( 66.73227421799262515, 57.84320248636868200, 3.999246569070631363 ) ) ;
#25652=VERTEX_POINT ( 'NONE', #16527 ) ;
#25662=CARTESIAN_POINT ( 'NONE',  ( 80.87650043350832618, 61.69514696456053571, -2.603857329607536464 ) ) ;
#25664=CARTESIAN_POINT ( 'NONE',  ( 81.04520860822712791, 61.30615853997439046, 1.682919622592479625 ) ) ;
#25675=CARTESIAN_POINT ( 'NONE',  ( -63.84700662236061675, 35.83977057131340871, -7.343444254795444159 ) ) ;
#25678=CARTESIAN_POINT ( 'NONE',  ( -74.92283640148284007, 18.87330372387142674, 9.800414904976365804 ) ) ;
#25683=CARTESIAN_POINT ( 'NONE',  ( 79.64653587341234697, 65.62447382577090593, 2.816708194897748374 ) ) ;
#25693=CARTESIAN_POINT ( 'NONE',  ( 68.66337269546751543, 58.46565884629779930, 3.990501929453249108 ) ) ;
#25696=CARTESIAN_POINT ( 'NONE',  ( 72.29787722903529357, 59.46803282872462404, -3.909340765805334961 ) ) ;
#25700=CARTESIAN_POINT ( 'NONE',  ( 81.25428736789774575, 61.63226232517330061, -2.112861953993772968 ) ) ;
#25711=CARTESIAN_POINT ( 'NONE',  ( 80.23783879855322709, 63.84144632218769999, -3.668443954219269276 ) ) ;
#25721=CARTESIAN_POINT ( 'NONE',  ( -58.94134291052900920, 28.40740006353605906, -6.287813344559351592 ) ) ;
#25724=CARTESIAN_POINT ( 'NONE',  ( -64.08758708074093136, 43.61223003902852469, -1.151575380241328439 ) ) ;
#25725=CARTESIAN_POINT ( 'NONE',  ( 71.26393988290669768, 58.68354208002635630, 3.837797619696095897 ) ) ;
#25733=CARTESIAN_POINT ( 'NONE',  ( 81.64001200210110198, 62.74592715519806774, 2.852119850618822117 ) ) ;
#25736=ORIENTED_EDGE ( 'NONE', *, *, #11131, .T. ) ;
#25750=VECTOR ( 'NONE', #18116, 1000.000000000000114 ) ;
#25751=CYLINDRICAL_SURFACE ( 'NONE', #14048, 95.38357402481355507 ) ;
#25756=CARTESIAN_POINT ( 'NONE',  ( 66.68517307240369973, 57.97439930951417608, -3.998354769216140525 ) ) ;
#25757=EDGE_CURVE ( 'NONE', #29308, #1802, #18561, .T. ) ;
#25760=EDGE_CURVE ( 'NONE', #17865, #12529, #6095, .T. ) ;
#25762=CARTESIAN_POINT ( 'NONE',  ( -64.85784325972055342, 34.81586596186931359, 6.466735817496056526 ) ) ;
#25769=CARTESIAN_POINT ( 'NONE',  ( 81.44533364721141311, 61.45470812716253306, -1.173033592341551579 ) ) ;
#25772=CARTESIAN_POINT ( 'NONE',  ( 74.72764284544139457, 63.14151651683601330, -3.204585025132376419 ) ) ;
#25776=CARTESIAN_POINT ( 'NONE',  ( 76.03108743707696249, 63.27561679962268215, 3.498861892150627373 ) ) ;
#25777=VERTEX_POINT ( 'NONE', #36096 ) ;
#25782=CARTESIAN_POINT ( 'NONE',  ( 81.43190433112084747, 61.44807093728565661, 1.203271478923120696 ) ) ;
#25784=CARTESIAN_POINT ( 'NONE',  ( -64.08758708074093136, 43.61223004741322740, 1.151969611512877467 ) ) ;
#25790=CARTESIAN_POINT ( 'NONE',  ( 27.60344192425479193, 81.15229837709949834, -4.000000000000000000 ) ) ;
#25802=CARTESIAN_POINT ( 'NONE',  ( 67.76947924466990969, 58.18518750870053680, -3.996132678073307964 ) ) ;
#25804=CARTESIAN_POINT ( 'NONE',  ( 28.52663967383706023, 50.14399159706753295, -1.000000000000000000 ) ) ;
#25805=CYLINDRICAL_SURFACE ( 'NONE', #30504, 0.9999999999999977796 ) ;
#25817=CARTESIAN_POINT ( 'NONE',  ( 79.96011558216464721, 64.80970700093439518, 3.432259906339278022 ) ) ;
#25821=CARTESIAN_POINT ( 'NONE',  ( 80.07249602437107683, 61.49066053983646896, -2.889371261047466000 ) ) ;
#25824=CARTESIAN_POINT ( 'NONE',  ( 80.02729359676482090, 65.84138187185882884, -2.563845612518027117 ) ) ;
#25825=CARTESIAN_POINT ( 'NONE',  ( 78.07544678589873399, 65.62285883043881540, 1.832491541757240494 ) ) ;
#25827=CARTESIAN_POINT ( 'NONE',  ( 80.36293583174433763, 66.30725055998102846, 1.299258709308648729 ) ) ;
#25828=CARTESIAN_POINT ( 'NONE',  ( -63.68258360981171506, 44.25809753515871137, 1.883067893878278998 ) ) ;
#25829=ORIENTED_EDGE ( 'NONE', *, *, #1351, .T. ) ;
#25851=ORIENTED_EDGE ( 'NONE', *, *, #29231, .F. ) ;
#25854=CARTESIAN_POINT ( 'NONE',  ( 66.56005047484954673, 57.86167872611329699, 3.999845987730311858 ) ) ;
#25865=CARTESIAN_POINT ( 'NONE',  ( 80.24949846641645479, 62.81397012663808255, -3.564905221331803098 ) ) ;
#25867=CARTESIAN_POINT ( 'NONE',  ( 80.78018476400359305, 61.88220158024267903, 2.864416008774245626 ) ) ;
#25875=CARTESIAN_POINT ( 'NONE',  ( -80.78329181448161478, 33.71485196875532608, -8.800414904976364028 ) ) ;
#25880=CARTESIAN_POINT ( 'NONE',  ( -72.95330471031414277, 33.71485196875532608, -8.800414904976364028 ) ) ;
#25885=CARTESIAN_POINT ( 'NONE',  ( 81.36058090587516745, 62.33601367849698249, 2.816708194897752815 ) ) ;
#25887=LINE ( 'NONE', #19303, #8840 ) ;
#25893=FACE_OUTER_BOUND ( 'NONE', #3522, .T. ) ;
#25898=CARTESIAN_POINT ( 'NONE',  ( 68.59886892412534110, 58.63590986220410173, 3.993768376023888234 ) ) ;
#25904=CARTESIAN_POINT ( 'NONE',  ( 80.70080623961231936, 63.70112813535636320, -3.588566286536281069 ) ) ;
#25911=AXIS2_PLACEMENT_3D ( 'NONE', #24584, #8515, #24377 ) ;
#25916=CARTESIAN_POINT ( 'NONE',  ( 80.57397677244573231, 62.93365480201026685, -3.508091314521179171 ) ) ;
#25921=CARTESIAN_POINT ( 'NONE',  ( 79.97870788650297413, 66.10023056730543090, -2.166533184762310604 ) ) ;
#25928=CARTESIAN_POINT ( 'NONE',  ( 70.86714415968630476, 59.66805877367134769, 3.971832046809244510 ) ) ;
#25937=CARTESIAN_POINT ( 'NONE',  ( 81.55127126995144238, 61.75833066296597451, 1.907437723464473711 ) ) ;
#25955=DIRECTION ( 'NONE',  ( 0.000000000000000000, 0.000000000000000000, 1.000000000000000000 ) ) ;
#25971=CARTESIAN_POINT ( 'NONE',  ( 81.96987370863051581, 65.13652322159772723, -1.905332024691357429 ) ) ;
#25976=CARTESIAN_POINT ( 'NONE',  ( 75.42787669100914627, 61.66269772210893763, -3.901127667181031100 ) ) ;
#25977=PLANE ( 'NONE',  #39032 ) ;
#25980=CARTESIAN_POINT ( 'NONE',  ( 77.82713238777958509, 60.98268764611925974, 3.435658781984941346 ) ) ;
#25986=CARTESIAN_POINT ( 'NONE',  ( 80.91683595914895477, 65.70075836866587338, 2.460680857248573883 ) ) ;
#25987=CARTESIAN_POINT ( 'NONE',  ( -64.08758708074093136, 43.61223004741322740, 1.000000000000000000 ) ) ;
#25995=EDGE_CURVE ( 'NONE', #26563, #22837, #3198, .T. ) ;
#26010=EDGE_CURVE ( 'NONE', #7366, #23047, #14007, .T. ) ;
#26011=CARTESIAN_POINT ( 'NONE',  ( 67.77942698303134250, 58.15829091545840157, -3.995247128881093790 ) ) ;
#26022=CARTESIAN_POINT ( 'NONE',  ( 78.75316082766835279, 66.06368344870412557, 1.496866203714574572 ) ) ;
#26025=CARTESIAN_POINT ( 'NONE',  ( 78.19628368166274868, 65.45398019160434444, -2.372109611208335078 ) ) ;
#26028=CARTESIAN_POINT ( 'NONE',  ( 78.84958593098521362, 66.12877247161736705, -1.370814772365197554 ) ) ;
#26029=CARTESIAN_POINT ( 'NONE',  ( 80.40236172895532718, 61.11465044667751556, 2.108843360059433625 ) ) ;
#26034=CARTESIAN_POINT ( 'NONE',  ( 82.54681503119226704, 63.20390409618732974, 1.263752851812355305 ) ) ;
#26035=CARTESIAN_POINT ( 'NONE',  ( -64.08758708074091714, 41.79071634614418684, 3.815532762722622095 ) ) ;
#26037=CARTESIAN_POINT ( 'NONE',  ( -63.39880662924674226, 35.63549842397627998, -6.795986594146541826 ) ) ;
#26061=CARTESIAN_POINT ( 'NONE',  ( 66.70872257673579497, 57.90880667275003901, 3.999713739233790921 ) ) ;
#26075=CARTESIAN_POINT ( 'NONE',  ( 80.83921286824487140, 61.18398161863571971, -1.552792442904344261 ) ) ;
#26077=CARTESIAN_POINT ( 'NONE',  ( 78.63837616148850884, 65.82632162494860495, 2.064111563736254595 ) ) ;
#26094=CARTESIAN_POINT ( 'NONE',  ( 81.20101650719863073, 62.86240828450105766, 3.233552917234625124 ) ) ;
#26096=( BOUNDED_SURFACE ( )  B_SPLINE_SURFACE ( 3, 2, ( 
 ( #28147, #19091, #38218 ),
 ( #19293, #6742, #31860 ),
 ( #25675, #12704, #12908 ),
 ( #40701, #10015, #12503 ) ),
 .UNSPECIFIED., .F., .F., .F. ) 
 B_SPLINE_SURFACE_WITH_KNOTS ( ( 4, 4 ),
 ( 3, 3 ),
 ( 1.734723475976807094E-18, 0.0006385966863608955914 ),
 ( 0.000000000000000000, 1.000000000000000000 ),
 .UNSPECIFIED. ) 
 GEOMETRIC_REPRESENTATION_ITEM ( )  RATIONAL_B_SPLINE_SURFACE ( (
 ( 1.000000000000000000, 0.5652620711642704077, 1.000000000000000000),
 ( 1.000000000000000000, 0.5746205253747180830, 1.000000000000000000),
 ( 1.000000000000000000, 0.5840949208454062624, 1.000000000000000000),
 ( 1.000000000000000000, 0.5935057080259644735, 1.000000000000000000) ) ) 
 REPRESENTATION_ITEM ( '' )  SURFACE ( )  );
#26113=CARTESIAN_POINT ( 'NONE',  ( 79.42059605865689775, 65.48104909687435793, -2.923497156821688314 ) ) ;
#26116=CARTESIAN_POINT ( 'NONE',  ( -57.65239026484333351, 32.60637517809080066, 4.103028154974615482 ) ) ;
#26119=EDGE_LOOP ( 'NONE', ( #15679, #34648, #19371 ) ) ;
#26123=CARTESIAN_POINT ( 'NONE',  ( 80.15465141033460839, 63.79803065853134569, -3.683925914261567680 ) ) ;
#26130=FACE_OUTER_BOUND ( 'NONE', #7419, .T. ) ;
#26134=CARTESIAN_POINT ( 'NONE',  ( 70.90076320674430121, 59.58500768881799559, 3.976054184260641833 ) ) ;
#26143=CARTESIAN_POINT ( 'NONE',  ( 79.04416262434369855, 66.14279969385417246, 1.662073781718003351 ) ) ;
#26161=DIRECTION ( 'NONE',  ( -1.000000000000000000, 0.000000000000000000, 0.000000000000000000 ) ) ;
#26166=CARTESIAN_POINT ( 'NONE',  ( -62.81463675898083210, 36.67811266762162603, -4.600311178732273021 ) ) ;
#26171=CARTESIAN_POINT ( 'NONE',  ( -57.02355111755383632, 29.45914411650375442, -1.982879248426652863 ) ) ;
#26176=CARTESIAN_POINT ( 'NONE',  ( 81.67240355425528264, 65.37253450681788536, -2.134985007310160832 ) ) ;
#26180=CARTESIAN_POINT ( 'NONE',  ( 75.46848212330048966, 60.05767933327602748, -3.584990529380367441 ) ) ;
#26185=CARTESIAN_POINT ( 'NONE',  ( 75.30130074865816425, 63.36357894040062178, 3.230144225280452641 ) ) ;
#26186=CIRCLE ( 'NONE', #24856, 1.000000000000000222 ) ;
#26188=CARTESIAN_POINT ( 'NONE',  ( -64.08758708074093136, 36.87876644325631759, 4.900609702795903466 ) ) ;
#26193=CARTESIAN_POINT ( 'NONE',  ( 80.13359286145602312, 66.18419574793108495, 1.944145319385262471 ) ) ;
#26201=CARTESIAN_POINT ( 'NONE',  ( 1.847632973160104664, 12.44248440543094958, -7.000000000000000000 ) ) ;
#26207=AXIS2_PLACEMENT_3D ( 'NONE', #4520, #36202, #34872 ) ;
#26215=CARTESIAN_POINT ( 'NONE',  ( 67.49481586879284123, 58.02828806359071478, -3.995059460290581121 ) ) ;
#26225=ORIENTED_EDGE ( 'NONE', *, *, #25291, .T. ) ;
#26228=CARTESIAN_POINT ( 'NONE',  ( 81.17453961776598703, 62.25628865055540473, 2.899379378185771738 ) ) ;
#26232=CARTESIAN_POINT ( 'NONE',  ( 79.07090634323701295, 63.55465448991838429, -3.774260586041105370 ) ) ;
#26237=CARTESIAN_POINT ( 'NONE',  ( 81.29034902432738363, 64.00233822786356086, -3.292658836668130196 ) ) ;
#26238=CARTESIAN_POINT ( 'NONE',  ( 80.62600653171161014, 61.47375110407241294, 2.475680338657083812 ) ) ;
#26240=CARTESIAN_POINT ( 'NONE',  ( 82.51683713915190310, 64.24667231656799515, 1.319711737399753781 ) ) ;
#26245=CARTESIAN_POINT ( 'NONE',  ( -62.76544114002936681, 35.76323014769233311, -5.464922856233972226 ) ) ;
#26263=EDGE_LOOP ( 'NONE', ( #18085, #6160, #23222, #15441 ) ) ;
#26264=CARTESIAN_POINT ( 'NONE',  ( 66.84168730393145097, 57.99964773888063974, 3.999029912551661070 ) ) ;
#26266=DIRECTION ( 'NONE',  ( 0.4582725098355734938, -0.8888117386314180468, 0.000000000000000000 ) ) ;
#26277=ORIENTED_EDGE ( 'NONE', *, *, #37499, .F. ) ;
#26278=CARTESIAN_POINT ( 'NONE',  ( 79.84106601136197412, 63.63461245521319398, -3.725738571856551662 ) ) ;
#26280=CARTESIAN_POINT ( 'NONE',  ( 80.95177907874119683, 61.22464621339454283, 1.448968528257557287 ) ) ;
#26289=CARTESIAN_POINT ( 'NONE',  ( 67.37492487370475658, 58.42787741793769385, -4.000000000000127898 ) ) ;
#26292=CARTESIAN_POINT ( 'NONE',  ( -63.08758708074093136, -21.25669541281728669, 3.000000000000000000 ) ) ;
#26296=CARTESIAN_POINT ( 'NONE',  ( 81.33630325801044592, 62.05105258569627580, 2.628317182735721680 ) ) ;
#26307=CARTESIAN_POINT ( 'NONE',  ( 68.51828301517210207, 58.84837915819282728, 3.980709302925309778 ) ) ;
#26311=CARTESIAN_POINT ( 'NONE',  ( 81.17805228937325523, 61.98952396227124950, -2.700485128497477572 ) ) ;
#26322=CARTESIAN_POINT ( 'NONE',  ( 80.65169068708779321, 62.63775009584335152, -3.403428918328328834 ) ) ;
#26324=CARTESIAN_POINT ( 'NONE',  ( 81.01565502672983143, 61.93906859853276359, 2.769656700700043217 ) ) ;
#26328=EDGE_CURVE ( 'NONE', #27835, #35702, #39468, .T. ) ;
#26331=( BOUNDED_CURVE ( )  B_SPLINE_CURVE ( 3, ( #39197, #14290, #36332, #30572 ),
 .UNSPECIFIED., .F., .T. ) 
 B_SPLINE_CURVE_WITH_KNOTS ( ( 4, 4 ),
 ( 0.7028477130386120431, 1.570796326794896558 ),
 .UNSPECIFIED. ) 
 CURVE ( )  GEOMETRIC_REPRESENTATION_ITEM ( )  RATIONAL_B_SPLINE_CURVE ( ( 1.000000000000000000, 0.9382012019593851671, 0.9382012019593851671, 1.000000000000000000 ) ) 
 REPRESENTATION_ITEM ( '' )  );
#26332=CARTESIAN_POINT ( 'NONE',  ( -58.47571659425080526, 29.43362125246419936, -5.129074445220336287 ) ) ;
#26334=DIRECTION ( 'NONE',  ( 1.000000000000000000, 0.000000000000000000, 0.000000000000000000 ) ) ;
#26336=CARTESIAN_POINT ( 'NONE',  ( -64.08758708074093136, 43.97597776728673580, -1.778916918605509823 ) ) ;
#26337=DIRECTION ( 'NONE',  ( 0.000000000000000000, 0.000000000000000000, 1.000000000000000000 ) ) ;
#26338=EDGE_LOOP ( 'NONE', ( #19064, #11369, #6118, #8205 ) ) ;
#26340=ORIENTED_EDGE ( 'NONE', *, *, #14908, .T. ) ;
#26346=CARTESIAN_POINT ( 'NONE',  ( 81.65590348734941983, 63.08388229440976858, 2.971291902561975284 ) ) ;
#26369=AXIS2_PLACEMENT_3D ( 'NONE', #36375, #7957, #24002 ) ;
#26378=CARTESIAN_POINT ( 'NONE',  ( 82.35726419014388000, 62.82676667106976254, -1.646077502936215797 ) ) ;
#26385=CARTESIAN_POINT ( 'NONE',  ( 76.81217388538114221, 61.66049381551723485, 3.848392762315859361 ) ) ;
#26386=ORIENTED_EDGE ( 'NONE', *, *, #40387, .T. ) ;
#26394=CARTESIAN_POINT ( 'NONE',  ( 82.01669802222870942, 64.37834105533568163, 2.512558077907662391 ) ) ;
#26401=CARTESIAN_POINT ( 'NONE',  ( 78.20309482563492054, 60.29564352725032705, 2.640401424216431092 ) ) ;
#26408=ADVANCED_FACE ( 'NONE', ( #20951 ), #32912, .T. ) ;
#26409=DIRECTION ( 'NONE',  ( -0.9267318687906785923, 0.3757233601570932335, 2.607104533349591435E-15 ) ) ;
#26410=ORIENTED_EDGE ( 'NONE', *, *, #2780, .T. ) ;
#26413=CARTESIAN_POINT ( 'NONE',  ( 67.65011695904739497, 58.50773134691538502, -3.985511447369839644 ) ) ;
#26426=CARTESIAN_POINT ( 'NONE',  ( 80.92403995952693663, 62.73960429493249791, 3.332694751021842094 ) ) ;
#26431=CARTESIAN_POINT ( 'NONE',  ( 78.07232077886961008, 65.35672112437505632, -2.431999527814446171 ) ) ;
#26434=CARTESIAN_POINT ( 'NONE',  ( 81.42106526724015225, 61.53660244640850863, -1.679744683809659467 ) ) ;
#26435=CARTESIAN_POINT ( 'NONE',  ( 80.49182418769538572, 61.81278841749719533, 2.961936469198068078 ) ) ;
#26438=CARTESIAN_POINT ( 'NONE',  ( 82.09527124944457910, 65.20214329949105547, 1.328060019257126356 ) ) ;
#26441=CARTESIAN_POINT ( 'NONE',  ( -64.26379470914697833, 34.82012742686825391, -5.122105205699029717 ) ) ;
#26445=ADVANCED_FACE ( 'NONE', ( #31402 ), #12854, .F. ) ;
#26450=DIRECTION ( 'NONE',  ( 0.000000000000000000, 0.000000000000000000, -1.000000000000000000 ) ) ;
#26457=CARTESIAN_POINT ( 'NONE',  ( 66.27376694608996388, 57.73522568913447373, 4.000000000000000000 ) ) ;
#26459=CARTESIAN_POINT ( 'NONE',  ( 71.06822368831490166, 59.17031991972731930, -3.954977122261625233 ) ) ;
#26460=CIRCLE ( 'NONE', #1485, 64.42751648247021024 ) ;
#26465=SHAPE_DEFINITION_REPRESENTATION ( #17779, #19830 ) ;
#26471=ADVANCED_FACE ( 'NONE', ( #9969 ), #3624, .T. ) ;
#26473=CARTESIAN_POINT ( 'NONE',  ( 80.42678074443089997, 62.56544727678156903, -3.449595662144188779 ) ) ;
#26475=CARTESIAN_POINT ( 'NONE',  ( 79.03665253560659210, 65.17130141867527016, 3.087291694836687306 ) ) ;
#26484=CARTESIAN_POINT ( 'NONE',  ( 70.64516890162954610, 60.54534949351131701, -3.764670254805445371 ) ) ;
#26492=CARTESIAN_POINT ( 'NONE',  ( 81.29039616289740877, 62.30485139745668732, 2.850064543546685591 ) ) ;
#26494=DIRECTION ( 'NONE',  ( 0.000000000000000000, 0.000000000000000000, 1.000000000000000000 ) ) ;
#26502=CARTESIAN_POINT ( 'NONE',  ( 69.37860636825551808, 58.34396603459876474, 3.943722715026767300 ) ) ;
#26508=CARTESIAN_POINT ( 'NONE',  ( 80.23319818986581708, 64.21721675003155383, -3.633989118465185353 ) ) ;
#26511=CARTESIAN_POINT ( 'NONE',  ( -58.86630245980595788, 29.17574657131979521, 6.015288659391247350 ) ) ;
#26512=ORIENTED_EDGE ( 'NONE', *, *, #8241, .F. ) ;
#26514=CARTESIAN_POINT ( 'NONE',  ( -64.08758708074093136, 43.61223004741322740, -8.800414904976381791 ) ) ;
#26517=CARTESIAN_POINT ( 'NONE',  ( 78.67172310627755394, 65.99640245491987400, -1.621665796799209636 ) ) ;
#26519=CARTESIAN_POINT ( 'NONE',  ( 81.07009230622236373, 61.73904331373560694, 2.506402126386315654 ) ) ;
#26527=CARTESIAN_POINT ( 'NONE',  ( -63.63041988795695403, 43.97068632168673474, -2.480371489381162586 ) ) ;
#26537=CARTESIAN_POINT ( 'NONE',  ( 79.37811825733636795, 65.99825290327245852, 2.263370276488442911 ) ) ;
#26551=EDGE_CURVE ( 'NONE', #30676, #31330, #39656, .T. ) ;
#26560=CARTESIAN_POINT ( 'NONE',  ( 66.27376694609004915, 57.73522568913436004, -4.000000000000000000 ) ) ;
#26563=VERTEX_POINT ( 'NONE', #21906 ) ;
#26567=CARTESIAN_POINT ( 'NONE',  ( -57.65239026484333351, 32.60637517809080066, -4.103028154974615482 ) ) ;
#26571=CARTESIAN_POINT ( 'NONE',  ( 79.65107971589624469, 66.31509156740916922, -1.306649493517272553 ) ) ;
#26577=CARTESIAN_POINT ( 'NONE',  ( 74.98537949548503434, 62.60475170799649192, 3.615102801931181276 ) ) ;
#26586=CARTESIAN_POINT ( 'NONE',  ( 81.16771000429746152, 61.30329618601649599, 1.041818241550642954 ) ) ;
#26597=FACE_OUTER_BOUND ( 'NONE', #2439, .T. ) ;
#26599=CARTESIAN_POINT ( 'NONE',  ( -72.95330471031414277, 33.71485196875532608, 12.49999999999999645 ) ) ;
#26607=CARTESIAN_POINT ( 'NONE',  ( 67.40765644887963504, 58.26613713413648554, -3.996173465816880377 ) ) ;
#26611=VECTOR ( 'NONE', #8793, 1000.000000000000000 ) ;
#26612=B_SPLINE_CURVE_WITH_KNOTS ( 'NONE', 3,
 ( #10424, #26289, #29170, #26484, #13516, #7934, #20285, #23000, #39011, #23592, #1575, #32465, #23190, #14107, #4264, #4656, #10614, #35565, #4470, #13723, #29369, #26685 ),
 .UNSPECIFIED., .F., .F.,
 ( 4, 2, 2, 2, 2, 2, 2, 2, 2, 2, 4 ),
 ( -7.124770226877074144E-05, 0.003831421772206580582, 0.007734091246681932055, 0.009685425983919597817, 0.01163676072115726184, 0.01261242808977608952, 0.01358809545839491720, 0.01456376282701374487, 0.01505159651132314397, 0.01529551335347784438, 0.01553943019563254133 ),
 .UNSPECIFIED. ) ;
#26619=ORIENTED_EDGE ( 'NONE', *, *, #40387, .F. ) ;
#26622=CARTESIAN_POINT ( 'NONE',  ( 80.20683918224330000, 64.20264744734686246, 3.640670270625568694 ) ) ;
#26626=CARTESIAN_POINT ( 'NONE',  ( 79.50866325991145800, 61.15032965923182218, -2.842954625922232026 ) ) ;
#26629=CARTESIAN_POINT ( 'NONE',  ( 81.50569694087069195, 63.36683741555938809, -3.125353918834852696 ) ) ;
#26631=CARTESIAN_POINT ( 'NONE',  ( 79.89463791284350691, 61.88150425735624083, 3.258123098320697686 ) ) ;
#26634=CARTESIAN_POINT ( 'NONE',  ( 81.74417899799371412, 61.69322615925147346, 1.090531591958330937 ) ) ;
#26639=CARTESIAN_POINT ( 'NONE',  ( -64.85784325972053921, 34.81586596186942018, -6.466735817496056526 ) ) ;
#26644=ORIENTED_EDGE ( 'NONE', *, *, #33705, .T. ) ;
#26645=AXIS2_PLACEMENT_3D ( 'NONE', #35583, #38432, #9841 ) ;
#26649=B_SPLINE_CURVE_WITH_KNOTS ( 'NONE', 3,
 ( #37656, #9054, #12967, #6796, #9458, #3730, #21631, #34212, #18521, #19146 ),
 .UNSPECIFIED., .F., .F.,
 ( 4, 2, 2, 2, 4 ),
 ( 0.000000000000000000, 0.0003392619605000338277, 0.0005088929407500506060, 0.0005937084308750540350, 0.0006785239210000574639 ),
 .UNSPECIFIED. ) ;
#26659=CARTESIAN_POINT ( 'NONE',  ( 66.57179245706689130, 57.82874523672322908, 3.999903336035371293 ) ) ;
#26660=CARTESIAN_POINT ( 'NONE',  ( 71.95566904218743787, 60.28642714153433957, -3.942504219403032639 ) ) ;
#26673=CARTESIAN_POINT ( 'NONE',  ( 80.58270521159307975, 62.07868998654234360, -3.101774481621347945 ) ) ;
#26676=CARTESIAN_POINT ( 'NONE',  ( 78.47952394835844814, 65.90892955575914414, 1.487544896895793389 ) ) ;
#26685=CARTESIAN_POINT ( 'NONE',  ( 78.69038500580363404, 66.05859403932464602, -1.000000000000000000 ) ) ;
#26687=ORIENTED_EDGE ( 'NONE', *, *, #1494, .F. ) ;
#26692=CARTESIAN_POINT ( 'NONE',  ( 78.66788830423078593, 66.04261347698269446, 1.159471704397124547 ) ) ;
#26698=CARTESIAN_POINT ( 'NONE',  ( -64.19126555651345711, 34.97929361893064026, 4.821066086844552068 ) ) ;
#26703=CARTESIAN_POINT ( 'NONE',  ( 67.68985761519660116, 58.40038676363953840, 3.993918888840239934 ) ) ;
#26705=AXIS2_PLACEMENT_3D ( 'NONE', #20396, #5168, #2097 ) ;
#26708=CARTESIAN_POINT ( 'NONE',  ( 79.55838722571232324, 65.27247487857083286, -3.155412080370053385 ) ) ;
#26711=CARTESIAN_POINT ( 'NONE',  ( -57.26775771055920217, 29.21795897888089755, 2.148764163877427968 ) ) ;
#26718=CARTESIAN_POINT ( 'NONE',  ( 78.74908976354470269, 65.92676629176580150, -1.950029235564220809 ) ) ;
#26720=CARTESIAN_POINT ( 'NONE',  ( 79.27128227901764035, 65.37053819277495847, 2.988136994358710385 ) ) ;
#26740=CARTESIAN_POINT ( 'NONE',  ( 79.79491195507890211, 65.71105728010107327, 2.731335034814814211 ) ) ;
#26757=VERTEX_POINT ( 'NONE', #288 ) ;
#26762=CARTESIAN_POINT ( 'NONE',  ( 66.27376694609004915, 57.73522568913436004, -4.000000000000000000 ) ) ;
#26766=EDGE_LOOP ( 'NONE', ( #18515, #14577, #765, #31235 ) ) ;
#26775=CARTESIAN_POINT ( 'NONE',  ( 78.68971998042104588, 66.05812159354535140, -1.027726681410898957 ) ) ;
#26782=CARTESIAN_POINT ( 'NONE',  ( 74.67253486855700828, 63.25418332940030552, 3.074209570828856819 ) ) ;
#26784=CARTESIAN_POINT ( 'NONE',  ( -64.08758708074093136, 36.14363715547679590, 3.800414904976366692 ) ) ;
#26785=EDGE_CURVE ( 'NONE', #29308, #23344, #35034, .T. ) ;
#26791=CARTESIAN_POINT ( 'NONE',  ( 82.02157412789779301, 62.93630067300351527, 2.502189764415794215 ) ) ;
#26794=CIRCLE ( 'NONE', #29411, 31.02204673211315011 ) ;
#26799=DIRECTION ( 'NONE',  ( -0.4582725098355734938, 0.8888117386314180468, -0.000000000000000000 ) ) ;
#26808=CARTESIAN_POINT ( 'NONE',  ( 67.08924564209870312, 58.23032185317626386, -3.992323350375290403 ) ) ;
#26821=CARTESIAN_POINT ( 'NONE',  ( 80.71579011337402676, 63.33293116964227920, 3.563857694938810106 ) ) ;
#26822=CARTESIAN_POINT ( 'NONE',  ( -63.45510661405219821, 43.01213780119760344, 3.461531625003003487 ) ) ;
#26824=CARTESIAN_POINT ( 'NONE',  ( 79.13122682291697174, 61.20693062157209852, -3.102003663616897278 ) ) ;
#26827=CARTESIAN_POINT ( 'NONE',  ( 79.22754343384272602, 66.08014515008352419, -1.953285432042054293 ) ) ;
#26828=CARTESIAN_POINT ( 'NONE',  ( 79.32744125533960755, 63.05206431288016944, 3.774260586041107146 ) ) ;
#26833=CARTESIAN_POINT ( 'NONE',  ( 81.95295003160661906, 61.95651309483399416, 1.189854999565118421 ) ) ;
#26836=CARTESIAN_POINT ( 'NONE',  ( -62.77932549131168116, 36.45562188509678236, -4.736925958236502865 ) ) ;
#26840=CARTESIAN_POINT ( 'NONE',  ( 25.11437021580303863, 164.7550792202006562, 4.000000000000000000 ) ) ;
#26847=CARTESIAN_POINT ( 'NONE',  ( -64.08758708074093136, 41.04287353446839148, 3.000000000000000000 ) ) ;
#26854=CARTESIAN_POINT ( 'NONE',  ( 66.43484696874301676, 57.75462747860474622, 4.000000000000002665 ) ) ;
#26855=CARTESIAN_POINT ( 'NONE',  ( 73.82474952339838126, 59.08733682254641195, -3.476886323308218785 ) ) ;
#26867=CARTESIAN_POINT ( 'NONE',  ( 80.44079772350292501, 62.04115482339160792, -3.140153738741080058 ) ) ;
#26868=CARTESIAN_POINT ( 'NONE',  ( 80.44027647058022978, 62.28541378099806280, 3.311815948186458858 ) ) ;
#26886=CARTESIAN_POINT ( 'NONE',  ( 81.29933375999361544, 61.48586111389077757, 1.777114115212626189 ) ) ;
#26891=CARTESIAN_POINT ( 'NONE',  ( -64.52565643081008773, 34.68665887112012314, 5.852036696963947904 ) ) ;
#26894=CARTESIAN_POINT ( 'NONE',  ( 67.41558015167861129, 58.24452080056473591, 3.997009152755513384 ) ) ;
#26901=CARTESIAN_POINT ( 'NONE',  ( 81.19396390929411211, 61.77420168221062369, -2.442092683901112782 ) ) ;
#26904=CARTESIAN_POINT ( 'NONE',  ( -58.56870219631061758, 27.89510117891460439, 3.538387446898187072 ) ) ;
#26909=EDGE_CURVE ( 'NONE', #22985, #3507, #28980, .T. ) ;
#26910=ORIENTED_EDGE ( 'NONE', *, *, #33189, .T. ) ;
#26911=CARTESIAN_POINT ( 'NONE',  ( 80.98641699598172750, 61.40056178693503597, -2.031354376635674086 ) ) ;
#26913=CARTESIAN_POINT ( 'NONE',  ( -73.45070404594234503, 38.65432087843067421, -8.800414904976364028 ) ) ;
#26914=CARTESIAN_POINT ( 'NONE',  ( 79.95665241583073168, 64.06168528317471100, 3.692178340560209548 ) ) ;
#26916=CARTESIAN_POINT ( 'NONE',  ( -59.93345510331042902, 24.73247967741478703, -46.17089178453873188 ) ) ;
#26918=CARTESIAN_POINT ( 'NONE',  ( 76.61572510735733488, 60.58450557137939541, -3.562065002338889119 ) ) ;
#26928=CARTESIAN_POINT ( 'NONE',  ( 9.703489126596460679, 56.50623631086180154, 4.000000000000000000 ) ) ;
#26932=CARTESIAN_POINT ( 'NONE',  ( 81.29424054903499552, 63.61798189665044134, 3.316380171285405076 ) ) ;
#26956=CARTESIAN_POINT ( 'NONE',  ( -75.45330471031414277, 33.71485196875532608, -9.800414904976365804 ) ) ;
#26958=EDGE_CURVE ( 'NONE', #11154, #18734, #26460, .T. ) ;
#26965=CARTESIAN_POINT ( 'NONE',  ( -58.97431419818038734, 27.59684639285645247, -7.041158924856742551 ) ) ;
#26971=CARTESIAN_POINT ( 'NONE',  ( 81.43190433112079063, 61.44807093728562819, -1.203271478923240601 ) ) ;
#26972=AXIS2_PLACEMENT_3D ( 'NONE', #28009, #15451, #12368 ) ;
#26973=DIRECTION ( 'NONE',  ( -1.000000000000000000, 0.000000000000000000, 0.000000000000000000 ) ) ;
#26978=CARTESIAN_POINT ( 'NONE',  ( 75.21236926079949114, 60.63031288236823002, 3.833662259905124436 ) ) ;
#26984=CARTESIAN_POINT ( 'NONE',  ( -63.05329786184842078, 35.53802554122869850, 6.297540867206088855 ) ) ;
#26986=CARTESIAN_POINT ( 'NONE',  ( 79.14825301983928796, 66.20254961713405351, 1.551099981298356134 ) ) ;
#26989=CIRCLE ( 'NONE', #28999, 0.9999999999999998890 ) ;
#26997=ADVANCED_FACE ( 'NONE', ( #12157 ), #36971, .T. ) ;
#26998=CARTESIAN_POINT ( 'NONE',  ( -63.08379346057684245, 18.80112958435945458, -12.49999999999999645 ) ) ;
#27005=CARTESIAN_POINT ( 'NONE',  ( 67.39973655466486946, 58.28774108029888623, -3.995059460290581121 ) ) ;
#27019=CARTESIAN_POINT ( 'NONE',  ( 82.34614708994676846, 62.54074552962156019, -1.204231967108631007 ) ) ;
#27020=CARTESIAN_POINT ( 'NONE',  ( 80.26353224374042838, 64.23390916343181800, 3.625945587094182798 ) ) ;
#27023=CARTESIAN_POINT ( 'NONE',  ( 77.48714025262371763, 64.49898405264993073, -3.102003663616890172 ) ) ;
#27027=CARTESIAN_POINT ( 'NONE',  ( 79.79491195508184376, 65.71105728010222435, -2.731335034813057394 ) ) ;
#27029=CARTESIAN_POINT ( 'NONE',  ( 78.38159772055728070, 63.47233311668939848, 3.766285651913923171 ) ) ;
#27030=ORIENTED_EDGE ( 'NONE', *, *, #36633, .F. ) ;
#27033=CARTESIAN_POINT ( 'NONE',  ( 79.98571111508546494, 66.33520038980110201, 1.398807481800126595 ) ) ;
#27036=ORIENTED_EDGE ( 'NONE', *, *, #27961, .T. ) ;
#27046=CYLINDRICAL_SURFACE ( 'NONE', #23570, 7.999999999999986677 ) ;
#27058=CARTESIAN_POINT ( 'NONE',  ( 66.42099604079459141, 57.79375748135252877, 4.000000000000015099 ) ) ;
#27059=CARTESIAN_POINT ( 'NONE',  ( 72.08456622119051360, 59.97905947476213839, -3.962431611483851146 ) ) ;
#27074=DIRECTION ( 'NONE',  ( -0.000000000000000000, -0.000000000000000000, 1.000000000000000000 ) ) ;
#27075=ORIENTED_EDGE ( 'NONE', *, *, #39253, .F. ) ;
#27076=CARTESIAN_POINT ( 'NONE',  ( 79.93741260258519787, 63.33597468792986973, -3.730195463674648604 ) ) ;
#27078=CARTESIAN_POINT ( 'NONE',  ( 79.70081467235786477, 66.18075109116946919, -1.965143080302318879 ) ) ;
#27079=CARTESIAN_POINT ( 'NONE',  ( 80.83613523452670790, 61.24682340193511010, 1.855758959884430181 ) ) ;
#27080=CARTESIAN_POINT ( 'NONE',  ( -9.741734729663692249, 54.65020406074287251, 4.000000000000000000 ) ) ;
#27094=CARTESIAN_POINT ( 'NONE',  ( -64.36803618090942791, 34.71695719680190706, 5.457112545582705643 ) ) ;
#27098=CARTESIAN_POINT ( 'NONE',  ( 68.79143787039059532, 58.12720587843082853, 3.950303728398663949 ) ) ;
#27107=CARTESIAN_POINT ( 'NONE',  ( -57.13133194381639868, 29.70675091384940814, 4.151468609674973109 ) ) ;
#27112=CARTESIAN_POINT ( 'NONE',  ( 79.30978077413506355, 65.08723789429433282, -3.243225924683098338 ) ) ;
#27114=CARTESIAN_POINT ( 'NONE',  ( 80.93223178899255288, 61.91756539228708789, 2.804471013201325746 ) ) ;
#27116=AXIS2_PLACEMENT_3D ( 'NONE', #2594, #27476, #5044 ) ;
#27117=CARTESIAN_POINT ( 'NONE',  ( -58.99872204295122913, 28.54795728317057169, 6.891578894883348738 ) ) ;
#27120=CARTESIAN_POINT ( 'NONE',  ( 73.45088770829859470, 61.50831400533110127, -3.795548882783541522 ) ) ;
#27133=CARTESIAN_POINT ( 'NONE',  ( 78.83208086995101382, 66.11806168415743912, 1.392093260605097971 ) ) ;
#27136=ORIENTED_EDGE ( 'NONE', *, *, #21355, .T. ) ;
#27150=EDGE_LOOP ( 'NONE', ( #34592, #26910, #22652, #28480, #21974, #7977, #9856, #17068, #20045 ) ) ;
#27155=EDGE_LOOP ( 'NONE', ( #20244, #13701 ) ) ;
#27159=ORIENTED_EDGE ( 'NONE', *, *, #38294, .T. ) ;
#27161=CARTESIAN_POINT ( 'NONE',  ( 78.64144163184205638, 66.02383098553904972, -1.235082213173780419 ) ) ;
#27162=CARTESIAN_POINT ( 'NONE',  ( -58.66072975137505807, 29.93711237438063222, -5.396324374907178978 ) ) ;
#27167=CARTESIAN_POINT ( 'NONE',  ( 80.13359286145576732, 66.18419574793094284, -1.944145319385670589 ) ) ;
#27173=CARTESIAN_POINT ( 'NONE',  ( 76.92031397606373844, 59.90536750123394683, 2.950589020716061661 ) ) ;
#27182=CARTESIAN_POINT ( 'NONE',  ( 81.80618415539490229, 63.87961589575515120, 2.903340743335354190 ) ) ;
#27198=AXIS2_PLACEMENT_3D ( 'NONE', #34343, #31437, #3057 ) ;
#27204=CARTESIAN_POINT ( 'NONE',  ( 66.74110339505794798, 57.81860698948682398, -3.998609561963397674 ) ) ;
#27215=CARTESIAN_POINT ( 'NONE',  ( 79.00097698949592484, 66.21430696267364624, -1.000000000000000000 ) ) ;
#27217=CARTESIAN_POINT ( 'NONE',  ( 79.72815809223409644, 65.03555043453914664, 3.332694751021850976 ) ) ;
#27220=CARTESIAN_POINT ( 'NONE',  ( 77.20018789615933485, 65.00686241173515612, -2.285396881590235019 ) ) ;
#27223=CARTESIAN_POINT ( 'NONE',  ( 79.61430779865581542, 65.89704723538382325, -2.499697124808075710 ) ) ;
#27224=CARTESIAN_POINT ( 'NONE',  ( 78.26672476572065307, 63.69414582742362541, 3.691425412862291644 ) ) ;
#27225=VECTOR ( 'NONE', #34947, 1000.000000000000000 ) ;
#27228=CARTESIAN_POINT ( 'NONE',  ( 80.67264098608451661, 66.18930038384924330, 1.451695327222104703 ) ) ;
#27230=LINE ( 'NONE', #39796, #33444 ) ;
#27253=CARTESIAN_POINT ( 'NONE',  ( 66.41802798480563297, 57.80214248194133830, 4.000000000000018652 ) ) ;
#27254=CARTESIAN_POINT ( 'NONE',  ( 69.87460780774588898, 58.79389746341001199, -3.972683913566375402 ) ) ;
#27267=CARTESIAN_POINT ( 'NONE',  ( 78.59965762292412705, 65.58148208812491475, -2.436540443961504820 ) ) ;
#27269=CARTESIAN_POINT ( 'NONE',  ( 81.88543442889042012, 63.19940289366422803, -2.771525467262165421 ) ) ;
#27270=CARTESIAN_POINT ( 'NONE',  ( 78.50817655541952433, 65.71198414996337078, 2.174061886842030944 ) ) ;
#27276=CARTESIAN_POINT ( 'NONE',  ( -64.08758708074091714, 24.84364830758654108, -3.800414904976364028 ) ) ;
#27280=DIRECTION ( 'NONE',  ( -1.000000000000000000, 0.000000000000000000, 0.000000000000000000 ) ) ;
#27282=VECTOR ( 'NONE', #32655, 1000.000000000000000 ) ;
#27295=DIRECTION ( 'NONE',  ( -1.000000000000000000, 0.000000000000000000, 0.000000000000000000 ) ) ;
#27297=CARTESIAN_POINT ( 'NONE',  ( 67.88769211468458309, 58.75904380331535037, 3.964697573200772762 ) ) ;
#27313=CARTESIAN_POINT ( 'NONE',  ( 78.55684871931622126, 65.96378271911972035, -1.386845825021860490 ) ) ;
#27314=LINE ( 'NONE', #26913, #11508 ) ;
#27316=CARTESIAN_POINT ( 'NONE',  ( 79.53095237740791390, 64.90064992126237087, 3.392181771880189434 ) ) ;
#27320=CARTESIAN_POINT ( 'NONE',  ( 74.19779514372055473, 59.81543539827580958, -3.749455561448977736 ) ) ;
#27337=CARTESIAN_POINT ( 'NONE',  ( 81.53866496494931937, 61.91358381440762315, 2.246767365023751406 ) ) ;
#27346=CARTESIAN_POINT ( 'NONE',  ( -64.36865852185155745, 34.97220226750604866, -7.506047544094577084 ) ) ;
#27348=CARTESIAN_POINT ( 'NONE',  ( -62.81463675898083210, 36.67811266762162603, 4.600311178732273021 ) ) ;
#27355=CARTESIAN_POINT ( 'NONE',  ( 81.28781607649123941, 61.48165154268892252, -1.786209778413326621 ) ) ;
#27365=CARTESIAN_POINT ( 'NONE',  ( 80.68955802291256418, 62.97990070207239199, -3.482375488376182382 ) ) ;
#27367=CARTESIAN_POINT ( 'NONE',  ( -59.61240458878659609, 26.78407864000503835, -6.268956829791695995 ) ) ;
#27371=CARTESIAN_POINT ( 'NONE',  ( 82.15073535245149117, 63.33429545135105343, -2.460680857249039732 ) ) ;
#27378=CARTESIAN_POINT ( 'NONE',  ( 73.98866219012947454, 61.81968298976576648, 3.762445401688966573 ) ) ;
#27384=ORIENTED_EDGE ( 'NONE', *, *, #15147, .F. ) ;
#27386=CARTESIAN_POINT ( 'NONE',  ( 80.77640933968173442, 65.62578451531319956, 2.636331425444717436 ) ) ;
#27398=AXIS2_PLACEMENT_3D ( 'NONE', #26292, #3884, #32278 ) ;
#27406=CARTESIAN_POINT ( 'NONE',  ( 66.96854123855969476, 58.10689591609776983, -3.996990690923976519 ) ) ;
#27407=CARTESIAN_POINT ( 'NONE',  ( -60.14275962559869981, 24.84364830758654108, 9.154021781743367114 ) ) ;
#27408=ORIENTED_EDGE ( 'NONE', *, *, #25074, .F. ) ;
#27412=CARTESIAN_POINT ( 'NONE',  ( 25.11437021580303863, 164.7550792202006562, 4.000000000000000000 ) ) ;
#27415=CARTESIAN_POINT ( 'NONE',  ( -63.08758708074093136, 41.04287353446839859, -3.000000000000000000 ) ) ;
#27418=CARTESIAN_POINT ( 'NONE',  ( 79.34209122208885390, 66.30884595491197331, -1.045691535380374182 ) ) ;
#27420=EDGE_CURVE ( 'NONE', #23344, #7366, #7373, .T. ) ;
#27421=CARTESIAN_POINT ( 'NONE',  ( 80.11713744326790732, 64.15277314745162585, 3.661914029440277218 ) ) ;
#27425=CARTESIAN_POINT ( 'NONE',  ( 78.58187568275401702, 60.86241699943117567, -3.054665556626412926 ) ) ;
#27430=CARTESIAN_POINT ( 'NONE',  ( 81.15786166771449928, 61.29969053694480152, -1.104694797982636256 ) ) ;
#27431=CARTESIAN_POINT ( 'NONE',  ( 80.24754081275330009, 61.06584331557482415, 2.177161688561031649 ) ) ;
#27438=CARTESIAN_POINT ( 'NONE',  ( 82.42900007550694852, 62.86339166853763061, 1.342843868341103697 ) ) ;
#27456=DIRECTION ( 'NONE',  ( -0.000000000000000000, -0.000000000000000000, -1.000000000000000000 ) ) ;
#27465=CARTESIAN_POINT ( 'NONE',  ( 70.86714415968630476, 59.66805877367134769, -3.971832046809243622 ) ) ;
#27472=EDGE_CURVE ( 'NONE', #11154, #28588, #22171, .T. ) ;
#27476=DIRECTION ( 'NONE',  ( 0.000000000000000000, 0.000000000000000000, 1.000000000000000000 ) ) ;
#27484=CARTESIAN_POINT ( 'NONE',  ( 79.32339967214609544, 64.38349706316869003, -3.578491385641962896 ) ) ;
#27487=CARTESIAN_POINT ( 'NONE',  ( 81.36794360107698765, 64.82106189941457330, -2.952528780688971288 ) ) ;
#27488=CARTESIAN_POINT ( 'NONE',  ( 79.54992950373221561, 64.18601594420306355, 3.671038198312437384 ) ) ;
#27504=DIRECTION ( 'NONE',  ( 0.4690749385695657803, 0.8831583674551003460, 0.000000000000000000 ) ) ;
#27510=CARTESIAN_POINT ( 'NONE',  ( 67.38390057489351648, 58.33093658501181267, 3.992553130659727056 ) ) ;
#27519=ORIENTED_EDGE ( 'NONE', *, *, #28296, .F. ) ;
#27527=CARTESIAN_POINT ( 'NONE',  ( 80.03595747215288725, 63.73611138703243029, -3.702313260098204939 ) ) ;
#27528=DIRECTION ( 'NONE',  ( -0.9267318687906771491, 0.3757233601570964532, 0.000000000000000000 ) ) ;
#27529=CARTESIAN_POINT ( 'NONE',  ( 81.06392658325412981, 61.26538850743066433, 1.312782405654757678 ) ) ;
#27532=CARTESIAN_POINT ( 'NONE',  ( 74.52260502535293085, 62.13706486897681458, -3.724166978290282426 ) ) ;
#27543=CARTESIAN_POINT ( 'NONE',  ( 81.15786166771449928, 61.29969053694482994, 1.104694797982963328 ) ) ;
#27560=CARTESIAN_POINT ( 'NONE',  ( 79.22467975445887589, 65.90355157830848043, -2.361823859647588897 ) ) ;
#27566=VERTEX_POINT ( 'NONE', #13742 ) ;
#27573=CARTESIAN_POINT ( 'NONE',  ( 78.93014367432635936, 65.87924701951081374, -2.174925636353739922 ) ) ;
#27579=CARTESIAN_POINT ( 'NONE',  ( 82.02451737050265024, 62.15044802891514308, -1.700667878122839261 ) ) ;
#27584=DIRECTION ( 'NONE',  ( 0.3757233601570931225, 0.9267318687906784813, 0.000000000000000000 ) ) ;
#27587=CARTESIAN_POINT ( 'NONE',  ( 74.44738948069034734, 59.23650550459285569, 3.391332960764822158 ) ) ;
#27594=CARTESIAN_POINT ( 'NONE',  ( 79.89307030929712994, 66.05340108613447114, 2.264354540981408093 ) ) ;
#27596=DIRECTION ( 'NONE',  ( 1.000000000000000000, 0.000000000000000000, 0.000000000000000000 ) ) ;
#27605=LINE ( 'NONE', #30099, #34140 ) ;
#27610=CARTESIAN_POINT ( 'NONE',  ( 66.90064367344375285, 57.83598502562791310, -3.997265020308770289 ) ) ;
#27622=CARTESIAN_POINT ( 'NONE',  ( 81.04763707098177861, 66.10603528134693363, -1.133121492189030244 ) ) ;
#27623=CARTESIAN_POINT ( 'NONE',  ( 80.46181058475262660, 63.58258928487767037, 3.654032574946329603 ) ) ;
#27625=ORIENTED_EDGE ( 'NONE', *, *, #32458, .F. ) ;
#27626=CARTESIAN_POINT ( 'NONE',  ( 78.09760114435862022, 60.38799743245723306, -2.844364419925348830 ) ) ;
#27630=CARTESIAN_POINT ( 'NONE',  ( 79.92917477698983930, 65.49944209122774907, -2.989933650881962279 ) ) ;
#27631=CARTESIAN_POINT ( 'NONE',  ( 77.65955580186948737, 62.78993503910592011, 3.839379600940506343 ) ) ;
#27634=DIRECTION ( 'NONE',  ( 0.1006641980670203301, -0.9949204587440765302, 0.000000000000000000 ) ) ;
#27635=ORIENTED_EDGE ( 'NONE', *, *, #32739, .F. ) ;
#27636=CARTESIAN_POINT ( 'NONE',  ( 81.73765358980278961, 61.68994590043250525, 1.132734665583299494 ) ) ;
#27643=DIRECTION ( 'NONE',  ( -0.3757233601570931225, -0.9267318687906784813, 0.000000000000000000 ) ) ;
#27644=CARTESIAN_POINT ( 'NONE',  ( -64.30032790741496740, 34.77233229845844420, 5.249462333892575217 ) ) ;
#27646=DIRECTION ( 'NONE',  ( 0.000000000000000000, 0.000000000000000000, -1.000000000000000000 ) ) ;
#27657=FACE_OUTER_BOUND ( 'NONE', #34597, .T. ) ;
#27663=CARTESIAN_POINT ( 'NONE',  ( 69.70139497306261944, 59.23354404394888917, -3.977789803233245269 ) ) ;
#27669=CARTESIAN_POINT ( 'NONE',  ( 69.82526079983220768, 58.91932963963509451, 3.982895692900140894 ) ) ;
#27677=CARTESIAN_POINT ( 'NONE',  ( 78.38646849266343963, 65.84297019793960715, -1.584170212883422524 ) ) ;
#27679=CARTESIAN_POINT ( 'NONE',  ( 78.68815740766761735, 66.05701152551952759, -1.050153991572640777 ) ) ;
#27680=CARTESIAN_POINT ( 'NONE',  ( 78.92462413491021778, 65.07527128086412915, 3.128253119413329397 ) ) ;
#27706=CARTESIAN_POINT ( 'NONE',  ( 67.09515986712425217, 58.21407947277521089, 3.993497817183392584 ) ) ;
#27712=CARTESIAN_POINT ( 'NONE',  ( -75.45330471031414277, 33.71485196875532608, -8.800414904976364028 ) ) ;
#27721=CARTESIAN_POINT ( 'NONE',  ( 79.06216475166031898, 65.51459655345134081, -2.804471013201359497 ) ) ;
#27723=CARTESIAN_POINT ( 'NONE',  ( 79.33915194569573259, 65.11111034845949064, 3.233326467035608331 ) ) ;
#27727=CARTESIAN_POINT ( 'NONE',  ( 74.74317362787380148, 60.13816936446348649, -3.762445401688810698 ) ) ;
#27735=ORIENTED_EDGE ( 'NONE', *, *, #15251, .T. ) ;
#27742=CARTESIAN_POINT ( 'NONE',  ( 81.09074532527962731, 63.51554843946190232, 3.425340496581063654 ) ) ;
#27751=CARTESIAN_POINT ( 'NONE',  ( -65.33937732661527775, 36.44481994371090394, -7.201454646436823204 ) ) ;
#27758=CARTESIAN_POINT ( 'NONE',  ( 80.77164629763790060, 63.73694215246327133, -3.562450064734660415 ) ) ;
#27768=CARTESIAN_POINT ( 'NONE',  ( 80.04018988431747061, 64.49293993294404004, -3.578839808218921004 ) ) ;
#27774=CARTESIAN_POINT ( 'NONE',  ( 82.02157412789767932, 62.93630067300345843, -2.502189764415934548 ) ) ;
#27776=CARTESIAN_POINT ( 'NONE',  ( 79.89212576172680258, 63.66154800590240370, 4.000000000000000000 ) ) ;
#27782=CARTESIAN_POINT ( 'NONE',  ( 74.62207946275562165, 60.41194043352551546, 3.856662941142526169 ) ) ;
#27789=CARTESIAN_POINT ( 'NONE',  ( 81.88105255503974433, 62.58610580235438192, 2.445541897054072766 ) ) ;
#27804=DIRECTION ( 'NONE',  ( -0.000000000000000000, -0.000000000000000000, 1.000000000000000000 ) ) ;
#27805=ORIENTED_EDGE ( 'NONE', *, *, #20871, .T. ) ;
#27808=CARTESIAN_POINT ( 'NONE',  ( 66.81810912255278367, 58.06508983445694128, -3.996770903032645261 ) ) ;
#27819=CARTESIAN_POINT ( 'NONE',  ( 81.62248346935345467, 65.70993096190730398, -1.000000000000000000 ) ) ;
#27820=CARTESIAN_POINT ( 'NONE',  ( 78.70126604931442671, 66.02149264047228883, 1.577285172236843280 ) ) ;
#27822=ORIENTED_EDGE ( 'NONE', *, *, #30743, .T. ) ;
#27823=CARTESIAN_POINT ( 'NONE',  ( 77.29563288604617810, 62.10585478181958763, -3.856837490696089610 ) ) ;
#27828=CARTESIAN_POINT ( 'NONE',  ( 79.01071357413613327, 66.12284964548064181, -1.692865493181706649 ) ) ;
#27829=CARTESIAN_POINT ( 'NONE',  ( 77.96902425052304864, 62.15836910947907512, 3.808649511194706516 ) ) ;
#27835=VERTEX_POINT ( 'NONE', #29667 ) ;
#27836=CARTESIAN_POINT ( 'NONE',  ( 81.88767907424694670, 65.09350295521473129, 2.164558651853291771 ) ) ;
#27864=CARTESIAN_POINT ( 'NONE',  ( 69.89919258653301881, 58.73135405362895511, -3.965028736237033780 ) ) ;
#27869=DIRECTION ( 'NONE',  ( -1.000000000000000000, -8.706234683161959233E-16, 0.000000000000000000 ) ) ;
#27872=ADVANCED_FACE ( 'NONE', ( #11520 ), #10562, .T. ) ;
#27878=CARTESIAN_POINT ( 'NONE',  ( 78.37355578220726215, 65.75145430471653185, -1.935054690158703128 ) ) ;
#27881=CARTESIAN_POINT ( 'NONE',  ( 79.93288853953357886, 66.07525097314714912, -2.222430037836083727 ) ) ;
#27882=CARTESIAN_POINT ( 'NONE',  ( 79.32339967214608123, 64.38349706316869003, 3.578491385641963785 ) ) ;
#27884=FACE_OUTER_BOUND ( 'NONE', #35644, .T. ) ;
#27909=CARTESIAN_POINT ( 'NONE',  ( 67.10107710889761279, 58.19782780592215943, 3.994504660676310159 ) ) ;
#27923=ORIENTED_EDGE ( 'NONE', *, *, #39836, .T. ) ;
#27924=CARTESIAN_POINT ( 'NONE',  ( 80.11945187304007732, 63.42025125984802969, -3.710743084827438310 ) ) ;
#27928=CARTESIAN_POINT ( 'NONE',  ( 80.29143557890645866, 63.14717164025322660, 3.649417990092601372 ) ) ;
#27935=DIRECTION ( 'NONE',  ( 0.3757233601570964532, 0.9267318687906771491, -0.000000000000000000 ) ) ;
#27946=CARTESIAN_POINT ( 'NONE',  ( 79.15160802321621247, 66.03480532732626784, 2.011547652603496328 ) ) ;
#27950=CARTESIAN_POINT ( 'NONE',  ( -64.36785089794297221, 34.71712033580043055, -5.456534462680674658 ) ) ;
#27960=CIRCLE ( 'NONE', #14174, 1.000000000000002220 ) ;
#27961=EDGE_CURVE ( 'NONE', #6853, #26757, #32080, .T. ) ;
#27964=CARTESIAN_POINT ( 'NONE',  ( 80.13405435096433393, 64.91068451853310250, -3.368075118064919327 ) ) ;
#27972=CARTESIAN_POINT ( 'NONE',  ( 78.71191388991731230, 66.03048852543453506, -1.560659576774502622 ) ) ;
#27980=CARTESIAN_POINT ( 'NONE',  ( 80.30040509403147553, 65.99001427540433440, -2.270757614041408523 ) ) ;
#27988=CARTESIAN_POINT ( 'NONE',  ( 73.28086911227147482, 60.35416371166882499, 3.944160774611113585 ) ) ;
#27998=CARTESIAN_POINT ( 'NONE',  ( 80.26729624682498354, 65.68772892857236911, 2.758880570191253323 ) ) ;
#28001=ORIENTED_EDGE ( 'NONE', *, *, #10372, .T. ) ;
#28009=CARTESIAN_POINT ( 'NONE',  ( -64.01189449551645794, 34.81586596186931359, 6.999999999999992006 ) ) ;
#28016=CARTESIAN_POINT ( 'NONE',  ( 66.74404603967394678, 57.81040951471371159, -3.998354769210576976 ) ) ;
#28021=CARTESIAN_POINT ( 'NONE',  ( -57.59497484894375674, 32.71166363405644262, 4.078840986107554301 ) ) ;
#28022=ADVANCED_FACE ( 'NONE', ( #10617 ), #20094, .T. ) ;
#28031=CARTESIAN_POINT ( 'NONE',  ( 82.42900007550682062, 62.86339166853757376, -1.342843868341962343 ) ) ;
#28032=CARTESIAN_POINT ( 'NONE',  ( 81.11951992695615843, 61.28566998660698317, 1.215327096190474965 ) ) ;
#28035=EDGE_LOOP ( 'NONE', ( #5995, #36821, #28865, #20815 ) ) ;
#28036=CARTESIAN_POINT ( 'NONE',  ( 76.86947707741236968, 60.02096306738866360, -3.097219288968816375 ) ) ;
#28040=CARTESIAN_POINT ( 'NONE',  ( 81.34140156818914136, 61.66514490546132521, -2.058202901128797446 ) ) ;
#28041=CARTESIAN_POINT ( 'NONE',  ( 78.76819457884748488, 61.97782169454070811, 3.640295653905004425 ) ) ;
#28045=CARTESIAN_POINT ( 'NONE',  ( 81.07719038108473342, 65.78599662769329370, 2.192618372226455836 ) ) ;
#28051=DIRECTION ( 'NONE',  ( -1.000000000000000000, 8.723105632544016523E-16, 0.000000000000000000 ) ) ;
#28052=CARTESIAN_POINT ( 'NONE',  ( -62.75662366181008878, 35.73757431566994569, -5.477568781475775417 ) ) ;
#28053=CARTESIAN_POINT ( 'NONE',  ( -64.44214806826555275, 36.58397470404603524, 5.707342493247510973 ) ) ;
#28056=PLANE ( 'NONE',  #16900 ) ;
#28061=CARTESIAN_POINT ( 'NONE',  ( 81.14431272898491443, 61.29471917812056603, -1.169946933694579583 ) ) ;
#28067=CARTESIAN_POINT ( 'NONE',  ( -62.96463773297413269, 37.71389135159273565, -4.136849086240373730 ) ) ;
#28072=CARTESIAN_POINT ( 'NONE',  ( 69.94804423520642445, 58.60696991578217308, -3.944663542062683881 ) ) ;
#28074=VERTEX_POINT ( 'NONE', #28974 ) ;
#28088=CARTESIAN_POINT ( 'NONE',  ( 80.40236172895532718, 61.11465044667751556, -2.108843360059433625 ) ) ;
#28091=CARTESIAN_POINT ( 'NONE',  ( 81.87453109492308556, 63.55405699985828960, -2.808566127056343564 ) ) ;
#28092=CARTESIAN_POINT ( 'NONE',  ( 80.65804582012491153, 61.64568945823259583, 2.699019001080979141 ) ) ;
#28094=DIRECTION ( 'NONE',  ( 0.000000000000000000, -0.000000000000000000, 1.000000000000000000 ) ) ;
#28100=VERTEX_POINT ( 'NONE', #25880 ) ;
#28102=DIRECTION ( 'NONE',  ( -0.000000000000000000, -0.000000000000000000, -1.000000000000000000 ) ) ;
#28107=CARTESIAN_POINT ( 'NONE',  ( -73.45070404594234503, 38.65432087843066000, -9.800414904976365804 ) ) ;
#28111=AXIS2_PLACEMENT_3D ( 'NONE', #26840, #5220, #23553 ) ;
#28112=CIRCLE ( 'NONE', #11628, 114.6618724293813898 ) ;
#28119=CARTESIAN_POINT ( 'NONE',  ( 67.01285850879368411, 57.98447793263278527, 3.999354069328931782 ) ) ;
#28133=EDGE_LOOP ( 'NONE', ( #34846, #14266, #4738, #15157 ) ) ;
#28134=CARTESIAN_POINT ( 'NONE',  ( 78.75315097705549761, 65.71977079011871581, -2.326060681237740013 ) ) ;
#28137=CARTESIAN_POINT ( 'NONE',  ( 79.25608414939210888, 65.04333590781634200, 3.260928702718600469 ) ) ;
#28143=CARTESIAN_POINT ( 'NONE',  ( -63.99293516169446150, 35.89893413629672381, -7.506047544094577084 ) ) ;
#28147=CARTESIAN_POINT ( 'NONE',  ( -63.58520484588294153, 35.72026407271188475, -7.000000000000000888 ) ) ;
#28151=CARTESIAN_POINT ( 'NONE',  ( 81.11561130678133225, 63.91242180912993831, 3.402511877379639227 ) ) ;
#28167=CARTESIAN_POINT ( 'NONE',  ( 80.49748116766497219, 63.97695225015618803, -3.602832836245128956 ) ) ;
#28177=CARTESIAN_POINT ( 'NONE',  ( 79.27128227901765456, 65.37053819277495847, -2.988136994358709497 ) ) ;
#28183=CARTESIAN_POINT ( 'NONE',  ( 78.68884106766326170, 66.05749720280910253, -1.041818241550652724 ) ) ;
#28188=CARTESIAN_POINT ( 'NONE',  ( -64.08758708074093136, 41.64075302466238071, -2.960467338825643058 ) ) ;
#28189=CARTESIAN_POINT ( 'NONE',  ( 73.78163614357571021, 59.18917187859454998, 3.552420216828422017 ) ) ;
#28196=CARTESIAN_POINT ( 'NONE',  ( -77.95330471031414277, 33.71485196875532608, 12.49999999999999645 ) ) ;
#28197=CARTESIAN_POINT ( 'NONE',  ( 81.54961753534279012, 61.59690320141231723, 1.551099981298355468 ) ) ;
#28215=CARTESIAN_POINT ( 'NONE',  ( 66.59136238364995108, 57.77385624644436746, -3.999229419681933351 ) ) ;
#28217=CIRCLE ( 'NONE', #10470, 7.999999999999992895 ) ;
#28218=VERTEX_POINT ( 'NONE', #37363 ) ;
#28219=CARTESIAN_POINT ( 'NONE',  ( -57.81912131869246707, 32.28080896713289860, 4.194423477175957871 ) ) ;
#28222=CARTESIAN_POINT ( 'NONE',  ( -65.15514661499977933, 34.97220226750606997, 6.888442104241535802 ) ) ;
#28223=CARTESIAN_POINT ( 'NONE',  ( -74.03402466285142225, 19.33157623370699341, -8.800414904976364028 ) ) ;
#28226=CARTESIAN_POINT ( 'NONE',  ( -58.99872204295123623, 28.48507918597136523, -6.834244957304557389 ) ) ;
#28229=CARTESIAN_POINT ( 'NONE',  ( 80.00335259508500485, 66.34466434620085806, -1.325417871280742066 ) ) ;
#28231=CARTESIAN_POINT ( 'NONE',  ( 81.17223480711247419, 61.34085670634290466, 1.541060042019463561 ) ) ;
#28235=CARTESIAN_POINT ( 'NONE',  ( 76.75621762107158474, 64.55157797518407392, -2.701592190110922331 ) ) ;
#28240=CARTESIAN_POINT ( 'NONE',  ( 81.39824655423379340, 62.07766870923514801, -2.596981798947365583 ) ) ;
#28241=CARTESIAN_POINT ( 'NONE',  ( 78.51266523469810465, 61.01400193535553029, 3.220231295875823463 ) ) ;
#28247=CARTESIAN_POINT ( 'NONE',  ( 79.56604632444089020, 66.26916991809642354, 1.539394129974047676 ) ) ;
#28253=CARTESIAN_POINT ( 'NONE',  ( -64.17943696418036836, 35.01970154838168980, 4.761094547372117347 ) ) ;
#28256=CIRCLE ( 'NONE', #40092, 1.000000000000002220 ) ;
#28266=CARTESIAN_POINT ( 'NONE',  ( 17.04338035915418459, 48.81061067247630092, 4.000000000000000000 ) ) ;
#28273=ORIENTED_EDGE ( 'NONE', *, *, #3817, .F. ) ;
#28276=CARTESIAN_POINT ( 'NONE',  ( 67.97136023280155825, 58.53559134324396496, -3.990965707299544363 ) ) ;
#28277=B_SPLINE_CURVE_WITH_KNOTS ( 'NONE', 3,
 ( #19668, #28731, #25438, #738, #9580, #16363 ),
 .UNSPECIFIED., .F., .F.,
 ( 4, 2, 4 ),
 ( 0.000000000000000000, 0.0003568402636276586356, 0.0007136805272553172711 ),
 .UNSPECIFIED. ) ;
#28286=DIRECTION ( 'NONE',  ( 0.000000000000000000, 0.000000000000000000, 1.000000000000000000 ) ) ;
#28289=ORIENTED_EDGE ( 'NONE', *, *, #38773, .F. ) ;
#28290=CARTESIAN_POINT ( 'NONE',  ( 78.44523713320049296, 65.65863411530537519, -2.218931858625903697 ) ) ;
#28293=CARTESIAN_POINT ( 'NONE',  ( 79.54388053879580411, 66.09379204087656490, -2.134710458528699561 ) ) ;
#28294=CARTESIAN_POINT ( 'NONE',  ( 80.53617040090055923, 61.82406284986342371, 2.948506306558747347 ) ) ;
#28296=EDGE_CURVE ( 'NONE', #1666, #37345, #37562, .T. ) ;
#28297=CIRCLE ( 'NONE', #13840, 5.329987104167474676 ) ;
#28298=CARTESIAN_POINT ( 'NONE',  ( 80.38645948019593845, 66.31981033314002616, 1.000000000000000000 ) ) ;
#28320=ADVANCED_FACE ( 'NONE', ( #21940, #30808 ), #12029, .F. ) ;
#28321=DIRECTION ( 'NONE',  ( 0.6751708784618154491, -0.7376613619250370624, 0.000000000000000000 ) ) ;
#28327=CARTESIAN_POINT ( 'NONE',  ( 67.06698855917106528, 57.83491659372258908, 3.993952884371010814 ) ) ;
#28342=CARTESIAN_POINT ( 'NONE',  ( 80.23164863168994998, 63.12273326640273297, -3.657510014241807106 ) ) ;
#28344=CARTESIAN_POINT ( 'NONE',  ( 80.00230669363345726, 63.71856487089239351, 3.706996517075249908 ) ) ;
#28348=AXIS2_PLACEMENT_3D ( 'NONE', #2139, #14867, #1186 ) ;
#28362=CARTESIAN_POINT ( 'NONE',  ( 81.27686174477064185, 61.37652599617184990, 1.416821487223855813 ) ) ;
#28379=CARTESIAN_POINT ( 'NONE',  ( 80.75501959326771839, 63.35152955421530407, -3.552238747020028953 ) ) ;
#28389=CARTESIAN_POINT ( 'NONE',  ( 80.39050082614866710, 63.54812927569808778, -3.668443954219268832 ) ) ;
#28396=CARTESIAN_POINT ( 'NONE',  ( 78.92300404249584744, 66.17133619070195039, -1.270639542487659535 ) ) ;
#28402=CARTESIAN_POINT ( 'NONE',  ( 71.32664523234116416, 58.52704510057537135, 3.775670717450666736 ) ) ;
#28406=CARTESIAN_POINT ( 'NONE',  ( -58.72867408015306978, 29.68869064929980794, -5.572828569880161176 ) ) ;
#28409=CARTESIAN_POINT ( 'NONE',  ( 81.68586513309682573, 63.81782706256000637, 3.019849704268901647 ) ) ;
#28430=CARTESIAN_POINT ( 'NONE',  ( 66.56592146697632018, 57.84521198437244038, -3.999917672785076483 ) ) ;
#28441=CARTESIAN_POINT ( 'NONE',  ( 82.20671311902168554, 64.86843738523475622, -1.633153239555407144 ) ) ;
#28443=CARTESIAN_POINT ( 'NONE',  ( 81.12024331894987483, 61.43208913379082503, 1.925402693829570300 ) ) ;
#28446=CARTESIAN_POINT ( 'NONE',  ( 77.39092423430425072, 61.90746491491129433, -3.829716617890468022 ) ) ;
#28451=CARTESIAN_POINT ( 'NONE',  ( 80.22001885188437598, 64.95903095167622610, -3.330128783915600632 ) ) ;
#28452=CARTESIAN_POINT ( 'NONE',  ( 76.82516749139865908, 64.42394039557471785, 2.889099817377080548 ) ) ;
#28458=CARTESIAN_POINT ( 'NONE',  ( 82.29876416100432834, 62.79692783100102105, 1.831286414254331030 ) ) ;
#28464=CARTESIAN_POINT ( 'NONE',  ( -64.12237394559150516, 36.72939681796538025, 5.075523754375453223 ) ) ;
#28471=CARTESIAN_POINT ( 'NONE',  ( 80.84587339237160108, 61.18626677283346993, -1.559707275244749836 ) ) ;
#28480=ORIENTED_EDGE ( 'NONE', *, *, #27420, .T. ) ;
#28483=CARTESIAN_POINT ( 'NONE',  ( 68.03141654933527604, 58.37504561612195886, -3.996230182412892074 ) ) ;
#28498=CARTESIAN_POINT ( 'NONE',  ( 80.72640005664072760, 61.14345848406946260, -1.640065189519674060 ) ) ;
#28501=CARTESIAN_POINT ( 'NONE',  ( 81.73261497063171532, 63.12224843555907938, -2.914706979937542020 ) ) ;
#28502=CARTESIAN_POINT ( 'NONE',  ( 79.28407881342867825, 64.35615987108396041, 3.584461231902843714 ) ) ;
#28503=ORIENTED_EDGE ( 'NONE', *, *, #10053, .F. ) ;
#28527=CIRCLE ( 'NONE', #25911, 83.68529983683480111 ) ;
#28533=CARTESIAN_POINT ( 'NONE',  ( 66.96854123855969476, 58.10689591609776983, 3.996990690923977407 ) ) ;
#28549=CARTESIAN_POINT ( 'NONE',  ( 80.89520131247707013, 61.53942361443163378, -2.340042473998850348 ) ) ;
#28551=CARTESIAN_POINT ( 'NONE',  ( 80.14986013843031287, 63.43437088187635453, 3.706996517075249020 ) ) ;
#28559=ADVANCED_FACE ( 'NONE', ( #20649 ), #39178, .T. ) ;
#28565=FACE_OUTER_BOUND ( 'NONE', #28035, .T. ) ;
#28567=AXIS2_PLACEMENT_3D ( 'NONE', #22107, #34684, #31169 ) ;
#28573=CARTESIAN_POINT ( 'NONE',  ( 78.91475304129781421, 66.06124928554449127, 1.777114115212670598 ) ) ;
#28577=DIRECTION ( 'NONE',  ( 0.4690749385695657803, 0.8831583674551003460, 0.000000000000000000 ) ) ;
#28581=CARTESIAN_POINT ( 'NONE',  ( -73.07498068578524908, 39.58105274722134226, 9.800414904976365804 ) ) ;
#28582=LINE ( 'NONE', #16415, #5723 ) ;
#28588=VERTEX_POINT ( 'NONE', #11170 ) ;
#28589=CARTESIAN_POINT ( 'NONE',  ( 79.82117971689783076, 65.09389273565577128, -3.300462285847908905 ) ) ;
#28599=CARTESIAN_POINT ( 'NONE',  ( 78.77108537463556104, 65.94663689831973841, -1.925402693829578515 ) ) ;
#28604=CARTESIAN_POINT ( 'NONE',  ( 78.93443484242880004, 66.17773471521378781, -1.251938014746446504 ) ) ;
#28613=CARTESIAN_POINT ( 'NONE',  ( 71.78591447743995957, 60.68937113591298527, 3.856543183828340826 ) ) ;
#28618=TOROIDAL_SURFACE ( 'NONE', #5565, 5.329987104167480894, 1.000000000000000000 ) ;
#28622=CARTESIAN_POINT ( 'NONE',  ( 81.13122672737068797, 64.30755116177446951, 3.292658836682930801 ) ) ;
#28623=VECTOR ( 'NONE', #27456, 1000.000000000000000 ) ;
#28624=B_SPLINE_CURVE_WITH_KNOTS ( 'NONE', 3,
 ( #28222, #12169, #40571, #25762 ),
 .UNSPECIFIED., .F., .F.,
 ( 4, 4 ),
 ( 0.000000000000000000, 0.0005391349717845224593 ),
 .UNSPECIFIED. ) ;
#28640=CARTESIAN_POINT ( 'NONE',  ( 66.27376694609004915, 57.73522568913436004, -4.000000000000000000 ) ) ;
#28652=CARTESIAN_POINT ( 'NONE',  ( 82.52706534919252590, 63.19378067493415330, -1.386429027374526557 ) ) ;
#28653=CARTESIAN_POINT ( 'NONE',  ( 81.04993867939978713, 61.73413400689827313, 2.516896548562573610 ) ) ;
#28658=CARTESIAN_POINT ( 'NONE',  ( 75.66308047697206973, 62.61957414976298963, -3.723120700747940770 ) ) ;
#28660=DIRECTION ( 'NONE',  ( 0.000000000000000000, 0.000000000000000000, 1.000000000000000000 ) ) ;
#28662=CARTESIAN_POINT ( 'NONE',  ( 80.95544561733511557, 63.83034742112755566, -3.486376426170565868 ) ) ;
#28664=CARTESIAN_POINT ( 'NONE',  ( 77.48272095992959407, 61.71466691532017990, 3.776276000690670376 ) ) ;
#28668=CARTESIAN_POINT ( 'NONE',  ( -58.83394063668751528, 29.29677716115665831, 5.900615745428536840 ) ) ;
#28669=CARTESIAN_POINT ( 'NONE',  ( 82.04814969336737818, 64.78574761690819628, 2.164558651853291771 ) ) ;
#28678=CARTESIAN_POINT ( 'NONE',  ( 72.82963479777622240, 58.84354944748790217, 3.620166419653539691 ) ) ;
#28682=DIRECTION ( 'NONE',  ( 1.000000000000000000, 0.000000000000000000, 0.000000000000000000 ) ) ;
#28691=CARTESIAN_POINT ( 'NONE',  ( 68.53436546801150087, 58.80600050245282517, -3.985059344218151445 ) ) ;
#28702=CARTESIAN_POINT ( 'NONE',  ( 78.97731087898851854, 65.91669204587326192, 2.137206601789621185 ) ) ;
#28706=CARTESIAN_POINT ( 'NONE',  ( 80.29582733418162377, 61.38465067277564202, -2.608847861177660654 ) ) ;
#28710=CARTESIAN_POINT ( 'NONE',  ( 80.26729624682485564, 65.68772892857229806, -2.758880570191356796 ) ) ;
#28711=CARTESIAN_POINT ( 'NONE',  ( 78.31969284963511768, 65.55289002357415029, 2.305838555344982499 ) ) ;
#28714=CARTESIAN_POINT ( 'NONE',  ( -64.08758708074093136, 43.50655619156747633, 1.588711929257163868 ) ) ;
#28731=CARTESIAN_POINT ( 'NONE',  ( -60.05933043039490826, 24.84364830758654108, -9.240995299818665742 ) ) ;
#28740=CARTESIAN_POINT ( 'NONE',  ( 66.74698822326750758, 57.80221319398844315, 3.998057522770657624 ) ) ;
#28755=CARTESIAN_POINT ( 'NONE',  ( 80.91969899470512928, 61.54505855127015934, -2.326060681237731576 ) ) ;
#28757=CARTESIAN_POINT ( 'NONE',  ( 80.69037048981478222, 62.35571368504050582, 3.252077313700840300 ) ) ;
#28761=CARTESIAN_POINT ( 'NONE',  ( -58.17279802585986204, 29.79606812221977563, 4.661957855074470025 ) ) ;
#28768=ORIENTED_EDGE ( 'NONE', *, *, #32739, .T. ) ;
#28778=CARTESIAN_POINT ( 'NONE',  ( 79.95152939680102122, 65.17166210280107919, 3.248659383495577480 ) ) ;
#28784=DIRECTION ( 'NONE',  ( 0.000000000000000000, -1.000000000000000000, -0.000000000000000000 ) ) ;
#28788=CARTESIAN_POINT ( 'NONE',  ( 69.07430361466936120, 59.13263628650475567, 3.969490915146614007 ) ) ;
#28791=CARTESIAN_POINT ( 'NONE',  ( 73.38675137958711048, 60.10977650211887635, -3.914122288815134798 ) ) ;
#28797=CARTESIAN_POINT ( 'NONE',  ( 81.28814307398172900, 61.80674180605062418, -2.393593008231202024 ) ) ;
#28807=CARTESIAN_POINT ( 'NONE',  ( 79.92294945466714751, 64.42298636752006757, -3.607546830629785539 ) ) ;
#28817=CARTESIAN_POINT ( 'NONE',  ( -64.08758708074093136, 43.50509228929546879, -1.592748447102107390 ) ) ;
#28818=CARTESIAN_POINT ( 'NONE',  ( 72.29787722903529357, 59.46803282872462404, 3.909340765805334961 ) ) ;
#28822=CIRCLE ( 'NONE', #11029, 0.9999999999999998890 ) ;
#28826=CARTESIAN_POINT ( 'NONE',  ( 81.36150051721972432, 64.03901721960635030, 3.243459512806143419 ) ) ;
#28836=CARTESIAN_POINT ( 'NONE',  ( -63.99293516169446150, 35.89893413629672381, -7.506047544094577084 ) ) ;
#28837=ADVANCED_FACE ( 'NONE', ( #36710 ), #24981, .F. ) ;
#28838=ADVANCED_FACE ( 'NONE', ( #21277, #12200 ), #28056, .F. ) ;
#28845=VECTOR ( 'NONE', #35913, 1000.000000000000000 ) ;
#28847=CARTESIAN_POINT ( 'NONE',  ( 66.57374945270225908, 57.82325632336715415, -3.999874661881728688 ) ) ;
#28855=CARTESIAN_POINT ( 'NONE',  ( 82.56043351944043707, 63.54438683934779419, -1.421283058691077850 ) ) ;
#28860=CARTESIAN_POINT ( 'NONE',  ( 75.21236926079949114, 60.63031288236823002, -3.833662259905124436 ) ) ;
#28864=CARTESIAN_POINT ( 'NONE',  ( 75.90485726080819973, 62.11260916716570080, 3.867068906737703760 ) ) ;
#28865=ORIENTED_EDGE ( 'NONE', *, *, #30751, .F. ) ;
#28869=CARTESIAN_POINT ( 'NONE',  ( 81.60411730068159386, 64.94496191031764454, 2.665107514500538066 ) ) ;
#28878=DIRECTION ( 'NONE',  ( -0.000000000000000000, -0.000000000000000000, -1.000000000000000000 ) ) ;
#28879=DIRECTION ( 'NONE',  ( 0.9267318687906771491, -0.3757233601570964532, 0.000000000000000000 ) ) ;
#28883=CARTESIAN_POINT ( 'NONE',  ( -73.07498068578524908, 39.58105274722134936, 9.800414904976365804 ) ) ;
#28894=CARTESIAN_POINT ( 'NONE',  ( 67.78936902810559673, 58.13140593263176470, -3.993918888840292780 ) ) ;
#28897=CARTESIAN_POINT ( 'NONE',  ( -64.08758708074093136, 38.13199975834322686, 3.043809435734686097 ) ) ;
#28905=CARTESIAN_POINT ( 'NONE',  ( 81.26478070948648735, 61.47323240028521241, 1.804401104814719270 ) ) ;
#28908=CARTESIAN_POINT ( 'NONE',  ( 78.30161670990426614, 64.30707665991987199, -3.470679136763274109 ) ) ;
#28911=CARTESIAN_POINT ( 'NONE',  ( 78.85932765206329975, 66.13466208586149264, -1.358900964588049431 ) ) ;
#28913=CARTESIAN_POINT ( 'NONE',  ( 80.39617744327613025, 62.02891139109912899, 3.151254463355007918 ) ) ;
#28914=EDGE_LOOP ( 'NONE', ( #37845, #22724, #37175, #31834 ) ) ;
#28917=CARTESIAN_POINT ( 'NONE',  ( 78.99916064199126708, 66.21331998952631182, 1.048259027381037267 ) ) ;
#28918=CARTESIAN_POINT ( 'NONE',  ( -63.70768059418392681, 44.39675795296274430, 1.227925197078028052 ) ) ;
#28935=FACE_OUTER_BOUND ( 'NONE', #10844, .T. ) ;
#28943=CARTESIAN_POINT ( 'NONE',  ( 66.68811621373450294, 57.96620201306357956, 3.998609561968404336 ) ) ;
#28945=CARTESIAN_POINT ( 'NONE',  ( -64.08758708074093136, 38.60011822860882802, 4.018727294472848044 ) ) ;
#28958=CARTESIAN_POINT ( 'NONE',  ( 78.60455099833406223, 65.79598288722390009, -2.095806625474251117 ) ) ;
#28960=CARTESIAN_POINT ( 'NONE',  ( 79.35276748299807537, 64.76637986602914054, 3.438247877890458160 ) ) ;
#28961=DIRECTION ( 'NONE',  ( -0.9949204587440765302, -0.1006641980670203163, -0.000000000000000000 ) ) ;
#28969=CARTESIAN_POINT ( 'NONE',  ( -63.08758708074093136, 41.04287353446839148, 4.000000000000000000 ) ) ;
#28971=VERTEX_POINT ( 'NONE', #15907 ) ;
#28972=AXIS2_PLACEMENT_3D ( 'NONE', #33805, #27804, #36667 ) ;
#28974=CARTESIAN_POINT ( 'NONE',  ( -63.03213158086148837, 38.26878225442760595, -4.032857076800604901 ) ) ;
#28978=CARTESIAN_POINT ( 'NONE',  ( 80.35608454708177817, 64.67152608030556848, 3.471690071579478953 ) ) ;
#28980=( BOUNDED_CURVE ( )  B_SPLINE_CURVE ( 3, ( #20015, #39345, #1912, #33413 ),
 .UNSPECIFIED., .F., .T. ) 
 B_SPLINE_CURVE_WITH_KNOTS ( ( 4, 4 ),
 ( 4.712388980384691450, 4.860526820865776365 ),
 .UNSPECIFIED. ) 
 CURVE ( )  GEOMETRIC_REPRESENTATION_ITEM ( )  RATIONAL_B_SPLINE_CURVE ( ( 1.000000000000000000, 0.9981721009331622207, 0.9981721009331622207, 1.000000000000000000 ) ) 
 REPRESENTATION_ITEM ( '' )  );
#28995=CARTESIAN_POINT ( 'NONE',  ( 79.68007496026339709, 65.35156779369863500, -3.108243619504652333 ) ) ;
#28997=CARTESIAN_POINT ( 'NONE',  ( 17.97454669799173033, 51.66243977840390755, -1.000000000000000000 ) ) ;
#28999=AXIS2_PLACEMENT_3D ( 'NONE', #7456, #26409, #20407 ) ;
#29005=CARTESIAN_POINT ( 'NONE',  ( 81.11523045952515076, 61.59071516775626520, -2.202709653501093712 ) ) ;
#29018=CARTESIAN_POINT ( 'NONE',  ( -64.08758708074093136, 43.24969657044037064, -2.909329950559495614 ) ) ;
#29019=CARTESIAN_POINT ( 'NONE',  ( 72.08456622119051360, 59.97905947476213839, 3.962431611483851146 ) ) ;
#29022=EDGE_CURVE ( 'NONE', #23047, #9808, #26794, .T. ) ;
#29028=CARTESIAN_POINT ( 'NONE',  ( 79.28168835805398373, 66.11151980550600626, 1.907437723464478152 ) ) ;
#29043=VERTEX_POINT ( 'NONE', #19808 ) ;
#29047=CARTESIAN_POINT ( 'NONE',  ( 66.67928806435183731, 57.99078996168128697, -3.997717836774547617 ) ) ;
#29058=CARTESIAN_POINT ( 'NONE',  ( 81.16398582655315863, 65.83200543430099572, -2.021051955677195533 ) ) ;
#29062=CARTESIAN_POINT ( 'NONE',  ( 75.58676173236689522, 62.77776356238130973, -3.642592851537363341 ) ) ;
#29066=CARTESIAN_POINT ( 'NONE',  ( 76.11285053945339030, 63.10974250081548576, 3.590981437842967861 ) ) ;
#29073=CARTESIAN_POINT ( 'NONE',  ( 80.42596214810052402, 66.05751922670457077, 2.080779877698174296 ) ) ;
#29095=CARTESIAN_POINT ( 'NONE',  ( 68.48614864092384380, 58.93304109727553453, -3.970924506823389599 ) ) ;
#29103=CIRCLE ( 'NONE', #31109, 1.000000000000002220 ) ;
#29107=CARTESIAN_POINT ( 'NONE',  ( 81.96779975749585390, 61.96402392828839822, -1.000000000000000000 ) ) ;
#29109=CARTESIAN_POINT ( 'NONE',  ( 79.47520324823358351, 65.51774519012143116, 2.899379378185759748 ) ) ;
#29112=CARTESIAN_POINT ( 'NONE',  ( 79.93789898034924590, 60.96822905336945553, -2.313798345564227255 ) ) ;
#29115=CARTESIAN_POINT ( 'NONE',  ( 81.20219841817447559, 64.34456771238251349, -3.243459512787965959 ) ) ;
#29116=CARTESIAN_POINT ( 'NONE',  ( 78.12595179671936307, 65.55859174716130156, 2.108843360059416749 ) ) ;
#29122=CARTESIAN_POINT ( 'NONE',  ( 81.03660848153769791, 66.10018949144995304, 1.263752851812355305 ) ) ;
#29123=CARTESIAN_POINT ( 'NONE',  ( -64.08758708074093136, 43.38479242966779736, 2.769427336171834675 ) ) ;
#29138=AXIS2_PLACEMENT_3D ( 'NONE', #4702, #17237, #29810 ) ;
#29139=FACE_OUTER_BOUND ( 'NONE', #18917, .T. ) ;
#29144=ORIENTED_EDGE ( 'NONE', *, *, #37878, .F. ) ;
#29145=CARTESIAN_POINT ( 'NONE',  ( 66.86134338034700875, 57.94508673653880493, 3.999594749380241510 ) ) ;
#29157=CARTESIAN_POINT ( 'NONE',  ( 80.53463578537552792, 62.06606814882641743, -3.115013800517337117 ) ) ;
#29159=CARTESIAN_POINT ( 'NONE',  ( 79.88928440695138988, 63.65969051258275613, 3.720735635808744668 ) ) ;
#29170=CARTESIAN_POINT ( 'NONE',  ( 68.47051737416747130, 59.12915321841263960, -3.950001462127424645 ) ) ;
#29178=CARTESIAN_POINT ( 'NONE',  ( 80.98576866654177309, 63.46339031992857826, 3.471690071579480286 ) ) ;
#29183=CIRCLE ( 'NONE', #16663, 0.9999999999999998890 ) ;
#29184=CARTESIAN_POINT ( 'NONE',  ( -63.71117060422361078, 35.77969396829419679, 7.174848616057642126 ) ) ;
#29190=ADVANCED_FACE ( 'NONE', ( #21637 ), #3177, .F. ) ;
#29193=CARTESIAN_POINT ( 'NONE',  ( 81.18881611591316982, 61.34569122823198484, -1.520709669156494748 ) ) ;
#29198=CARTESIAN_POINT ( 'NONE',  ( -60.66839582778040807, 24.84364830758653397, -8.800414904976364028 ) ) ;
#29205=CARTESIAN_POINT ( 'NONE',  ( 79.55117250774208060, 64.91534908514013580, -3.386558198656252738 ) ) ;
#29209=AXIS2_PLACEMENT_3D ( 'NONE', #2434, #12056, #18241 ) ;
#29217=CARTESIAN_POINT ( 'NONE',  ( 72.17048485476517783, 59.77360812419138369, 3.955776929930288510 ) ) ;
#29226=CARTESIAN_POINT ( 'NONE',  ( 80.36688112369847659, 65.40474626847709771, 3.015199126130975404 ) ) ;
#29231=EDGE_CURVE ( 'NONE', #6802, #32211, #4798, .T. ) ;
#29243=DIRECTION ( 'NONE',  ( -0.000000000000000000, -0.000000000000000000, -1.000000000000000000 ) ) ;
#29250=CARTESIAN_POINT ( 'NONE',  ( 66.27376694609004915, 57.73522568913436004, -4.000000000000000000 ) ) ;
#29258=CARTESIAN_POINT ( 'NONE',  ( 82.20862031248746860, 64.47799227860153337, -2.164558651854042282 ) ) ;
#29259=VECTOR ( 'NONE', #32835, 1000.000000000000000 ) ;
#29263=CARTESIAN_POINT ( 'NONE',  ( 74.98537949548503434, 62.60475170799649192, -3.615102801931181276 ) ) ;
#29268=CARTESIAN_POINT ( 'NONE',  ( 75.18153624412201452, 63.60369824193129773, 2.950589020697209186 ) ) ;
#29271=CIRCLE ( 'NONE', #11486, 7.999999999999992895 ) ;
#29275=CARTESIAN_POINT ( 'NONE',  ( 80.02452723347246888, 66.12521016146376951, 2.110636331688408696 ) ) ;
#29288=EDGE_CURVE ( 'NONE', #7364, #6802, #26186, .T. ) ;
#29295=ORIENTED_EDGE ( 'NONE', *, *, #26328, .T. ) ;
#29298=CARTESIAN_POINT ( 'NONE',  ( 67.11883677231543288, 58.14904800069622581, -3.997022163556062324 ) ) ;
#29301=ORIENTED_EDGE ( 'NONE', *, *, #40713, .T. ) ;
#29307=CARTESIAN_POINT ( 'NONE',  ( -55.62677557291493713, 30.95433239688069804, 1.979412988903658022 ) ) ;
#29308=VERTEX_POINT ( 'NONE', #31717 ) ;
#29310=CARTESIAN_POINT ( 'NONE',  ( 81.23328907848380709, 61.46306935600725296, 1.830101370957705642 ) ) ;
#29313=CARTESIAN_POINT ( 'NONE',  ( 78.12595179671936307, 65.55859174716130156, -2.108843360059416749 ) ) ;
#29316=CARTESIAN_POINT ( 'NONE',  ( 80.45827632841502464, 65.09029793562378075, -3.202775791559303808 ) ) ;
#29317=CARTESIAN_POINT ( 'NONE',  ( 78.47217392918747692, 65.00024052541876074, 3.055712048904924760 ) ) ;
#29318=CIRCLE ( 'NONE', #7587, 7.999999999999986677 ) ;
#29321=CARTESIAN_POINT ( 'NONE',  ( 79.00097698949592484, 66.21430696267364624, 1.024355359505926488 ) ) ;
#29324=CARTESIAN_POINT ( 'NONE',  ( -64.43126815475758917, 34.69310041339028317, -5.627269573384313439 ) ) ;
#29342=CARTESIAN_POINT ( 'NONE',  ( 66.81810912255278367, 58.06508983445694128, 3.996770903032645261 ) ) ;
#29349=ORIENTED_EDGE ( 'NONE', *, *, #7219, .T. ) ;
#29358=CARTESIAN_POINT ( 'NONE',  ( 79.98443850338786376, 63.35773072451035404, -3.725738571856551662 ) ) ;
#29360=CARTESIAN_POINT ( 'NONE',  ( 80.35827824124314134, 62.85331387716630758, 3.547878946066059136 ) ) ;
#29361=DIRECTION ( 'NONE',  ( 0.1006641980670203301, -0.9949204587440765302, 0.000000000000000000 ) ) ;
#29368=VERTEX_POINT ( 'NONE', #19572 ) ;
#29369=CARTESIAN_POINT ( 'NONE',  ( 78.69038500580364826, 66.05859403932464602, -1.083708649521440526 ) ) ;
#29376=CARTESIAN_POINT ( 'NONE',  ( 79.60946285158566127, 65.60230831631017168, 2.836177733672696988 ) ) ;
#29377=CARTESIAN_POINT ( 'NONE',  ( 17.04338035915418459, 48.81061067247630092, 1.000000000000000000 ) ) ;
#29379=CARTESIAN_POINT ( 'NONE',  ( -80.19065981525227471, 31.27226540113728248, 8.800414904976364028 ) ) ;
#29385=CARTESIAN_POINT ( 'NONE',  ( -63.84700662236109281, 35.83977057131359345, 7.343444254794666115 ) ) ;
#29390=CARTESIAN_POINT ( 'NONE',  ( 69.27779986746136842, 58.60568623525134768, 3.981537309218750487 ) ) ;
#29395=CARTESIAN_POINT ( 'NONE',  ( 78.85897125043997846, 66.02047811250265852, -1.830101370957685880 ) ) ;
#29397=DIRECTION ( 'NONE',  ( 7.051707954578238605E-15, 0.9905719730872860618, 0.1369933068947565835 ) ) ;
#29399=ORIENTED_EDGE ( 'NONE', *, *, #29643, .T. ) ;
#29408=CARTESIAN_POINT ( 'NONE',  ( 81.06165217645960297, 61.41816154915739645, -1.973779052376056775 ) ) ;
#29409=CIRCLE ( 'NONE', #23501, 6.329987104167475565 ) ;
#29411=AXIS2_PLACEMENT_3D ( 'NONE', #25790, #16503, #35077 ) ;
#29412=CARTESIAN_POINT ( 'NONE',  ( 78.67172310627759657, 65.99640245491993085, 1.621665796799045101 ) ) ;
#29417=CARTESIAN_POINT ( 'NONE',  ( -58.80557074721224353, 28.82763571155858173, -5.859597094982712306 ) ) ;
#29428=CARTESIAN_POINT ( 'NONE',  ( 79.25461589594502243, 66.09583247779279702, 1.930361577756013691 ) ) ;
#29431=ORIENTED_EDGE ( 'NONE', *, *, #9953, .T. ) ;
#29439=CARTESIAN_POINT ( 'NONE',  ( -58.99872204295123623, 28.48507918597134037, -46.17089178453873188 ) ) ;
#29455=( BOUNDED_CURVE ( )  B_SPLINE_CURVE ( 3, ( #31267, #12920, #25486, #40299 ),
 .UNSPECIFIED., .F., .T. ) 
 B_SPLINE_CURVE_WITH_KNOTS ( ( 4, 4 ),
 ( 4.712388980384689674, 5.617490880575807033 ),
 .UNSPECIFIED. ) 
 CURVE ( )  GEOMETRIC_REPRESENTATION_ITEM ( )  RATIONAL_B_SPLINE_CURVE ( ( 1.000000000000000000, 0.9328897322841716022, 0.9328897322841716022, 1.000000000000000000 ) ) 
 REPRESENTATION_ITEM ( '' )  );
#29456=CARTESIAN_POINT ( 'NONE',  ( -57.29470892912325297, 33.22074752690817689, -3.999999999999999112 ) ) ;
#29460=CARTESIAN_POINT ( 'NONE',  ( 80.25084519670726024, 66.24728552308208407, -1.725837398063457373 ) ) ;
#29468=CARTESIAN_POINT ( 'NONE',  ( 76.89779646338298846, 61.47851784853087054, 3.801074476324135087 ) ) ;
#29475=CARTESIAN_POINT ( 'NONE',  ( 81.93064166251132008, 62.10341262211382229, 1.859759604986720438 ) ) ;
#29498=CARTESIAN_POINT ( 'NONE',  ( 67.20767295658653495, 57.90495500903578829, -3.994504660676310603 ) ) ;
#29499=AXIS2_PLACEMENT_3D ( 'NONE', #20866, #39595, #8909 ) ;
#29511=CARTESIAN_POINT ( 'NONE',  ( 81.02539575022784391, 62.78269734341446195, 3.300462285847920008 ) ) ;
#29513=CARTESIAN_POINT ( 'NONE',  ( -63.63873222603260160, 44.01641787740143030, 2.404113166277060731 ) ) ;
#29515=CARTESIAN_POINT ( 'NONE',  ( 80.27394690667868815, 60.98324426164374046, -1.908681007153611553 ) ) ;
#29518=CARTESIAN_POINT ( 'NONE',  ( 81.21919753141084186, 63.96565923610828008, -3.341858160548294876 ) ) ;
#29519=CARTESIAN_POINT ( 'NONE',  ( 79.36252896413687097, 63.71833510339342155, 3.756013696796373758 ) ) ;
#29523=CARTESIAN_POINT ( 'NONE',  ( 82.58199242721491373, 63.55547749749371178, 1.287552078897677976 ) ) ;
#29524=CARTESIAN_POINT ( 'NONE',  ( -63.55813210593559859, 43.57418346405783183, 2.980081600457315183 ) ) ;
#29526=CARTESIAN_POINT ( 'NONE',  ( -62.74303057475820111, 35.98358351542150046, -5.167368988332354363 ) ) ;
#29543=CARTESIAN_POINT ( 'NONE',  ( 66.86920591220189181, 57.92326096844472261, 3.999524142429984330 ) ) ;
#29544=CARTESIAN_POINT ( 'NONE',  ( 73.12040677118544352, 60.72248633788713335, -3.934110468535476191 ) ) ;
#29554=CARTESIAN_POINT ( 'NONE',  ( 80.91431153141793686, 61.21107275232141376, -1.487544896896259239 ) ) ;
#29556=CARTESIAN_POINT ( 'NONE',  ( 78.85101321104561123, 65.59805058642720610, 2.603857329607151883 ) ) ;
#29574=CARTESIAN_POINT ( 'NONE',  ( 81.05462132553121535, 63.14435662960352147, 3.368075118064897566 ) ) ;
#29580=CARTESIAN_POINT ( 'NONE',  ( -64.78468263673624961, 34.77444586572286767, 6.350676759654645842 ) ) ;
#29584=CARTESIAN_POINT ( 'NONE',  ( 68.99357861020946814, 59.34113723602050783, 3.933428174212677320 ) ) ;
#29586=ORIENTED_EDGE ( 'NONE', *, *, #9436, .F. ) ;
#29587=CARTESIAN_POINT ( 'NONE',  ( -64.08758708074094557, 43.59023632408901960, -1.301703141159380017 ) ) ;
#29590=CARTESIAN_POINT ( 'NONE',  ( 79.25894186866878499, 65.67357942822117423, -2.700485128497464249 ) ) ;
#29598=ORIENTED_EDGE ( 'NONE', *, *, #21243, .F. ) ;
#29600=CARTESIAN_POINT ( 'NONE',  ( 81.02780191652712460, 61.56951766280579363, -2.259810845157016246 ) ) ;
#29602=CARTESIAN_POINT ( 'NONE',  ( 78.68112288793685138, 66.00442204571392324, 1.607835478472332547 ) ) ;
#29607=CARTESIAN_POINT ( 'NONE',  ( -64.08758708074093136, 38.76906266698303227, -3.999999999999999556 ) ) ;
#29613=ORIENTED_EDGE ( 'NONE', *, *, #20485, .T. ) ;
#29622=CARTESIAN_POINT ( 'NONE',  ( 79.20630559137210014, 66.06758606029012526, 1.969816429103250055 ) ) ;
#29643=EDGE_CURVE ( 'NONE', #7364, #16945, #36990, .T. ) ;
#29649=ORIENTED_EDGE ( 'NONE', *, *, #14086, .T. ) ;
#29650=CARTESIAN_POINT ( 'NONE',  ( -56.58158928110403707, 30.30283765713063815, -3.953813256333429837 ) ) ;
#29655=CARTESIAN_POINT ( 'NONE',  ( 82.33210628740326342, 64.54215504103264323, -1.775718711110015224 ) ) ;
#29660=CARTESIAN_POINT ( 'NONE',  ( 74.65712387123647886, 61.84722771748617731, 3.833662259905226133 ) ) ;
#29663=CARTESIAN_POINT ( 'NONE',  ( -56.59682361629209879, 30.63869417066593925, -3.015094993620159425 ) ) ;
#29666=CARTESIAN_POINT ( 'NONE',  ( -62.76709047716261125, 35.75517504125645729, 5.477639365100117175 ) ) ;
#29667=CARTESIAN_POINT ( 'NONE',  ( -59.87552183813137674, 24.84364830758654108, -9.800414904976365804 ) ) ;
#29668=CARTESIAN_POINT ( 'NONE',  ( 78.91303721271685845, 66.16570306020605585, 1.285939662725142485 ) ) ;
#29681=CARTESIAN_POINT ( 'NONE',  ( -63.38664175810290402, 42.64173782962942028, -3.644997060774788800 ) ) ;
#29682=CARTESIAN_POINT ( 'NONE',  ( -63.08758708074093136, 38.76906266698301806, -4.000000000000000000 ) ) ;
#29688=CARTESIAN_POINT ( 'NONE',  ( 67.10107710889761279, 58.19782780592215943, -3.994504660676309271 ) ) ;
#29691=DIRECTION ( 'NONE',  ( -0.9995570907297058882, -0.02975940812527359119, -0.000000000000000000 ) ) ;
#29693=CARTESIAN_POINT ( 'NONE',  ( -59.87552183813137674, 24.84364830758654108, 9.800414904976365804 ) ) ;
#29703=CARTESIAN_POINT ( 'NONE',  ( 81.21856020378538688, 61.45841878490982424, 1.842213953838256257 ) ) ;
#29706=ORIENTED_EDGE ( 'NONE', *, *, #8071, .T. ) ;
#29707=CARTESIAN_POINT ( 'NONE',  ( 79.14505932034367675, 62.66850290118683375, -3.750642650174860204 ) ) ;
#29711=CARTESIAN_POINT ( 'NONE',  ( 80.50924551448741795, 65.11801186547818077, -3.171364025122248353 ) ) ;
#29712=CARTESIAN_POINT ( 'NONE',  ( 77.45101235711661047, 65.18271368322074011, 2.178915381671227891 ) ) ;
#29715=CARTESIAN_POINT ( 'NONE',  ( 81.47320529907104003, 61.46857867680783016, 1.048259027381037489 ) ) ;
#29718=CARTESIAN_POINT ( 'NONE',  ( -64.25913952751385239, 36.58001704789106867, -5.467911005455038165 ) ) ;
#29730=CARTESIAN_POINT ( 'NONE',  ( -66.99872204295122913, 28.48507918597134037, 12.49999999999999645 ) ) ;
#29734=CARTESIAN_POINT ( 'NONE',  ( 66.41604928081299875, 57.80773248233388983, 4.000000000000020428 ) ) ;
#29735=CARTESIAN_POINT ( 'NONE',  ( 72.38109545502503295, 59.26788356430734694, -3.856543183738433633 ) ) ;
#29749=VERTEX_POINT ( 'NONE', #39509 ) ;
#29750=CARTESIAN_POINT ( 'NONE',  ( 80.87678155331657592, 61.19751495238254790, -1.521414672925269995 ) ) ;
#29752=CARTESIAN_POINT ( 'NONE',  ( 80.95922275190024209, 61.28229338972336393, 1.760837461004386428 ) ) ;
#29755=FACE_BOUND ( 'NONE', #20776, .T. ) ;
#29767=CARTESIAN_POINT ( 'NONE',  ( 80.38786582577540685, 64.30167536105096815, 3.588566286536285510 ) ) ;
#29777=CARTESIAN_POINT ( 'NONE',  ( 67.65011695904739497, 58.50773134691538502, 3.985511447369839644 ) ) ;
#29782=CARTESIAN_POINT ( 'NONE',  ( -56.59682361629209879, 30.63869417066593925, 4.000000000000000000 ) ) ;
#29785=CARTESIAN_POINT ( 'NONE',  ( 79.12779906683437048, 65.83686883797783196, -2.419967184825690953 ) ) ;
#29795=CYLINDRICAL_SURFACE ( 'NONE', #30750, 2.500000000000002220 ) ;
#29797=CARTESIAN_POINT ( 'NONE',  ( 79.10907727509470533, 65.55534887285777756, -2.778975589575376937 ) ) ;
#29800=CARTESIAN_POINT ( 'NONE',  ( 80.85530923529174174, 62.40557805022640991, 3.206617288017366452 ) ) ;
#29810=DIRECTION ( 'NONE',  ( 0.4582725098355734938, -0.8888117386314180468, 0.000000000000000000 ) ) ;
#29832=DIRECTION ( 'NONE',  ( 0.2666961468790325918, 0.9637806624122924326, 0.000000000000000000 ) ) ;
#29851=EDGE_LOOP ( 'NONE', ( #5918, #34141, #5808 ) ) ;
#29852=CARTESIAN_POINT ( 'NONE',  ( -57.26775771055921638, 29.21795897888110005, -2.148764163877388444 ) ) ;
#29857=CARTESIAN_POINT ( 'NONE',  ( 82.26850461147272142, 62.50126132183002170, -1.564050819714059681 ) ) ;
#29859=ORIENTED_EDGE ( 'NONE', *, *, #22203, .F. ) ;
#29863=CARTESIAN_POINT ( 'NONE',  ( 75.34312381977423456, 60.33875818837522331, 3.724166978290133212 ) ) ;
#29870=CARTESIAN_POINT ( 'NONE',  ( 81.94417840557107979, 63.58970459987536827, 2.726953404243151358 ) ) ;
#29881=CARTESIAN_POINT ( 'NONE',  ( -69.08758708074093136, -65.19654454972992141, 3.800414904976363140 ) ) ;
#29888=CARTESIAN_POINT ( 'NONE',  ( 67.41558015167861129, 58.24452080056473591, -3.997009152755513384 ) ) ;
#29896=CARTESIAN_POINT ( 'NONE',  ( 78.56550182460473764, 65.96991646449161806, 1.378756462391438786 ) ) ;
#29902=( LENGTH_UNIT ( ) NAMED_UNIT ( * ) SI_UNIT ( .MILLI., .METRE. ) );
#29904=CARTESIAN_POINT ( 'NONE',  ( 80.06561887301042191, 64.50783488872738758, 3.572022490087454649 ) ) ;
#29907=CARTESIAN_POINT ( 'NONE',  ( 78.26672476572068149, 63.69414582742361119, -3.691425412862290756 ) ) ;
#29910=CARTESIAN_POINT ( 'NONE',  ( 81.16342859511064489, 63.93697670172024061, -3.375310687856056369 ) ) ;
#29911=CARTESIAN_POINT ( 'NONE',  ( 77.70122879141796091, 65.35873351754847249, 2.061059937946295495 ) ) ;
#29913=CARTESIAN_POINT ( 'NONE',  ( 82.47906632153727458, 63.16918237499284317, 1.623788564013678659 ) ) ;
#29917=CARTESIAN_POINT ( 'NONE',  ( -64.12237394559149095, 36.72939681796546552, -5.075523754374912322 ) ) ;
#29923=VECTOR ( 'NONE', #22186, 1000.000000000000000 ) ;
#29927=AXIS2_PLACEMENT_3D ( 'NONE', #736, #13273, #38378 ) ;
#29929=DIRECTION ( 'NONE',  ( 0.000000000000000000, 0.000000000000000000, 1.000000000000000000 ) ) ;
#29930=CARTESIAN_POINT ( 'NONE',  ( -75.45330471031414277, 33.71485196875532608, 12.49999999999999645 ) ) ;
#29937=CARTESIAN_POINT ( 'NONE',  ( 66.27376694608996388, 57.73522568913447373, 4.000000000000000000 ) ) ;
#29938=CARTESIAN_POINT ( 'NONE',  ( 73.18282872914367942, 62.10277071170013841, -3.478821770299028948 ) ) ;
#29941=DIRECTION ( 'NONE',  ( -7.215117721222287909E-15, -0.8314686954258618812, 0.5555716052200790900 ) ) ;
#29955=CARTESIAN_POINT ( 'NONE',  ( 80.02751534128088906, 63.03952351013455768, -3.681573067026197243 ) ) ;
#29957=CARTESIAN_POINT ( 'NONE',  ( 80.85057025077259141, 61.36744894077060763, 2.123311106147461658 ) ) ;
#29966=DIRECTION ( 'NONE',  ( 0.9267318687906764829, -0.3757233601570978965, 0.000000000000000000 ) ) ;
#29972=CARTESIAN_POINT ( 'NONE',  ( 81.06839910345442490, 62.80152057670050425, 3.286127602909470813 ) ) ;
#29979=EDGE_CURVE ( 'NONE', #9808, #14204, #11684, .T. ) ;
#29982=CARTESIAN_POINT ( 'NONE',  ( 28.52663967383706023, 50.14399159706753295, 4.000000000000000000 ) ) ;
#29984=CARTESIAN_POINT ( 'NONE',  ( 68.00738522489628224, 58.43930376306189345, 3.995571880668716602 ) ) ;
#29990=CARTESIAN_POINT ( 'NONE',  ( 78.99338515863716736, 65.92867347524024524, -2.125034277891688639 ) ) ;
#29995=CARTESIAN_POINT ( 'NONE',  ( -58.76908243668979281, 27.83904476269672656, 5.922484465878444126 ) ) ;
#29999=DIRECTION ( 'NONE',  ( 1.000000000000000000, 0.000000000000000000, 0.000000000000000000 ) ) ;
#30001=CARTESIAN_POINT ( 'NONE',  ( 79.70909206056978746, 64.65202245283539639, -3.503057693382717996 ) ) ;
#30003=CARTESIAN_POINT ( 'NONE',  ( 81.09055442218992482, 61.42501475223632923, 1.950029235564090913 ) ) ;
#30008=CARTESIAN_POINT ( 'NONE',  ( 76.13754644452941989, 60.10671110989439825, -3.424891502433685453 ) ) ;
#30026=CARTESIAN_POINT ( 'NONE',  ( 80.50924551447106126, 65.11801186546927056, 3.171364025132954456 ) ) ;
#30065=CARTESIAN_POINT ( 'NONE',  ( 80.18989135007151958, 66.21456565649044990, -1.848245342697680815 ) ) ;
#30066=CARTESIAN_POINT ( 'NONE',  ( -73.07498068578524908, 39.58105274722134226, -46.17089178453873188 ) ) ;
#30072=CARTESIAN_POINT ( 'NONE',  ( 75.57967633106541427, 61.33476069914100748, 3.901127667181007119 ) ) ;
#30077=DIRECTION ( 'NONE',  ( 0.2666961468790325918, 0.9637806624122924326, 0.000000000000000000 ) ) ;
#30079=CARTESIAN_POINT ( 'NONE',  ( -75.45330471031414277, 33.71485196875532608, -9.800414904976365804 ) ) ;
#30081=CARTESIAN_POINT ( 'NONE',  ( 79.97870788650307361, 66.10023056730548774, 2.166533184762201358 ) ) ;
#30093=DIRECTION ( 'NONE',  ( -0.000000000000000000, 0.000000000000000000, 1.000000000000000000 ) ) ;
#30099=CARTESIAN_POINT ( 'NONE',  ( -63.08379346057677139, 18.80112958435941906, -46.17089178453873188 ) ) ;
#30104=CARTESIAN_POINT ( 'NONE',  ( 67.37599051809213790, 58.35250968650521486, -3.990882853436547251 ) ) ;
#30110=CARTESIAN_POINT ( 'NONE',  ( 77.23471303065964833, 65.03087687845577136, 2.276447073266238963 ) ) ;
#30116=CARTESIAN_POINT ( 'NONE',  ( 82.18073233876086192, 62.22941084722766902, -1.168532795814369418 ) ) ;
#30117=CARTESIAN_POINT ( 'NONE',  ( 79.39927235112092774, 65.46614203786569419, 2.932725070486263519 ) ) ;
#30120=CARTESIAN_POINT ( 'NONE',  ( 79.57681890279654624, 60.99726435378322975, -2.643019404356985014 ) ) ;
#30123=CARTESIAN_POINT ( 'NONE',  ( 80.84588251005583004, 64.54609234697846887, -3.375310687856057257 ) ) ;
#30124=CARTESIAN_POINT ( 'NONE',  ( 77.65795924533195205, 64.82981391430571705, 2.842954625922254674 ) ) ;
#30126=CARTESIAN_POINT ( 'NONE',  ( 82.41151909044434376, 62.85445852417080914, 1.451695327222104703 ) ) ;
#30149=CARTESIAN_POINT ( 'NONE',  ( 66.42495344877985985, 57.78257748056745413, 4.000000000000011546 ) ) ;
#30150=CARTESIAN_POINT ( 'NONE',  ( 71.70339147920792300, 60.88422586754655441, -3.784404822148339953 ) ) ;
#30161=CARTESIAN_POINT ( 'NONE',  ( 79.22323586724851907, 64.66701280635210480, -3.467090974304450235 ) ) ;
#30163=CARTESIAN_POINT ( 'NONE',  ( 78.83700374940842437, 65.31049604782704421, 2.918211652848220261 ) ) ;
#30177=CARTESIAN_POINT ( 'NONE',  ( 80.77164629763791481, 63.73694215246327133, 3.562450064734656419 ) ) ;
#30186=CARTESIAN_POINT ( 'NONE',  ( 68.04343099365841852, 58.34291608657256489, 3.996230182412897403 ) ) ;
#30196=CARTESIAN_POINT ( 'NONE',  ( -58.20517375958247186, 28.49598760833110944, 5.016376253474285285 ) ) ;
#30203=CARTESIAN_POINT ( 'NONE',  ( 80.83598165300548999, 61.89502789394175863, -2.843122152733553065 ) ) ;
#30207=CARTESIAN_POINT ( 'NONE',  ( 78.83217078968489488, 65.79276158749709680, 2.259810845156947412 ) ) ;
#30213=CARTESIAN_POINT ( 'NONE',  ( 73.50720661118039345, 61.38260725348155944, -3.841642204035220942 ) ) ;
#30214=CARTESIAN_POINT ( 'NONE',  ( -63.99293516169446150, 35.89893413629672381, -12.49999999999999645 ) ) ;
#30216=DIRECTION ( 'NONE',  ( 0.000000000000000000, 0.000000000000000000, -1.000000000000000000 ) ) ;
#30227=EDGE_CURVE ( 'NONE', #18554, #10884, #28624, .T. ) ;
#30230=CARTESIAN_POINT ( 'NONE',  ( 80.71310200136858271, 64.86488640220490254, 3.283621700565936052 ) ) ;
#30246=VERTEX_POINT ( 'NONE', #10498 ) ;
#30252=EDGE_LOOP ( 'NONE', ( #3935, #31074, #980, #17439, #31782 ) ) ;
#30258=CARTESIAN_POINT ( 'NONE',  ( 79.34351131543186852, 65.42632830064326299, -2.956864960647760832 ) ) ;
#30259=CARTESIAN_POINT ( 'NONE',  ( -57.86591918990971806, 28.88504657882484494, -4.653542815086523454 ) ) ;
#30265=CARTESIAN_POINT ( 'NONE',  ( 81.85640814870936310, 64.68575429476366878, -2.512558077908312537 ) ) ;
#30273=CARTESIAN_POINT ( 'NONE',  ( 76.19819836466999163, 59.97076997751576499, 3.322260703561256800 ) ) ;
#30279=CARTESIAN_POINT ( 'NONE',  ( 80.45692750329155274, 65.79057296784172593, 2.573500632437474511 ) ) ;
#30285=FACE_OUTER_BOUND ( 'NONE', #8827, .T. ) ;
#30299=CARTESIAN_POINT ( 'NONE',  ( 66.72638704319571445, 57.85960203741856134, -3.999543855871245945 ) ) ;
#30313=CIRCLE ( 'NONE', #28348, 5.329987104167474676 ) ;
#30315=CARTESIAN_POINT ( 'NONE',  ( 81.47320529907102582, 61.46857867680781595, -1.048259027381222008 ) ) ;
#30317=CARTESIAN_POINT ( 'NONE',  ( 81.21586879471321652, 61.61940358760092806, 2.137206601789639393 ) ) ;
#30321=CARTESIAN_POINT ( 'NONE',  ( 77.32551012344487162, 64.79183443757983696, -2.725046208697011529 ) ) ;
#30325=CARTESIAN_POINT ( 'NONE',  ( 81.01997673013535461, 63.86331202395377460, -3.456914256419913567 ) ) ;
#30326=CARTESIAN_POINT ( 'NONE',  ( 79.57145864546818359, 62.55878779196851269, 3.641957811749160001 ) ) ;
#30327=VERTEX_POINT ( 'NONE', #22604 ) ;
#30332=CARTESIAN_POINT ( 'NONE',  ( 79.65107971589632996, 66.31509156740921185, 1.306649493516908400 ) ) ;
#30342=VERTEX_POINT ( 'NONE', #23395 ) ;
#30359=CARTESIAN_POINT ( 'NONE',  ( 66.27376694608996388, 57.73522568913447373, 4.000000000000000000 ) ) ;
#30360=CARTESIAN_POINT ( 'NONE',  ( 69.15563817390996348, 58.92225492517195562, -3.988427515945576207 ) ) ;
#30369=EDGE_LOOP ( 'NONE', ( #14357, #1658, #22677, #30481 ) ) ;
#30376=CARTESIAN_POINT ( 'NONE',  ( 78.50817655541952433, 65.71198414996337078, -2.174061886842029168 ) ) ;
#30378=CARTESIAN_POINT ( 'NONE',  ( 79.89307030929698783, 66.05340108613441430, -2.264354540981541764 ) ) ;
#30379=CARTESIAN_POINT ( 'NONE',  ( 78.44852601586514140, 65.88695166727248420, 1.521414672925275546 ) ) ;
#30397=CARTESIAN_POINT ( 'NONE',  ( -64.71577923686258771, 34.74117003693350370, 6.230828392942166616 ) ) ;
#30399=CARTESIAN_POINT ( 'NONE',  ( -11.81496944966682960, -21.25669541281728669, -4.000000000000000000 ) ) ;
#30401=CARTESIAN_POINT ( 'NONE',  ( 68.80725167329416081, 58.08536582812667604, 3.941639393089866328 ) ) ;
#30414=CARTESIAN_POINT ( 'NONE',  ( 79.28293246176357911, 65.06528690105534452, -3.252077313700849182 ) ) ;
#30416=CARTESIAN_POINT ( 'NONE',  ( 80.10672643282893546, 63.77302114994544269, 3.692178340560209993 ) ) ;
#30421=CARTESIAN_POINT ( 'NONE',  ( 74.33180802611956040, 62.54477577240981390, -3.494507759124076962 ) ) ;
#30434=CARTESIAN_POINT ( 'NONE',  ( 81.53696963055323010, 62.69563756174483160, 2.920975158735852784 ) ) ;
#30439=EDGE_CURVE ( 'NONE', #8770, #4319, #33691, .T. ) ;
#30445=ADVANCED_FACE ( 'NONE', ( #5470 ), #18880, .T. ) ;
#30453=ORIENTED_EDGE ( 'NONE', *, *, #30439, .F. ) ;
#30454=CARTESIAN_POINT ( 'NONE',  ( 80.91044703854151976, 63.42644682079063045, -3.500437194783537542 ) ) ;
#30466=CARTESIAN_POINT ( 'NONE',  ( 81.13529310646418935, 61.59586411174932152, -2.189516896894245779 ) ) ;
#30467=CARTESIAN_POINT ( 'NONE',  ( -59.35030935981331623, 27.06751177275600995, -5.142387704658982095 ) ) ;
#30473=CARTESIAN_POINT ( 'NONE',  ( 82.09661666296807425, 62.69434707785882921, -2.190303691588676216 ) ) ;
#30477=DIRECTION ( 'NONE',  ( 0.000000000000000000, 0.000000000000000000, -1.000000000000000000 ) ) ;
#30480=CARTESIAN_POINT ( 'NONE',  ( 74.33180802611956040, 62.54477577240979969, 3.494507759124076962 ) ) ;
#30481=ORIENTED_EDGE ( 'NONE', *, *, #27961, .F. ) ;
#30488=CARTESIAN_POINT ( 'NONE',  ( 81.80968396272741927, 62.04343910699811460, 2.011780557866075014 ) ) ;
#30490=CARTESIAN_POINT ( 'NONE',  ( -62.86576508122315943, 38.67912974266877058, -4.000000000000000000 ) ) ;
#30499=EDGE_CURVE ( 'NONE', #446, #36353, #39425, .T. ) ;
#30504=AXIS2_PLACEMENT_3D ( 'NONE', #32205, #16713, #6676 ) ;
#30509=CARTESIAN_POINT ( 'NONE',  ( 66.87706763805377363, 57.90143666482605056, -3.999241724014405364 ) ) ;
#30511=ORIENTED_EDGE ( 'NONE', *, *, #12306, .T. ) ;
#30514=CARTESIAN_POINT ( 'NONE',  ( 66.55049206961604114, 57.90943322382748448, 3.999192535317435571 ) ) ;
#30521=CARTESIAN_POINT ( 'NONE',  ( 81.88789819931514558, 65.48572365615879676, -1.000000000000000000 ) ) ;
#30522=CARTESIAN_POINT ( 'NONE',  ( 81.08836214216863425, 62.22329742272083308, 2.932725070486250196 ) ) ;
#30526=ORIENTED_EDGE ( 'NONE', *, *, #9953, .F. ) ;
#30527=CARTESIAN_POINT ( 'NONE',  ( 79.44050761702638397, 61.30339496468042171, -3.042889847487479038 ) ) ;
#30530=CARTESIAN_POINT ( 'NONE',  ( 81.43870310587888639, 62.97649354279380418, -3.113722587672206554 ) ) ;
#30531=CARTESIAN_POINT ( 'NONE',  ( 78.68856915541800845, 64.27844437337117256, 3.554489553981586170 ) ) ;
#30536=CARTESIAN_POINT ( 'NONE',  ( 82.15576060805999248, 62.21674973124325447, 1.325417871280149429 ) ) ;
#30541=DIRECTION ( 'NONE',  ( -1.000000000000000000, 4.455221922683638036E-15, 0.000000000000000000 ) ) ;
#30567=CARTESIAN_POINT ( 'NONE',  ( 70.70040249450607917, 60.07892802134021792, -3.908768822720051883 ) ) ;
#30572=CARTESIAN_POINT ( 'NONE',  ( -61.00670947824507806, 24.84364830758654108, 8.800414904976364028 ) ) ;
#30579=ORIENTED_EDGE ( 'NONE', *, *, #9020, .F. ) ;
#30584=CARTESIAN_POINT ( 'NONE',  ( 80.20116317610164458, 62.79640268260013158, -3.571698303486882331 ) ) ;
#30587=CARTESIAN_POINT ( 'NONE',  ( 81.36533387373951598, 61.41589781867487829, -1.313329331391850374 ) ) ;
#30588=CARTESIAN_POINT ( 'NONE',  ( 78.66571724150243483, 65.64011997358944939, 2.392122129321807567 ) ) ;
#30601=DIRECTION ( 'NONE',  ( 0.4690749385695657803, 0.8831583674551003460, -0.000000000000000000 ) ) ;
#30615=CARTESIAN_POINT ( 'NONE',  ( 67.62039053056824400, 58.58799842263783120, 3.976226663256290372 ) ) ;
#30625=ORIENTED_EDGE ( 'NONE', *, *, #22203, .T. ) ;
#30628=AXIS2_PLACEMENT_3D ( 'NONE', #9378, #34941, #6309 ) ;
#30631=ORIENTED_EDGE ( 'NONE', *, *, #7388, .T. ) ;
#30632=CARTESIAN_POINT ( 'NONE',  ( 78.89219914629886432, 65.63660985470716014, -2.576318598473995358 ) ) ;
#30634=CARTESIAN_POINT ( 'NONE',  ( 80.76107640992965742, 62.37607017537889931, 3.233326467035614105 ) ) ;
#30638=CARTESIAN_POINT ( 'NONE',  ( 74.39246203999459794, 62.41596060291494297, -3.584990529380562840 ) ) ;
#30650=CARTESIAN_POINT ( 'NONE',  ( 81.25398435008600018, 63.24110186484338669, 3.279590910093575840 ) ) ;
#30662=CARTESIAN_POINT ( 'NONE',  ( -63.03213158086253287, 38.26878225442504800, 4.032857076801014351 ) ) ;
#30668=CARTESIAN_POINT ( 'NONE',  ( 79.92139222979439239, 65.15389119341904234, -3.261148789966887840 ) ) ;
#30675=CARTESIAN_POINT ( 'NONE',  ( -2.954197855305039422, -12.43481156997016157, 1.000000000000000000 ) ) ;
#30676=VERTEX_POINT ( 'NONE', #22453 ) ;
#30679=CARTESIAN_POINT ( 'NONE',  ( 80.65823571794965119, 63.30623879605501259, -3.578839808218915230 ) ) ;
#30681=CARTESIAN_POINT ( 'NONE',  ( -58.83253814471410692, 27.61819298006735224, -3.984408728655165710 ) ) ;
#30686=VERTEX_POINT ( 'NONE', #28196 ) ;
#30687=CARTESIAN_POINT ( 'NONE',  ( 82.15165036511221786, 63.00212529317509080, -2.340562087103692956 ) ) ;
#30690=DIRECTION ( 'NONE',  ( 0.9267318687906785923, -0.3757233601570932335, 2.607104533349591435E-15 ) ) ;
#30693=CARTESIAN_POINT ( 'NONE',  ( 75.02040913282911561, 59.50525224047964201, 3.395557233589185042 ) ) ;
#30703=CARTESIAN_POINT ( 'NONE',  ( 81.83960663661416390, 62.56551448482344568, 2.484976468875359057 ) ) ;
#30721=DIRECTION ( 'NONE',  ( -1.000000000000000000, -5.331188706255073750E-15, 0.000000000000000000 ) ) ;
#30722=CARTESIAN_POINT ( 'NONE',  ( 66.94886299149460740, 58.16124406473343811, -3.993952884371009926 ) ) ;
#30726=ORIENTED_EDGE ( 'NONE', *, *, #26958, .T. ) ;
#30729=CARTESIAN_POINT ( 'NONE',  ( 76.21257126924976433, 64.31732071985945254, 2.649600530246794872 ) ) ;
#30735=CARTESIAN_POINT ( 'NONE',  ( 81.88789819931514558, 65.48572365615879676, -1.161365684106807850 ) ) ;
#30736=CARTESIAN_POINT ( 'NONE',  ( 80.42360172120015704, 63.56407742133696104, 3.661914029440276330 ) ) ;
#30740=CARTESIAN_POINT ( 'NONE',  ( 78.71019189666368732, 60.57837954350633680, -2.701592190110933878 ) ) ;
#30743=EDGE_CURVE ( 'NONE', #8555, #5492, #26649, .T. ) ;
#30744=AXIS2_PLACEMENT_3D ( 'NONE', #35448, #9485, #3553 ) ;
#30746=CARTESIAN_POINT ( 'NONE',  ( 80.79838846786208251, 64.52093256242186214, -3.402511877377343286 ) ) ;
#30747=CARTESIAN_POINT ( 'NONE',  ( 79.50866325991141537, 61.15032965923190034, 2.842954625922348821 ) ) ;
#30750=AXIS2_PLACEMENT_3D ( 'NONE', #32497, #20317, #29999 ) ;
#30751=EDGE_CURVE ( 'NONE', #7709, #32308, #32039, .T. ) ;
#30753=CARTESIAN_POINT ( 'NONE',  ( 81.94344439483592168, 61.95170768642839221, 1.250177805244208740 ) ) ;
#30763=CARTESIAN_POINT ( 'NONE',  ( 80.30486976649511632, 60.99341039245124563, 1.909076843291450443 ) ) ;
#30764=DIRECTION ( 'NONE',  ( 1.000000000000000000, 0.000000000000000000, 0.000000000000000000 ) ) ;
#30779=CARTESIAN_POINT ( 'NONE',  ( 69.23715119732055712, 58.71109548446294468, -3.988427515945585089 ) ) ;
#30784=CARTESIAN_POINT ( 'NONE',  ( 70.02038816076994010, 58.42250406220534131, 3.901551322707178304 ) ) ;
#30793=CARTESIAN_POINT ( 'NONE',  ( 79.79522905248630593, 63.61080392591205168, -3.730195463674648604 ) ) ;
#30796=CARTESIAN_POINT ( 'NONE',  ( 81.53193199008818226, 61.58838919619021368, -1.571309534768102090 ) ) ;
#30797=CARTESIAN_POINT ( 'NONE',  ( 78.41749725426429052, 65.86496093260605278, 1.552792442904350034 ) ) ;
#30804=ORIENTED_EDGE ( 'NONE', *, *, #16875, .F. ) ;
#30808=FACE_BOUND ( 'NONE', #27155, .T. ) ;
#30818=DIRECTION ( 'NONE',  ( -0.000000000000000000, -0.000000000000000000, -1.000000000000000000 ) ) ;
#30821=CARTESIAN_POINT ( 'NONE',  ( 67.53434038244741089, 57.92037869207645429, 3.987264345885670913 ) ) ;
#30831=CARTESIAN_POINT ( 'NONE',  ( -68.71186372058383540, 37.81212149306784909, 9.800414904976364028 ) ) ;
#30836=CARTESIAN_POINT ( 'NONE',  ( 81.02662073326128223, 61.25180701697230035, -1.364493914842159539 ) ) ;
#30838=CARTESIAN_POINT ( 'NONE',  ( 79.84444348018428173, 64.37461814510217550, 3.624000857162003264 ) ) ;
#30842=CARTESIAN_POINT ( 'NONE',  ( 74.45643886899652841, 62.27924959144220196, -3.661998389317300706 ) ) ;
#30857=CARTESIAN_POINT ( 'NONE',  ( 79.12689763788453945, 66.01933680498311219, 2.028924249969734195 ) ) ;
#30863=AXIS2_PLACEMENT_3D ( 'NONE', #26201, #28879, #32385 ) ;
#30864=VERTEX_POINT ( 'NONE', #16845 ) ;
#30865=DIRECTION ( 'NONE',  ( 1.000000000000000000, 0.000000000000000000, 0.000000000000000000 ) ) ;
#30867=CARTESIAN_POINT ( 'NONE',  ( -1.432293644835494373, -27.47664038617742577, 4.000000000000000000 ) ) ;
#30876=CARTESIAN_POINT ( 'NONE',  ( 79.06971639787833794, 65.98240043192647875, -2.069468987430130635 ) ) ;
#30883=ORIENTED_EDGE ( 'NONE', *, *, #452, .T. ) ;
#30884=CARTESIAN_POINT ( 'NONE',  ( 80.20683918224331421, 64.20264744734686246, -3.640670270625566918 ) ) ;
#30885=CARTESIAN_POINT ( 'NONE',  ( -58.75407610588014506, 29.59432899155028807, -5.651746018159727214 ) ) ;
#30890=CARTESIAN_POINT ( 'NONE',  ( 81.98790212893277385, 62.35967063417181322, -2.110636331688536593 ) ) ;
#30898=CARTESIAN_POINT ( 'NONE',  ( 73.54169881536046205, 59.75047131450637750, 3.824679913398719044 ) ) ;
#30907=CARTESIAN_POINT ( 'NONE',  ( 81.16644189562721579, 61.30283181452514185, 1.054034669007994252 ) ) ;
#30925=CARTESIAN_POINT ( 'NONE',  ( 66.84561829912908593, 57.98873651192412382, -3.999241724016630251 ) ) ;
#30933=CARTESIAN_POINT ( 'NONE',  ( 66.96277167016233989, 58.17005278565000026, 3.993702900079018292 ) ) ;
#30939=CARTESIAN_POINT ( 'NONE',  ( 82.10909544300281482, 65.20937546977818045, -1.165579324820864571 ) ) ;
#30940=CARTESIAN_POINT ( 'NONE',  ( 81.15397050155256409, 61.44050475792813870, 1.896863055073854332 ) ) ;
#30944=CARTESIAN_POINT ( 'NONE',  ( 76.31986902294666208, 64.06746608568099077, -3.012346708716354016 ) ) ;
#30948=CARTESIAN_POINT ( 'NONE',  ( 78.68070521837707076, 66.05171761244720585, -1.104694797982641363 ) ) ;
#30949=CARTESIAN_POINT ( 'NONE',  ( 77.76298154960849729, 62.57953843473563893, 3.839379600940513892 ) ) ;
#30954=CARTESIAN_POINT ( 'NONE',  ( 79.92383974732996421, 66.30194418458920325, 1.599335268229121754 ) ) ;
#30955=CARTESIAN_POINT ( 'NONE',  ( -64.08758708074097399, 41.34492105184755673, 2.999999999999999112 ) ) ;
#30960=CARTESIAN_POINT ( 'NONE',  ( -64.62035675219918573, 36.25855371424984952, 6.071883532254790161 ) ) ;
#30962=DIRECTION ( 'NONE',  ( -0.3757233601570971193, -0.9267318687906769270, 0.000000000000000000 ) ) ;
#30980=CARTESIAN_POINT ( 'NONE',  ( 69.72614016916874391, 59.17085620800508394, -3.982895692900132456 ) ) ;
#30993=CARTESIAN_POINT ( 'NONE',  ( -75.45330471031414277, 33.71485196875532608, -12.49999999999999645 ) ) ;
#30997=CARTESIAN_POINT ( 'NONE',  ( 80.23310653198076636, 61.53645999506316855, -2.845586111146968911 ) ) ;
#30999=CARTESIAN_POINT ( 'NONE',  ( 80.71114116412915962, 65.59088185864118259, -2.713791510777194382 ) ) ;
#31000=CARTESIAN_POINT ( 'NONE',  ( 78.59965762292412705, 65.58148208812491475, 2.436540443961506597 ) ) ;
#31023=CARTESIAN_POINT ( 'NONE',  ( 67.01778322055632486, 57.97087264248310134, 3.999241514195644775 ) ) ;
#31040=CARTESIAN_POINT ( 'NONE',  ( 79.03702048636715460, 65.49184929578454728, -2.818206040476802343 ) ) ;
#31042=CARTESIAN_POINT ( 'NONE',  ( 80.48752863069321961, 62.90068369996134834, 3.525318766974259166 ) ) ;
#31056=CARTESIAN_POINT ( 'NONE',  ( 81.34501369141621296, 61.50378551383993653, 1.741375869723579273 ) ) ;
#31058=FACE_OUTER_BOUND ( 'NONE', #2920, .T. ) ;
#31060=CARTESIAN_POINT ( 'NONE',  ( -64.08758708074093136, 35.89366350591650701, -3.939604612811969719 ) ) ;
#31066=CARTESIAN_POINT ( 'NONE',  ( -64.95171866297674512, 36.28765213650432742, -6.629387290673639299 ) ) ;
#31074=ORIENTED_EDGE ( 'NONE', *, *, #386, .T. ) ;
#31075=CARTESIAN_POINT ( 'NONE',  ( 81.23980251882781545, 61.36242252098747940, -1.459100623883069048 ) ) ;
#31084=CARTESIAN_POINT ( 'NONE',  ( 81.17684021745370160, 61.76890268566524611, -2.450942308261408353 ) ) ;
#31085=EDGE_CURVE ( 'NONE', #21319, #28100, #4903, .T. ) ;
#31086=CARTESIAN_POINT ( 'NONE',  ( -58.93521193748836140, 27.64319143539497148, -6.467610917686843486 ) ) ;
#31091=CARTESIAN_POINT ( 'NONE',  ( 80.77640933968160653, 65.62578451531314272, -2.636331425444868870 ) ) ;
#31098=CARTESIAN_POINT ( 'NONE',  ( 74.40173173411091057, 59.34324565254589601, 3.478821770173325501 ) ) ;
#31106=CARTESIAN_POINT ( 'NONE',  ( 81.81758241818920396, 62.27516227682820471, 2.299173245602474935 ) ) ;
#31109=AXIS2_PLACEMENT_3D ( 'NONE', #40633, #25003, #23326 ) ;
#31118=EDGE_CURVE ( 'NONE', #2581, #31697, #7706, .T. ) ;
#31125=CARTESIAN_POINT ( 'NONE',  ( 66.95869957004099149, 58.13407781516350070, -3.995640437668403155 ) ) ;
#31129=FACE_OUTER_BOUND ( 'NONE', #5216, .T. ) ;
#31135=CARTESIAN_POINT ( 'NONE',  ( 78.99916064199128130, 66.21331998952629760, -1.048259027381222008 ) ) ;
#31136=CARTESIAN_POINT ( 'NONE',  ( 79.01164091803718748, 65.74483092438761389, 2.494286432550486321 ) ) ;
#31139=CARTESIAN_POINT ( 'NONE',  ( 76.36824339142350482, 62.58715529212016548, -3.801074476319113327 ) ) ;
#31144=CARTESIAN_POINT ( 'NONE',  ( 79.20630559137384807, 66.06758606029085001, -1.969816429101940214 ) ) ;
#31145=CARTESIAN_POINT ( 'NONE',  ( 78.34663729941155452, 61.36874863982431094, 3.480716904142319379 ) ) ;
#31151=CARTESIAN_POINT ( 'NONE',  ( -57.69469465617550696, 32.53235267577638723, 4.116732114020066113 ) ) ;
#31152=CARTESIAN_POINT ( 'NONE',  ( 78.95874065903555561, 66.19121013986816138, 1.203271478923122251 ) ) ;
#31153=CARTESIAN_POINT ( 'NONE',  ( -64.08758708074093136, 43.50655619156261622, 1.588711929256377831 ) ) ;
#31158=CARTESIAN_POINT ( 'NONE',  ( -64.53809346645429912, 34.68836506924190388, 5.879071147244312456 ) ) ;
#31163=CARTESIAN_POINT ( 'NONE',  ( 80.84593566081812810, 61.18628925133899799, 1.559654057697081875 ) ) ;
#31169=DIRECTION ( 'NONE',  ( -1.000000000000000000, 0.000000000000000000, 0.000000000000000000 ) ) ;
#31178=CARTESIAN_POINT ( 'NONE',  ( 70.93434718597480071, 59.50194243796293136, -3.976054184260643609 ) ) ;
#31192=CARTESIAN_POINT ( 'NONE',  ( 80.45616750117871163, 61.42990784962029949, -2.551437666014049643 ) ) ;
#31194=CARTESIAN_POINT ( 'NONE',  ( 80.93893743487447523, 65.34845912995858441, -2.808566127056343564 ) ) ;
#31196=CARTESIAN_POINT ( 'NONE',  ( 78.76746739705249922, 65.24896075961403596, 2.948506306558721590 ) ) ;
#31199=CARTESIAN_POINT ( 'NONE',  ( 81.88789819931513136, 65.48572365615882518, 1.000000000000000000 ) ) ;
#31220=FACE_OUTER_BOUND ( 'NONE', #32914, .T. ) ;
#31224=CARTESIAN_POINT ( 'NONE',  ( 66.97346358352143625, 58.09330026553017490, 3.997553359131192696 ) ) ;
#31235=ORIENTED_EDGE ( 'NONE', *, *, #6816, .T. ) ;
#31240=ORIENTED_EDGE ( 'NONE', *, *, #17927, .T. ) ;
#31242=CARTESIAN_POINT ( 'NONE',  ( 79.37660656468217724, 64.78470313322911522, -3.432573985763849311 ) ) ;
#31245=CARTESIAN_POINT ( 'NONE',  ( 78.61081429290072720, 65.94468767047428059, 1.703597047176659940 ) ) ;
#31247=VERTEX_POINT ( 'NONE', #16006 ) ;
#31249=CARTESIAN_POINT ( 'NONE',  ( -58.90952946163269388, 28.52995886935198300, 6.184968675637443347 ) ) ;
#31254=EDGE_CURVE ( 'NONE', #12078, #27566, #7061, .T. ) ;
#31263=CARTESIAN_POINT ( 'NONE',  ( 81.29658979812207065, 62.90761208998647902, 3.189931650267155749 ) ) ;
#31267=CARTESIAN_POINT ( 'NONE',  ( -69.08758708074093136, 36.88538962427716683, 8.800414904976364028 ) ) ;
#31271=CARTESIAN_POINT ( 'NONE',  ( -68.71186372058383540, 37.81212149306784909, -9.800414904976365804 ) ) ;
#31278=CARTESIAN_POINT ( 'NONE',  ( 81.21493646480149664, 62.54560775605910550, -3.083955809406642601 ) ) ;
#31287=EDGE_LOOP ( 'NONE', ( #2701, #35421, #24948, #6776 ) ) ;
#31288=CARTESIAN_POINT ( 'NONE',  ( 80.20530801487242911, 63.82446735998111365, -3.674973878998262666 ) ) ;
#31295=CARTESIAN_POINT ( 'NONE',  ( 81.07711124303935435, 65.42186869171261776, -2.645340681430279339 ) ) ;
#31303=CARTESIAN_POINT ( 'NONE',  ( 73.73614897715009420, 59.29615633563123822, 3.619654763491260585 ) ) ;
#31309=ORIENTED_EDGE ( 'NONE', *, *, #23744, .F. ) ;
#31311=CARTESIAN_POINT ( 'NONE',  ( 78.68779346184201984, 66.05675297672225099, 1.054034669007998026 ) ) ;
#31329=CARTESIAN_POINT ( 'NONE',  ( 66.43187891275414358, 57.76301247919344206, -4.000000000000007994 ) ) ;
#31330=VERTEX_POINT ( 'NONE', #26928 ) ;
#31331=CARTESIAN_POINT ( 'NONE',  ( -57.97698207090199674, 31.94645990616745834, 4.307980060361010999 ) ) ;
#31337=ORIENTED_EDGE ( 'NONE', *, *, #37321, .F. ) ;
#31339=CARTESIAN_POINT ( 'NONE',  ( 82.13789946638775064, 62.20769933019765574, -1.398807481800598662 ) ) ;
#31340=CARTESIAN_POINT ( 'NONE',  ( 79.60112097352363492, 64.95058993122677293, 3.372125408468117591 ) ) ;
#31343=CARTESIAN_POINT ( 'NONE',  ( 76.81167355577591138, 60.15069890908841899, -3.230144225296931904 ) ) ;
#31347=CARTESIAN_POINT ( 'NONE',  ( 81.15350626233055209, 61.29809656771022475, -1.122020883098639565 ) ) ;
#31348=CARTESIAN_POINT ( 'NONE',  ( 76.75621762107158474, 64.55157797518404550, 2.701592190110927216 ) ) ;
#31355=CARTESIAN_POINT ( 'NONE',  ( 81.41819469040454749, 65.60226997055954712, 2.078018481492983405 ) ) ;
#31359=AXIS2_PLACEMENT_3D ( 'NONE', #3306, #18700, #3100 ) ;
#31362=CARTESIAN_POINT ( 'NONE',  ( -62.81463675898083210, 36.67811266762162603, -4.600311178732273021 ) ) ;
#31378=CARTESIAN_POINT ( 'NONE',  ( 68.71160781503239434, 58.33825098880495119, -3.980709302925372839 ) ) ;
#31393=CARTESIAN_POINT ( 'NONE',  ( 78.40460260197330911, 65.77602943765538157, -1.910479420724411570 ) ) ;
#31396=CARTESIAN_POINT ( 'NONE',  ( 81.12957769509920070, 64.69578868775869296, -3.179853676209053237 ) ) ;
#31397=CARTESIAN_POINT ( 'NONE',  ( 79.70629046221083058, 63.56464109829104814, 3.738478073092014853 ) ) ;
#31402=FACE_OUTER_BOUND ( 'NONE', #2796, .T. ) ;
#31410=CARTESIAN_POINT ( 'NONE',  ( -11.81496944966682960, -21.25669541281728669, 1.000000000000000000 ) ) ;
#31416=DIRECTION ( 'NONE',  ( 0.9267318687906785923, -0.3757233601570932335, 0.000000000000000000 ) ) ;
#31426=ORIENTED_EDGE ( 'NONE', *, *, #29643, .F. ) ;
#31428=CARTESIAN_POINT ( 'NONE',  ( 67.05223802139354916, 57.87567627276845883, 3.996315564296190725 ) ) ;
#31432=B_SPLINE_CURVE_WITH_KNOTS ( 'NONE', 3,
 ( #24861, #161, #3671, #15797, #12902, #25468, #15990, #37401, #28761, #9397, #34765, #5921, #6125, #572, #31249, #3273, #2854, #8989, #6539, #21574, #3070, #15375, #34560, #3468 ),
 .UNSPECIFIED., .F., .F.,
 ( 4, 2, 2, 2, 2, 2, 2, 2, 2, 2, 2, 4 ),
 ( 0.000000000000000000, 0.0006665208131132561780, 0.001333041626226512356, 0.001999562439339766691, 0.002666083252453021243, 0.003999124878679529912, 0.004332385285236159574, 0.004665645691792788367, 0.004832275895071106234, 0.004998906098349424100, 0.005165536301627741099, 0.005332166504906058965 ),
 .UNSPECIFIED. ) ;
#31437=DIRECTION ( 'NONE',  ( -0.000000000000000000, -0.000000000000000000, -1.000000000000000000 ) ) ;
#31444=CARTESIAN_POINT ( 'NONE',  ( 80.54480326438822146, 62.60292565479354465, -3.426353657592656976 ) ) ;
#31446=CARTESIAN_POINT ( 'NONE',  ( 78.52594532581824183, 65.94185624388921951, 1.429680343938493081 ) ) ;
#31463=CARTESIAN_POINT ( 'NONE',  ( 78.80232334588868071, 66.09893194982535647, 1.428845309148514486 ) ) ;
#31479=EDGE_LOOP ( 'NONE', ( #33476, #5031, #5116 ) ) ;
#31480=CARTESIAN_POINT ( 'NONE',  ( 81.23328907848382130, 61.46306935600725296, -1.830101370957703200 ) ) ;
#31487=ORIENTED_EDGE ( 'NONE', *, *, #36633, .T. ) ;
#31489=ORIENTED_EDGE ( 'NONE', *, *, #6829, .F. ) ;
#31490=CARTESIAN_POINT ( 'NONE',  ( 80.85530923529172753, 62.40557805022640991, -3.206617288017365119 ) ) ;
#31496=CARTESIAN_POINT ( 'NONE',  ( 82.00886418671275635, 63.26204695399086120, -2.636331425444868870 ) ) ;
#31503=CARTESIAN_POINT ( 'NONE',  ( 73.12040677118544352, 60.72248633788713335, 3.934110468535477079 ) ) ;
#31507=VECTOR ( 'NONE', #2520, 1000.000000000000000 ) ;
#31509=CARTESIAN_POINT ( 'NONE',  ( -58.28276732369787538, 31.18492359376757150, -4.639233030986043893 ) ) ;
#31511=CARTESIAN_POINT ( 'NONE',  ( 80.40506551886733178, 65.76252680069860901, 2.626729253126741881 ) ) ;
#31515=ADVANCED_FACE ( 'NONE', ( #28565 ), #26096, .T. ) ;
#31519=LINE ( 'NONE', #31723, #13448 ) ;
#31529=CARTESIAN_POINT ( 'NONE',  ( 66.41407057682044979, 57.81332248272632057, -4.000000000000023981 ) ) ;
#31539=ORIENTED_EDGE ( 'NONE', *, *, #19410, .T. ) ;
#31544=CARTESIAN_POINT ( 'NONE',  ( 78.69027363540493525, 66.05851491966868139, -1.011532654301245060 ) ) ;
#31545=CARTESIAN_POINT ( 'NONE',  ( 80.60461247708464327, 63.28149962716669563, 3.592474444481852824 ) ) ;
#31548=CARTESIAN_POINT ( 'NONE',  ( 77.06776432268853227, 63.96223838934590589, -3.363831406679916203 ) ) ;
#31552=CARTESIAN_POINT ( 'NONE',  ( 80.90189697519821266, 63.80306449575952144, -3.509897338575004966 ) ) ;
#31553=CARTESIAN_POINT ( 'NONE',  ( 76.98094665547928628, 64.12925941789167439, 3.220231295875716437 ) ) ;
#31558=CARTESIAN_POINT ( 'NONE',  ( 81.88210331175126555, 61.92077230045141789, 1.461108304021874416 ) ) ;
#31581=VERTEX_POINT ( 'NONE', #21783 ) ;
#31583=CARTESIAN_POINT ( 'NONE',  ( 68.58273017919226788, 58.67848115723035107, -3.992679187475148161 ) ) ;
#31594=AXIS2_PLACEMENT_3D ( 'NONE', #3692, #4278, #32480 ) ;
#31597=DIRECTION ( 'NONE',  ( 0.000000000000000000, 0.000000000000000000, 1.000000000000000000 ) ) ;
#31599=CARTESIAN_POINT ( 'NONE',  ( 78.31969284963511768, 65.55289002357415029, -2.305838555344981611 ) ) ;
#31602=CARTESIAN_POINT ( 'NONE',  ( 81.16407079065466235, 61.30196360636987407, -1.071687152255755171 ) ) ;
#31603=CARTESIAN_POINT ( 'NONE',  ( 80.61353453797053703, 61.63497835834533589, 2.716276829189518960 ) ) ;
#31605=CARTESIAN_POINT ( 'NONE',  ( 82.35470118046110599, 62.54510421749742477, 1.000000000000000000 ) ) ;
#31629=CARTESIAN_POINT ( 'NONE',  ( 67.16030903438456789, 58.03511467963866011, 3.999036733496184048 ) ) ;
#31634=AXIS2_PLACEMENT_3D ( 'NONE', #32894, #7560, #4681 ) ;
#31644=PRODUCT_DEFINITION_CONTEXT ( 'detailed design', #25032, 'design' ) ;
#31648=CARTESIAN_POINT ( 'NONE',  ( 78.94919473400545940, 65.41189549592658636, -2.864416008774570699 ) ) ;
#31650=CARTESIAN_POINT ( 'NONE',  ( 78.77165107407959965, 65.73683965358550552, 2.311104455577570604 ) ) ;
#31654=AXIS2_PLACEMENT_3D ( 'NONE', #32345, #10686, #29832 ) ;
#31667=CARTESIAN_POINT ( 'NONE',  ( 81.34140156818916978, 61.66514490546133942, 2.058202901128784568 ) ) ;
#31671=PLANE ( 'NONE',  #39138 ) ;
#31682=CARTESIAN_POINT ( 'NONE',  ( 79.33528816075221357, 65.72664079943768911, -2.661900242191241439 ) ) ;
#31683=CARTESIAN_POINT ( 'NONE',  ( -63.84790524989455918, 35.84013490037983729, 7.344445564913357316 ) ) ;
#31687=VERTEX_POINT ( 'NONE', #28969 ) ;
#31693=CARTESIAN_POINT ( 'NONE',  ( 78.63380675089919691, 66.01840951946610403, -1.252362053669528796 ) ) ;
#31697=VERTEX_POINT ( 'NONE', #19893 ) ;
#31699=CARTESIAN_POINT ( 'NONE',  ( 81.83803008603277362, 64.28563725689721764, -2.776691787112390397 ) ) ;
#31704=CARTESIAN_POINT ( 'NONE',  ( -64.08758708074091714, 41.79021386906870816, -3.815602545441736826 ) ) ;
#31705=CARTESIAN_POINT ( 'NONE',  ( 71.95566904218743787, 60.28642714153433957, 3.942504219403033527 ) ) ;
#31706=EDGE_CURVE ( 'NONE', #7366, #34454, #26612, .T. ) ;
#31713=CARTESIAN_POINT ( 'NONE',  ( 79.69124582246557509, 65.94093779614271966, 2.443770662203109900 ) ) ;
#31717=CARTESIAN_POINT ( 'NONE',  ( -63.08758708074093136, 41.04287353446839859, -4.000000000000000000 ) ) ;
#31718=ORIENTED_EDGE ( 'NONE', *, *, #39409, .T. ) ;
#31723=CARTESIAN_POINT ( 'NONE',  ( -60.75950795826495465, 23.17721540975219696, 12.49999999999999645 ) ) ;
#31734=CARTESIAN_POINT ( 'NONE',  ( 66.42198539279098668, 57.79096248115614998, -4.000000000000016875 ) ) ;
#31735=ORIENTED_EDGE ( 'NONE', *, *, #26328, .F. ) ;
#31742=ORIENTED_EDGE ( 'NONE', *, *, #23966, .T. ) ;
#31744=CARTESIAN_POINT ( 'NONE',  ( 79.33847868486726895, 66.30689617902910982, -1.090531591958677327 ) ) ;
#31746=CARTESIAN_POINT ( 'NONE',  ( 80.83002518733269426, 62.39751428130118427, 3.213872034465152350 ) ) ;
#31750=CARTESIAN_POINT ( 'NONE',  ( 76.28050337382489943, 62.76811984040514858, -3.753756190325745035 ) ) ;
#31754=CARTESIAN_POINT ( 'NONE',  ( 81.14353007428546505, 63.18723978346947945, -3.330128783915603297 ) ) ;
#31755=CARTESIAN_POINT ( 'NONE',  ( 77.97077402951191516, 60.66921691151922857, 3.160174624583325986 ) ) ;
#31759=CARTESIAN_POINT ( 'NONE',  ( -64.08758708074093136, 24.84364830758653397, -3.800414904976364028 ) ) ;
#31760=CARTESIAN_POINT ( 'NONE',  ( 82.20862031248780966, 64.47799227860164706, 2.164558651853291771 ) ) ;
#31767=CARTESIAN_POINT ( 'NONE',  ( -64.42495406928411228, 36.58927325464082259, 5.700117363500042167 ) ) ;
#31771=CARTESIAN_POINT ( 'NONE',  ( 69.57070405849451333, 58.21122316646445682, 3.900048895444411023 ) ) ;
#31782=ORIENTED_EDGE ( 'NONE', *, *, #40621, .T. ) ;
#31785=CARTESIAN_POINT ( 'NONE',  ( 68.69556364554829031, 58.38064408996493171, -3.985059344218202515 ) ) ;
#31787=ORIENTED_EDGE ( 'NONE', *, *, #8590, .T. ) ;
#31797=CARTESIAN_POINT ( 'NONE',  ( 78.84693035237091863, 66.01116107573028557, 1.842213953838237384 ) ) ;
#31802=CARTESIAN_POINT ( 'NONE',  ( 79.36252896413687097, 63.71833510339342155, -3.756013696796374202 ) ) ;
#31805=CARTESIAN_POINT ( 'NONE',  ( 81.68688842593499544, 61.98347795596144749, -2.134710458528695121 ) ) ;
#31806=CARTESIAN_POINT ( 'NONE',  ( 79.98243830041433000, 63.02105934045280833, 3.686141857899485341 ) ) ;
#31808=ADVANCED_FACE ( 'NONE', ( #18213 ), #39970, .T. ) ;
#31811=CARTESIAN_POINT ( 'NONE',  ( -63.16167114476460398, 41.43486696125795277, 4.000000000000000000 ) ) ;
#31818=EDGE_CURVE ( 'NONE', #33155, #33614, #3837, .T. ) ;
#31834=ORIENTED_EDGE ( 'NONE', *, *, #31085, .F. ) ;
#31835=CARTESIAN_POINT ( 'NONE',  ( 66.86527468745164526, 57.93417386730686758, 3.999594749379963066 ) ) ;
#31839=VECTOR ( 'NONE', #22496, 1000.000000000000000 ) ;
#31848=CARTESIAN_POINT ( 'NONE',  ( 78.87073352949229843, 65.61655597148102004, -2.590854534519451580 ) ) ;
#31850=CARTESIAN_POINT ( 'NONE',  ( 80.86726794284579967, 61.90233618827342355, 2.830664096605171931 ) ) ;
#31860=CARTESIAN_POINT ( 'NONE',  ( -64.94969296618683074, 34.86786693855481900, -6.612442482648054565 ) ) ;
#31864=AXIS2_PLACEMENT_3D ( 'NONE', #22157, #37568, #3443 ) ;
#31872=CARTESIAN_POINT ( 'NONE',  ( 79.22467975445889010, 65.90355157830849464, 2.361823859647586232 ) ) ;
#31875=FACE_OUTER_BOUND ( 'NONE', #13599, .T. ) ;
#31885=CARTESIAN_POINT ( 'NONE',  ( 68.64726599134355922, 58.50818873767699557, 3.992679187475169922 ) ) ;
#31887=AXIS2_PLACEMENT_3D ( 'NONE', #10932, #16909, #23511 ) ;
#31890=ORIENTED_EDGE ( 'NONE', *, *, #2688, .F. ) ;
#31891=CARTESIAN_POINT ( 'NONE',  ( 81.20826633916702519, 61.35171532218112844, -1.496866203714589449 ) ) ;
#31895=ORIENTED_EDGE ( 'NONE', *, *, #32245, .F. ) ;
#31901=CARTESIAN_POINT ( 'NONE',  ( 78.62614802285547455, 66.01297166972811681, -1.268354304253246800 ) ) ;
#31906=CARTESIAN_POINT ( 'NONE',  ( 79.43434746088962584, 66.19712225821032803, -1.744953761006743598 ) ) ;
#31908=CARTESIAN_POINT ( 'NONE',  ( -57.37156913083832421, 30.38049303703153470, -3.770258250959034996 ) ) ;
#31910=CARTESIAN_POINT ( 'NONE',  ( 81.16957891225059996, 61.30398062001309256, 4.000000000000000000 ) ) ;
#31911=CARTESIAN_POINT ( 'NONE',  ( -64.08758708074093136, 42.61892514857068193, -2.587732768873741929 ) ) ;
#31912=CARTESIAN_POINT ( 'NONE',  ( 69.57837460818548436, 59.54477471642375974, 3.931953536312648989 ) ) ;
#31922=CARTESIAN_POINT ( 'NONE',  ( 79.46506916754634631, 66.04886526173142158, 2.198649373794023809 ) ) ;
#31943=CARTESIAN_POINT ( 'NONE',  ( 66.70577848186255210, 57.91700714588437648, -3.999628797553631543 ) ) ;
#31956=CARTESIAN_POINT ( 'NONE',  ( 82.49284700683510607, 64.23424719397910110, -1.468380750528963663 ) ) ;
#31962=CARTESIAN_POINT ( 'NONE',  ( 75.90485726080815709, 62.11260916716577185, -3.867068906737686440 ) ) ;
#31966=CARTESIAN_POINT ( 'NONE',  ( 79.64653587341230434, 65.62447382577089172, -2.816708194897767026 ) ) ;
#31967=CARTESIAN_POINT ( 'NONE',  ( 75.98741087703858454, 61.93803417815122003, 3.887901781367217424 ) ) ;
#31971=ADVANCED_FACE ( 'NONE', ( #6651 ), #2174, .T. ) ;
#31972=CARTESIAN_POINT ( 'NONE',  ( 81.48599817137706225, 65.27445208842065938, 2.474249079298665777 ) ) ;
#31978=ORIENTED_EDGE ( 'NONE', *, *, #11125, .T. ) ;
#31980=CARTESIAN_POINT ( 'NONE',  ( -1.432293644835494373, -27.47664038617742577, -1.000000000000000000 ) ) ;
#31981=TOROIDAL_SURFACE ( 'NONE', #40485, 31.02204673211315011, 3.000000000000000000 ) ;
#31983=DIRECTION ( 'NONE',  ( 0.4690749385695657803, 0.8831583674551003460, 0.000000000000000000 ) ) ;
#31995=CARTESIAN_POINT ( 'NONE',  ( 68.07944445521805221, 58.24657026194513776, -3.992939643064505439 ) ) ;
#32005=ORIENTED_EDGE ( 'NONE', *, *, #11636, .F. ) ;
#32009=CARTESIAN_POINT ( 'NONE',  ( 78.65660921518627902, 66.03460256502702919, 1.194943971655634929 ) ) ;
#32012=CARTESIAN_POINT ( 'NONE',  ( 80.13677637144074595, 61.33843513727118335, -2.660685394430965189 ) ) ;
#32015=( GEOMETRIC_REPRESENTATION_CONTEXT ( 3 ) GLOBAL_UNCERTAINTY_ASSIGNED_CONTEXT ( ( #9388 ) ) GLOBAL_UNIT_ASSIGNED_CONTEXT ( ( #29902, #32408, #1319 ) ) REPRESENTATION_CONTEXT ( 'NONE', 'WORKASPACE' ) );
#32016=CARTESIAN_POINT ( 'NONE',  ( 78.68665600826857087, 66.05594492867547274, -1.065084354002965528 ) ) ;
#32017=CARTESIAN_POINT ( 'NONE',  ( 78.59948840878007559, 65.10367658859402695, 3.015657119755321691 ) ) ;
#32020=CARTESIAN_POINT ( 'NONE',  ( 82.44648106056955328, 62.87232481290445918, 1.233992409460102690 ) ) ;
#32021=CARTESIAN_POINT ( 'NONE',  ( -64.08758708074091714, 41.42074089612427912, 3.928585658033465489 ) ) ;
#32031=CARTESIAN_POINT ( 'NONE',  ( -64.08758708074093136, 35.93730870640388275, 3.800414904976363140 ) ) ;
#32034=CARTESIAN_POINT ( 'NONE',  ( -75.45330471031414277, 33.71485196875532608, -46.17089178453873188 ) ) ;
#32039=CIRCLE ( 'NONE', #22191, 0.9999999999999988898 ) ;
#32044=EDGE_LOOP ( 'NONE', ( #24463, #3433, #31337, #10689 ) ) ;
#32047=CARTESIAN_POINT ( 'NONE',  ( 66.55026548882318593, 57.88912323611526034, 3.999530551066472039 ) ) ;
#32063=CARTESIAN_POINT ( 'NONE',  ( 80.53991883815804442, 62.31343731104870898, -3.289664858626423438 ) ) ;
#32065=CARTESIAN_POINT ( 'NONE',  ( -66.99872204295122913, 28.48507918597134037, -9.800414904976365804 ) ) ;
#32066=ORIENTED_EDGE ( 'NONE', *, *, #17231, .F. ) ;
#32080=LINE ( 'NONE', #25678, #1793 ) ;
#32084=CARTESIAN_POINT ( 'NONE',  ( 79.98672868146593373, 65.19218680485846562, 3.233552917234622015 ) ) ;
#32088=B_SPLINE_CURVE_WITH_KNOTS ( 'NONE', 3,
 ( #15709, #9121, #24987, #21697, #35083, #34276, #24779, #278, #21894, #9736, #2773, #37522, #25390, #2985, #6045, #34884, #28471, #9317, #37715, #28061, #37929, #15503 ),
 .UNSPECIFIED., .F., .F.,
 ( 4, 2, 2, 2, 2, 2, 2, 2, 2, 2, 4 ),
 ( -6.342348469680895344E-05, 0.003936570167042379408, 0.007936563818781567498, 0.009936560644651162844, 0.01193655747052075992, 0.01293655588345555413, 0.01393655429639035007, 0.01493655270932514427, 0.01543655191579252316, 0.01568655151902622474, 0.01593655112225992460 ),
 .UNSPECIFIED. ) ;
#32094=CARTESIAN_POINT ( 'NONE',  ( -63.99293516169446150, 35.89893413629674512, 7.506047544094574420 ) ) ;
#32098=CARTESIAN_POINT ( 'NONE',  ( 68.75960254727382903, 58.21139355255508008, 3.964410623304020831 ) ) ;
#32105=CARTESIAN_POINT ( 'NONE',  ( 78.87101214850903830, 66.02979514927503146, -1.817988788077136375 ) ) ;
#32116=CARTESIAN_POINT ( 'NONE',  ( 81.11594168931695492, 61.32525408782629484, -1.607835478472321444 ) ) ;
#32127=CARTESIAN_POINT ( 'NONE',  ( -63.47040772160210054, 43.09577237655619797, -3.381599148487555162 ) ) ;
#32128=CARTESIAN_POINT ( 'NONE',  ( 70.60245471852235255, 60.31942058782808402, 3.837797619696055929 ) ) ;
#32130=B_SPLINE_CURVE_WITH_KNOTS ( 'NONE', 3,
 ( #10359, #16717, #29307, #32607, #38549, #9952 ),
 .UNSPECIFIED., .F., .F.,
 ( 4, 2, 4 ),
 ( 0.000000000000000000, 0.001088541862127112049, 0.002177083724254224098 ),
 .UNSPECIFIED. ) ;
#32132=ORIENTED_EDGE ( 'NONE', *, *, #23306, .T. ) ;
#32137=CARTESIAN_POINT ( 'NONE',  ( 81.64294641038151212, 62.46883698080834790, 2.647945256410963566 ) ) ;
#32149=PRODUCT_DEFINITION ( 'UNKNOWN', '', #18247, #31644 ) ;
#32157=CARTESIAN_POINT ( 'NONE',  ( 66.42099604079466246, 57.79375748135241508, -4.000000000000017764 ) ) ;
#32167=CARTESIAN_POINT ( 'NONE',  ( 81.88767907424660564, 65.09350295521461760, -2.164558651854042282 ) ) ;
#32170=CARTESIAN_POINT ( 'NONE',  ( 76.01163379375532259, 60.38783671147731980, -3.615102801931016074 ) ) ;
#32174=CARTESIAN_POINT ( 'NONE',  ( 76.68479537131447898, 60.43247505492697513, 3.462570962778594552 ) ) ;
#32180=CARTESIAN_POINT ( 'NONE',  ( 82.04158296082421487, 62.38656886254267420, 2.040045296073324632 ) ) ;
#32201=CARTESIAN_POINT ( 'NONE',  ( 68.63113683135277654, 58.55076364936792288, -3.993768376023898448 ) ) ;
#32205=CARTESIAN_POINT ( 'NONE',  ( -43.84925787048184986, -39.21126558444150589, 9.800414904976365804 ) ) ;
#32211=VERTEX_POINT ( 'NONE', #786 ) ;
#32213=CARTESIAN_POINT ( 'NONE',  ( 81.25428736789773154, 61.63226232517330061, 2.112861953993775632 ) ) ;
#32215=CARTESIAN_POINT ( 'NONE',  ( 79.97179536941432332, 60.87748285318664898, -2.061059937946318144 ) ) ;
#32218=CARTESIAN_POINT ( 'NONE',  ( 78.88661621011567604, 66.15061626711307952, -1.323744132979592925 ) ) ;
#32219=CARTESIAN_POINT ( 'NONE',  ( 78.20000946334697289, 65.71092203236408125, 1.748505333477076373 ) ) ;
#32222=CARTESIAN_POINT ( 'NONE',  ( 81.60972716517463255, 65.70321483603510160, 1.303631908148715990 ) ) ;
#32223=CARTESIAN_POINT ( 'NONE',  ( -64.08758708074093136, 44.09647857119033176, 1.198844121191492196 ) ) ;
#32227=CARTESIAN_POINT ( 'NONE',  ( -63.48867051204953782, 35.67471974816380964, -6.899503081314764863 ) ) ;
#32233=CARTESIAN_POINT ( 'NONE',  ( -66.99872204295122913, 28.48507918597134037, 6.999999999999999112 ) ) ;
#32234=CIRCLE ( 'NONE', #11814, 2.500000000000002220 ) ;
#32245=EDGE_CURVE ( 'NONE', #24852, #38011, #28822, .T. ) ;
#32247=DIRECTION ( 'NONE',  ( 0.000000000000000000, -1.000000000000000000, 0.000000000000000000 ) ) ;
#32263=ORIENTED_EDGE ( 'NONE', *, *, #40430, .F. ) ;
#32264=CARTESIAN_POINT ( 'NONE',  ( 78.83205648568244328, 65.58035453618786903, -2.615973384261010448 ) ) ;
#32265=CARTESIAN_POINT ( 'NONE',  ( 80.85043593073658030, 61.68942038033306829, 2.615973384260630308 ) ) ;
#32278=DIRECTION ( 'NONE',  ( 0.000000000000000000, 0.000000000000000000, -1.000000000000000000 ) ) ;
#32282=CARTESIAN_POINT ( 'NONE',  ( 81.37039951255474080, 61.83949519909547377, 2.349509806045097182 ) ) ;
#32290=FACE_OUTER_BOUND ( 'NONE', #18292, .T. ) ;
#32294=CARTESIAN_POINT ( 'NONE',  ( 68.42229528291726126, 59.10113456467039583, 3.941639393089738874 ) ) ;
#32298=CARTESIAN_POINT ( 'NONE',  ( 81.19854122754009040, 61.34870327520655309, -1.508787936435542099 ) ) ;
#32305=DIRECTION ( 'NONE',  ( 0.000000000000000000, 0.000000000000000000, -1.000000000000000000 ) ) ;
#32308=VERTEX_POINT ( 'NONE', #17002 ) ;
#32309=CARTESIAN_POINT ( 'NONE',  ( 80.83002518733226793, 62.39751428130106348, -3.213872034465284244 ) ) ;
#32320=CARTESIAN_POINT ( 'NONE',  ( 71.82805326594559858, 60.58951223549524201, 3.882941974849172695 ) ) ;
#32322=ORIENTED_EDGE ( 'NONE', *, *, #39527, .F. ) ;
#32332=CARTESIAN_POINT ( 'NONE',  ( 80.63952753653605043, 65.18836132072121359, 3.079343812564430127 ) ) ;
#32345=CARTESIAN_POINT ( 'NONE',  ( 9.703489126596464232, 56.50623631086179444, -1.000000000000000000 ) ) ;
#32346=AXIS2_PLACEMENT_3D ( 'NONE', #10893, #23471, #8007 ) ;
#32352=DIRECTION ( 'NONE',  ( 1.000000000000000000, 0.000000000000000000, 0.000000000000000000 ) ) ;
#32355=CARTESIAN_POINT ( 'NONE',  ( -64.08758708074093136, 38.13199975834722721, -3.043809435734133650 ) ) ;
#32356=( NAMED_UNIT ( * ) SI_UNIT ( $, .STERADIAN. ) SOLID_ANGLE_UNIT ( ) );
#32357=( BOUNDED_CURVE ( )  B_SPLINE_CURVE ( 3, ( #32535, #13786, #22317, #10879 ),
 .UNSPECIFIED., .F., .T. ) 
 B_SPLINE_CURVE_WITH_KNOTS ( ( 4, 4 ),
 ( 1.570796326794894560, 1.718934167276706892 ),
 .UNSPECIFIED. ) 
 CURVE ( )  GEOMETRIC_REPRESENTATION_ITEM ( )  RATIONAL_B_SPLINE_CURVE ( ( 1.000000000000000000, 0.9981721009331441241, 0.9981721009331441241, 1.000000000000000000 ) ) 
 REPRESENTATION_ITEM ( '' )  );
#32360=ORIENTED_EDGE ( 'NONE', *, *, #30227, .F. ) ;
#32361=CARTESIAN_POINT ( 'NONE',  ( 82.21758965863715218, 62.47540435105895540, -1.725837398063455819 ) ) ;
#32364=CARTESIAN_POINT ( 'NONE',  ( 74.85245598970902847, 62.88263772385705153, -3.424891502433893287 ) ) ;
#32366=DIRECTION ( 'NONE',  ( 0.000000000000000000, 0.000000000000000000, -1.000000000000000000 ) ) ;
#32368=CARTESIAN_POINT ( 'NONE',  ( 77.90315483005272768, 60.81789388943186481, 3.308002540436142169 ) ) ;
#32374=CARTESIAN_POINT ( 'NONE',  ( 79.82775505260907778, 66.24998868310150613, 1.780213741554581786 ) ) ;
#32385=DIRECTION ( 'NONE',  ( 0.3757233601570965087, 0.9267318687906770380, 0.000000000000000000 ) ) ;
#32391=CARTESIAN_POINT ( 'NONE',  ( -63.54340798299629256, 43.49363706015520137, -3.059022540971626736 ) ) ;
#32398=CARTESIAN_POINT ( 'NONE',  ( 67.35228065126028696, 58.41716755899589941, -3.985038673850037849 ) ) ;
#32408=( NAMED_UNIT ( * ) PLANE_ANGLE_UNIT ( ) SI_UNIT ( $, .RADIAN. ) );
#32409=CARTESIAN_POINT ( 'NONE',  ( 81.14373266700285114, 62.24431303712577090, 2.911438267503737354 ) ) ;
#32412=CARTESIAN_POINT ( 'NONE',  ( 78.56694041390316841, 64.50177951359142980, -3.424416364708429583 ) ) ;
#32415=CARTESIAN_POINT ( 'NONE',  ( 80.90131254180703024, 64.57540998626842565, -3.341858160548295764 ) ) ;
#32416=CARTESIAN_POINT ( 'NONE',  ( 79.84787171156668251, 62.37423782317881660, 3.536670452273173559 ) ) ;
#32417=CARTESIAN_POINT ( 'NONE',  ( 82.23130663822968245, 64.88126268290433529, 1.480606629405690544 ) ) ;
#32418=CARTESIAN_POINT ( 'NONE',  ( -64.08758708074093136, 43.59044912937621774, 1.299988725260725841 ) ) ;
#32420=CARTESIAN_POINT ( 'NONE',  ( -64.17177837788925387, 36.63861034030102815, -5.251833000746768398 ) ) ;
#32421=VERTEX_POINT ( 'NONE', #22542 ) ;
#32440=CARTESIAN_POINT ( 'NONE',  ( 66.82989622468531365, 58.03237508814455481, 3.998112125426342978 ) ) ;
#32441=CARTESIAN_POINT ( 'NONE',  ( -63.06903391669437298, 38.60168910470056147, 3.999999999999999112 ) ) ;
#32445=ORIENTED_EDGE ( 'NONE', *, *, #17912, .T. ) ;
#32453=CARTESIAN_POINT ( 'NONE',  ( 78.90889979212947480, 65.37513451817237353, -2.884918531047277135 ) ) ;
#32455=CARTESIAN_POINT ( 'NONE',  ( 80.62613562354553665, 62.33752749645049818, 3.268578535636590399 ) ) ;
#32458=EDGE_CURVE ( 'NONE', #23165, #30342, #21953, .T. ) ;
#32465=CARTESIAN_POINT ( 'NONE',  ( 76.98021629873809957, 64.85258827439523088, -2.378915702215372185 ) ) ;
#32468=DIRECTION ( 'NONE',  ( 0.4582725098355734938, -0.8888117386314180468, -0.000000000000000000 ) ) ;
#32474=CARTESIAN_POINT ( 'NONE',  ( 79.08570711028919220, 65.99300539798554155, 2.058202901128779239 ) ) ;
#32480=DIRECTION ( 'NONE',  ( -1.000000000000000000, 0.000000000000000000, 0.000000000000000000 ) ) ;
#32487=CARTESIAN_POINT ( 'NONE',  ( -64.08758708074093136, 42.21690229009149675, -2.785273621577612158 ) ) ;
#32489=CARTESIAN_POINT ( 'NONE',  ( 80.06561887301042191, 64.50783488872740179, -3.572022490087452873 ) ) ;
#32493=CARTESIAN_POINT ( 'NONE',  ( -58.66072975137505807, 29.93711237438063222, 5.396324374907178978 ) ) ;
#32496=ORIENTED_EDGE ( 'NONE', *, *, #1371, .T. ) ;
#32497=CARTESIAN_POINT ( 'NONE',  ( -75.45330471031414277, 33.71485196875532608, -46.17089178453873188 ) ) ;
#32500=VERTEX_POINT ( 'NONE', #35306 ) ;
#32502=CARTESIAN_POINT ( 'NONE',  ( 80.44862750795371653, 63.21300062201452619, -3.624000857162081424 ) ) ;
#32504=LINE ( 'NONE', #13759, #24667 ) ;
#32506=CARTESIAN_POINT ( 'NONE',  ( 81.09516781258611218, 61.58556622376321599, 2.215902410107942977 ) ) ;
#32510=AXIS2_PLACEMENT_3D ( 'NONE', #4821, #29929, #1746 ) ;
#32515=CARTESIAN_POINT ( 'NONE',  ( -64.08758708074093136, 42.98405160848505346, -2.320550955811203853 ) ) ;
#32516=CARTESIAN_POINT ( 'NONE',  ( 71.99851445618389789, 60.18445664521269123, 3.955776929956314358 ) ) ;
#32525=CARTESIAN_POINT ( 'NONE',  ( 81.75671479976297462, 62.52433184976159453, 2.563845612517931194 ) ) ;
#32535=CARTESIAN_POINT ( 'NONE',  ( -63.08758708074093136, 38.76906266698303227, 4.000000000000000000 ) ) ;
#32547=CARTESIAN_POINT ( 'NONE',  ( 66.27376694609004915, 57.73522568913436004, -4.000000000000000000 ) ) ;
#32555=CARTESIAN_POINT ( 'NONE',  ( -56.50908310466265050, 29.95896301100017567, -1.719924897558571697 ) ) ;
#32560=CARTESIAN_POINT ( 'NONE',  ( 82.43454424851934448, 64.20405324974024097, -1.755995906648851079 ) ) ;
#32566=CARTESIAN_POINT ( 'NONE',  ( 76.30453859000765249, 59.72919098693703432, -3.074209570828594362 ) ) ;
#32569=DIRECTION ( 'NONE',  ( -0.000000000000000000, -1.000000000000000000, -0.000000000000000000 ) ) ;
#32571=CARTESIAN_POINT ( 'NONE',  ( 75.82377327987001081, 62.28299708301691595, 3.825872951952284051 ) ) ;
#32573=CARTESIAN_POINT ( 'NONE',  ( -64.08758708074093136, 37.27332153486386090, 4.546479763849019307 ) ) ;
#32578=CARTESIAN_POINT ( 'NONE',  ( 81.80771926544794326, 61.88353390887446182, 1.601045042264324092 ) ) ;
#32585=CARTESIAN_POINT ( 'NONE',  ( 75.39030949273650606, 59.47930393830225171, 3.241331962143158663 ) ) ;
#32599=CARTESIAN_POINT ( 'NONE',  ( 67.21358634547439692, 57.88870193986200974, -3.993497817183393472 ) ) ;
#32600=CARTESIAN_POINT ( 'NONE',  ( -59.01947560891952804, 27.90920910948504385, 6.147301388271928957 ) ) ;
#32607=CARTESIAN_POINT ( 'NONE',  ( -56.10469124525552331, 30.75883671979821443, 2.489329600088167727 ) ) ;
#32608=EDGE_CURVE ( 'NONE', #4319, #31687, #10343, .T. ) ;
#32613=CARTESIAN_POINT ( 'NONE',  ( 79.61290006553409171, 65.30841326124827617, 3.134554000843265520 ) ) ;
#32617=CARTESIAN_POINT ( 'NONE',  ( 79.08256350411643609, 63.89089281391859032, -3.718817779187653549 ) ) ;
#32620=CARTESIAN_POINT ( 'NONE',  ( 81.38764266124616142, 63.30759111148670826, -3.202775791559302476 ) ) ;
#32621=CARTESIAN_POINT ( 'NONE',  ( 80.72640005664072760, 61.14345848406946260, 1.640065189519674282 ) ) ;
#32622=ORIENTED_EDGE ( 'NONE', *, *, #20871, .F. ) ;
#32626=CARTESIAN_POINT ( 'NONE',  ( 81.34501148009313454, 65.92776879248955879, 1.287552078897677976 ) ) ;
#32633=AXIS2_PLACEMENT_3D ( 'NONE', #6449, #15903, #28051 ) ;
#32645=EDGE_LOOP ( 'NONE', ( #8883, #17274, #31895, #965 ) ) ;
#32646=CARTESIAN_POINT ( 'NONE',  ( 66.67928806435183731, 57.99078996168128697, 3.997717836774547617 ) ) ;
#32647=CARTESIAN_POINT ( 'NONE',  ( 73.54169881536046205, 59.75047131450637750, -3.824679913398719044 ) ) ;
#32650=CIRCLE ( 'NONE', #18823, 5.000000000000000000 ) ;
#32653=AXIS2_PLACEMENT_3D ( 'NONE', #24716, #22405, #37264 ) ;
#32655=DIRECTION ( 'NONE',  ( 0.000000000000000000, 0.000000000000000000, 1.000000000000000000 ) ) ;
#32661=CARTESIAN_POINT ( 'NONE',  ( 78.56188500726528900, 65.90376500477491106, -1.760837461004926663 ) ) ;
#32663=CARTESIAN_POINT ( 'NONE',  ( 80.48490785079584953, 62.58389448792968324, 3.438247877890441728 ) ) ;
#32675=CARTESIAN_POINT ( 'NONE',  ( 81.13213036240664167, 62.83067685251092627, 3.261148789966860306 ) ) ;
#32676=CARTESIAN_POINT ( 'NONE',  ( -74.92283640148291113, 18.87330372387140187, -46.17089178453873188 ) ) ;
#32688=CARTESIAN_POINT ( 'NONE',  ( 69.09457860630368486, 59.08023000801873081, 3.976370928559271878 ) ) ;
#32691=CARTESIAN_POINT ( 'NONE',  ( -64.08758708074093136, 41.34489873040477903, -2.999999999999999556 ) ) ;
#32693=CARTESIAN_POINT ( 'NONE',  ( 80.57402935197538341, 63.63785766202913408, -3.625945587094183686 ) ) ;
#32696=CARTESIAN_POINT ( 'NONE',  ( -57.31959649706901416, 29.49889766843901029, 4.251262061546403181 ) ) ;
#32706=CARTESIAN_POINT ( 'NONE',  ( 80.76107640992933057, 62.37607017537882115, -3.233326467035619878 ) ) ;
#32708=VECTOR ( 'NONE', #37787, 1000.000000000000114 ) ;
#32710=CARTESIAN_POINT ( 'NONE',  ( 81.11523045952516497, 61.59071516775627231, 2.202709653501095488 ) ) ;
#32716=FACE_OUTER_BOUND ( 'NONE', #3705, .T. ) ;
#32720=EDGE_LOOP ( 'NONE', ( #21403, #10411, #36641 ) ) ;
#32727=CARTESIAN_POINT ( 'NONE',  ( 81.53035370524470693, 63.02147265738407356, 3.059106349699970639 ) ) ;
#32739=EDGE_CURVE ( 'NONE', #5157, #29043, #11755, .T. ) ;
#32744=B_SPLINE_CURVE_WITH_KNOTS ( 'NONE', 3,
 ( #263, #12804, #34869, #6645, #13014, #19196, #28668, #24760, #38121, #9923, #37308, #9104, #34258, #6030, #31151, #15485, #40595, #12402 ),
 .UNSPECIFIED., .F., .F.,
 ( 4, 2, 2, 2, 2, 2, 2, 2, 4 ),
 ( 0.000000000000000000, 0.0003909910682061002027, 0.0007819821364122004053, 0.001563964272824406882, 0.002345946409236613576, 0.003127928545648820269, 0.004691892818473243632, 0.005473874954885450325, 0.006255857091297657019 ),
 .UNSPECIFIED. ) ;
#32749=ORIENTED_EDGE ( 'NONE', *, *, #36748, .T. ) ;
#32752=CARTESIAN_POINT ( 'NONE',  ( 66.27376694609004915, 57.73522568913436004, -4.000000000000000000 ) ) ;
#32764=CARTESIAN_POINT ( 'NONE',  ( 81.91393161461809314, 61.93681595580208210, -1.358135763685572206 ) ) ;
#32768=LINE ( 'NONE', #9915, #31839 ) ;
#32771=CARTESIAN_POINT ( 'NONE',  ( 74.91689101425367880, 62.74844471888588515, 3.527522301306301067 ) ) ;
#32779=CARTESIAN_POINT ( 'NONE',  ( 81.85640814870976101, 64.68575429476388194, 2.512558077907662391 ) ) ;
#32798=CARTESIAN_POINT ( 'NONE',  ( 67.69980720754315939, 58.37350455430767937, -3.995247128881052046 ) ) ;
#32812=CARTESIAN_POINT ( 'NONE',  ( 79.22373596144829833, 65.64748706429476499, 2.718470589328619624 ) ) ;
#32816=CARTESIAN_POINT ( 'NONE',  ( 78.34436985318809832, 64.89959302631085336, -3.091829831932941808 ) ) ;
#32818=CARTESIAN_POINT ( 'NONE',  ( 81.43955525003346452, 63.33353925140134066, -3.171364025122245689 ) ) ;
#32819=CARTESIAN_POINT ( 'NONE',  ( 79.60787101065389493, 62.86536646861405586, 3.718817779187657990 ) ) ;
#32822=CARTESIAN_POINT ( 'NONE',  ( 82.45631153319118312, 62.87735296625318426, 1.118100487915077546 ) ) ;
#32825=CARTESIAN_POINT ( 'NONE',  ( -64.59661209699989115, 34.69995260619734267, -6.002488439271949083 ) ) ;
#32835=DIRECTION ( 'NONE',  ( -0.4690749385695657803, -0.8831583674551003460, 0.000000000000000000 ) ) ;
#32846=CARTESIAN_POINT ( 'NONE',  ( 66.41505992881667453, 57.81052748253015494, 4.000000000000021316 ) ) ;
#32847=CARTESIAN_POINT ( 'NONE',  ( 72.12755885004493450, 59.87634726091143023, -3.962431611477345239 ) ) ;
#32854=DIRECTION ( 'NONE',  ( 1.000000000000000000, 0.000000000000000000, 0.000000000000000000 ) ) ;
#32858=ORIENTED_EDGE ( 'NONE', *, *, #10159, .F. ) ;
#32859=CARTESIAN_POINT ( 'NONE',  ( 78.49831277043062983, 65.85142261852138290, -1.827177995460260718 ) ) ;
#32861=CARTESIAN_POINT ( 'NONE',  ( 79.82585920882016239, 63.98597419336261538, 3.710743084827283322 ) ) ;
#32874=CARTESIAN_POINT ( 'NONE',  ( 79.55653453243731121, 65.56957575487831491, 2.861733672647126525 ) ) ;
#32875=LINE ( 'NONE', #32676, #7132 ) ;
#32881=EDGE_CURVE ( 'NONE', #28588, #15750, #3542, .T. ) ;
#32888=CARTESIAN_POINT ( 'NONE',  ( 68.12732179974642577, 58.11841597887141120, 3.982418445723222789 ) ) ;
#32892=VECTOR ( 'NONE', #28660, 1000.000000000000000 ) ;
#32893=CARTESIAN_POINT ( 'NONE',  ( 78.96442931663766274, 65.90663607296401949, -2.147349935851027958 ) ) ;
#32894=CARTESIAN_POINT ( 'NONE',  ( -80.19065981525226050, 31.27226540113725406, 9.800414904976365804 ) ) ;
#32902=CARTESIAN_POINT ( 'NONE',  ( 81.09158065085919986, 61.31869227828924807, -1.634613895560571573 ) ) ;
#32904=CARTESIAN_POINT ( 'NONE',  ( 80.08517677095778708, 64.13476336867732641, 3.668443954219271053 ) ) ;
#32911=CARTESIAN_POINT ( 'NONE',  ( -75.45330471031414277, 33.71485196875532608, 12.49999999999999645 ) ) ;
#32912=PLANE ( 'NONE',  #29138 ) ;
#32914=EDGE_LOOP ( 'NONE', ( #25646, #12722, #17771, #30726 ) ) ;
#32917=CIRCLE ( 'NONE', #38163, 2.500000000000002220 ) ;
#32921=CARTESIAN_POINT ( 'NONE',  ( 79.02544788879011151, 66.13175326451143121, 1.679744683813971129 ) ) ;
#32932=LINE ( 'NONE', #23455, #19416 ) ;
#32951=( LENGTH_UNIT ( ) NAMED_UNIT ( * ) SI_UNIT ( .MILLI., .METRE. ) );
#32957=CARTESIAN_POINT ( 'NONE',  ( 81.45638069295013395, 61.46019730367517298, -1.134074597586742783 ) ) ;
#32963=CARTESIAN_POINT ( 'NONE',  ( 76.01163379375532259, 60.38783671147731980, 3.615102801931016074 ) ) ;
#32966=CARTESIAN_POINT ( 'NONE',  ( -64.08758708074093136, 38.00013147421745430, 4.165003120435059714 ) ) ;
#32973=CARTESIAN_POINT ( 'NONE',  ( 78.68849923766543952, 66.05725436416432217, 1.045986116561638202 ) ) ;
#32986=CARTESIAN_POINT ( 'NONE',  ( -57.16504416091206053, 33.41445838748276742, -4.000000000000000000 ) ) ;
#32987=CARTESIAN_POINT ( 'NONE',  ( -63.45304970008103140, 43.00143306355779771, -3.444018727593662899 ) ) ;
#32989=ORIENTED_EDGE ( 'NONE', *, *, #1837, .F. ) ;
#32992=CARTESIAN_POINT ( 'NONE',  ( 67.13660786288076565, 58.10023080654656980, -3.998533043703386802 ) ) ;
#33005=CARTESIAN_POINT ( 'NONE',  ( 80.99721608130789718, 62.45573281339171956, 3.163072811751561186 ) ) ;
#33007=CARTESIAN_POINT ( 'NONE',  ( -63.61790918070564516, 43.90188359253805572, 2.582768616493209990 ) ) ;
#33009=CARTESIAN_POINT ( 'NONE',  ( 77.57568143946795658, 64.97578145858240362, -2.643019404356976576 ) ) ;
#33014=CARTESIAN_POINT ( 'NONE',  ( 81.59170830166485189, 62.44397035145045294, -2.684801069570277310 ) ) ;
#33015=CARTESIAN_POINT ( 'NONE',  ( 78.78025785238997969, 63.39248666165328672, 3.791687334209851379 ) ) ;
#33019=CARTESIAN_POINT ( 'NONE',  ( 82.17153865661313716, 64.85009419791106211, 1.775718711109096404 ) ) ;
#33031=CARTESIAN_POINT ( 'NONE',  ( -72.95330471031414277, 33.71485196875532608, -12.49999999999999645 ) ) ;
#33039=CARTESIAN_POINT ( 'NONE',  ( 66.27376694608996388, 57.73522568913447373, 4.000000000000000000 ) ) ;
#33040=CARTESIAN_POINT ( 'NONE',  ( 71.62240613637702324, 61.07494268190701092, -3.699617110277040766 ) ) ;
#33045=DIRECTION ( 'NONE',  ( -0.8888117386314180468, -0.4582725098355734938, 0.000000000000000000 ) ) ;
#33051=DIRECTION ( 'NONE',  ( -1.000000000000000000, 9.435707606059839439E-16, 0.000000000000000000 ) ) ;
#33056=CARTESIAN_POINT ( 'NONE',  ( 80.10726245975679660, 62.76215410473258771, -3.584461231902855705 ) ) ;
#33058=CARTESIAN_POINT ( 'NONE',  ( 79.50676573472792086, 64.15826028415024496, 3.676305632669318424 ) ) ;
#33074=CARTESIAN_POINT ( 'NONE',  ( 81.14908696703564317, 61.29647948322620010, 1.137963815189210193 ) ) ;
#33082=CARTESIAN_POINT ( 'NONE',  ( 67.95937142815736820, 58.56762263466062279, 3.988335407916665520 ) ) ;
#33088=CARTESIAN_POINT ( 'NONE',  ( 81.04779914310620370, 62.47515088512101755, -3.146509185145923038 ) ) ;
#33093=CARTESIAN_POINT ( 'NONE',  ( -58.97431419818040155, 27.59684639285647378, 7.041158924856742551 ) ) ;
#33094=ORIENTED_EDGE ( 'NONE', *, *, #10508, .T. ) ;
#33100=CARTESIAN_POINT ( 'NONE',  ( 79.37669412903225918, 65.14038507876428241, -3.220356845322064565 ) ) ;
#33102=CARTESIAN_POINT ( 'NONE',  ( 79.64490966524790849, 64.60885719387560755, 3.518158556798112180 ) ) ;
#33117=VERTEX_POINT ( 'NONE', #33160 ) ;
#33124=CARTESIAN_POINT ( 'NONE',  ( 80.41462361966681271, 65.06645272473066655, 3.228380831072425572 ) ) ;
#33154=CARTESIAN_POINT ( 'NONE',  ( -57.41832745699786500, 33.02173582530747353, -4.020356607641593527 ) ) ;
#33155=VERTEX_POINT ( 'NONE', #21415 ) ;
#33159=CARTESIAN_POINT ( 'NONE',  ( 79.23414132050092462, 66.25012704882064440, -1.421876342974255802 ) ) ;
#33160=CARTESIAN_POINT ( 'NONE',  ( -62.81463675898083210, 36.67811266762162603, -4.600311178732273021 ) ) ;
#33166=CARTESIAN_POINT ( 'NONE',  ( 73.64914076101801754, 62.55656703988326939, 3.294766324886514663 ) ) ;
#33170=CARTESIAN_POINT ( 'NONE',  ( -64.08758708074093136, 37.42960919638050399, 3.182465448035748157 ) ) ;
#33175=CARTESIAN_POINT ( 'NONE',  ( 80.19490802141261554, 65.93291197049445884, 2.397965335136733600 ) ) ;
#33189=EDGE_CURVE ( 'NONE', #11880, #29308, #2703, .T. ) ;
#33194=CARTESIAN_POINT ( 'NONE',  ( 67.51854282697247811, 57.96351248157043301, -3.990882853436549027 ) ) ;
#33206=DIRECTION ( 'NONE',  ( 0.000000000000000000, 0.000000000000000000, 1.000000000000000000 ) ) ;
#33209=CARTESIAN_POINT ( 'NONE',  ( 78.69038500580381879, 66.05859403932473128, -1.002944004955704349 ) ) ;
#33211=CARTESIAN_POINT ( 'NONE',  ( 79.92454992231405697, 64.78853304740056274, 3.443978770203976136 ) ) ;
#33215=CARTESIAN_POINT ( 'NONE',  ( 77.67868059383670243, 64.13990294438298179, -3.401348408886263552 ) ) ;
#33218=CARTESIAN_POINT ( 'NONE',  ( 81.55137728095425587, 62.42468454963441360, -2.710336141770833596 ) ) ;
#33219=CARTESIAN_POINT ( 'NONE',  ( 77.74023705119593330, 64.68384637002905890, 3.042889847487493249 ) ) ;
#33221=CARTESIAN_POINT ( 'NONE',  ( 82.13789946638789274, 62.20769933019770548, 1.398807481800125485 ) ) ;
#33230=EDGE_CURVE ( 'NONE', #15453, #1114, #15222, .T. ) ;
#33239=CARTESIAN_POINT ( 'NONE',  ( -65.15514661499977933, 34.97220226750606997, -6.888442104241536690 ) ) ;
#33246=ADVANCED_FACE ( 'NONE', ( #24701 ), #17893, .T. ) ;
#33248=CARTESIAN_POINT ( 'NONE',  ( 66.59136238364995108, 57.77385624644436746, 3.999229419681933351 ) ) ;
#33250=CARTESIAN_POINT ( 'NONE',  ( 72.33948634203015615, 59.36795819651598549, -3.882941974771884297 ) ) ;
#33265=CARTESIAN_POINT ( 'NONE',  ( 78.63268743221328805, 65.61080103085718918, -2.414331286641655527 ) ) ;
#33267=CARTESIAN_POINT ( 'NONE',  ( 80.89410497084998042, 61.37834026963080447, 2.095806625473841223 ) ) ;
#33277=CARTESIAN_POINT ( 'NONE',  ( -75.45330471031414277, 33.71485196875532608, -9.800414904976365804 ) ) ;
#33278=EDGE_CURVE ( 'NONE', #11497, #23165, #4855, .T. ) ;
#33283=CARTESIAN_POINT ( 'NONE',  ( 81.16399599188275715, 62.84525499041613017, 3.248659383495554831 ) ) ;
#33288=EDGE_CURVE ( 'NONE', #16748, #38621, #10761, .T. ) ;
#33295=CARTESIAN_POINT ( 'NONE',  ( 67.35228065126028696, 58.41716755899589941, 3.985038673850037849 ) ) ;
#33297=AXIS2_PLACEMENT_3D ( 'NONE', #19097, #5572, #27596 ) ;
#33302=CARTESIAN_POINT ( 'NONE',  ( 78.74533340381492508, 66.05753824468469304, -1.508787936435524113 ) ) ;
#33311=ORIENTED_EDGE ( 'NONE', *, *, #32245, .T. ) ;
#33312=CARTESIAN_POINT ( 'NONE',  ( 78.57229106431512378, 65.97474043420317003, -1.364493914842173306 ) ) ;
#33314=CARTESIAN_POINT ( 'NONE',  ( 80.44862750795415707, 63.21300062201468251, 3.624000857162004152 ) ) ;
#33318=CARTESIAN_POINT ( 'NONE',  ( 75.02040913282911561, 59.50525224047964201, -3.395557233589185486 ) ) ;
#33320=CARTESIAN_POINT ( 'NONE',  ( -56.90710715293131017, 30.56612162020725165, -3.329579881309527423 ) ) ;
#33338=CARTESIAN_POINT ( 'NONE',  ( 81.60109106391716693, 62.17032169345860382, 2.476693319890299616 ) ) ;
#33345=EDGE_CURVE ( 'NONE', #31581, #22494, #10058, .T. ) ;
#33365=AXIS2_PLACEMENT_3D ( 'NONE', #391, #12929, #9633 ) ;
#33372=CARTESIAN_POINT ( 'NONE',  ( 81.17225696364401699, 61.44517649410261129, -1.881209715725437270 ) ) ;
#33380=CARTESIAN_POINT ( 'NONE',  ( 82.15586074033932107, 62.44414535927726462, -1.848245342697680593 ) ) ;
#33387=CARTESIAN_POINT ( 'NONE',  ( 74.17630236427460488, 61.40657735673663353, 3.883841728571264973 ) ) ;
#33393=CARTESIAN_POINT ( 'NONE',  ( 81.52783586777056257, 64.51439989829020760, 2.952528780688829624 ) ) ;
#33413=CARTESIAN_POINT ( 'NONE',  ( -64.08758708074093136, 38.13199975834722721, -3.043809435734133650 ) ) ;
#33414=CARTESIAN_POINT ( 'NONE',  ( 66.72933079118084265, 57.85140187965895819, -3.999416444359401357 ) ) ;
#33428=CARTESIAN_POINT ( 'NONE',  ( 82.41652906543019697, 64.58603266165640377, -1.328060019258380242 ) ) ;
#33429=CARTESIAN_POINT ( 'NONE',  ( 79.07783777134646641, 65.79916784333097723, 2.450942308261427893 ) ) ;
#33431=ORIENTED_EDGE ( 'NONE', *, *, #17403, .T. ) ;
#33432=CARTESIAN_POINT ( 'NONE',  ( 79.63092111360349179, 60.86998874196336828, -2.418543376929292332 ) ) ;
#33435=CARTESIAN_POINT ( 'NONE',  ( 80.61314501155287360, 64.81116531652870094, -3.343039074468324046 ) ) ;
#33436=CARTESIAN_POINT ( 'NONE',  ( 79.26553226962346343, 61.67928659302138783, 3.361664161258347772 ) ) ;
#33437=ORIENTED_EDGE ( 'NONE', *, *, #6663, .T. ) ;
#33440=CARTESIAN_POINT ( 'NONE',  ( 79.63539728012720786, 66.30663591242944221, 1.358135763685230923 ) ) ;
#33444=VECTOR ( 'NONE', #10967, 1000.000000000000000 ) ;
#33449=DIRECTION ( 'NONE',  ( -1.000000000000000000, 0.000000000000000000, 0.000000000000000000 ) ) ;
#33462=CIRCLE ( 'NONE', #29499, 2.500000000000002220 ) ;
#33467=CARTESIAN_POINT ( 'NONE',  ( 66.27376694608996388, 57.73522568913447373, 4.000000000000000000 ) ) ;
#33468=CARTESIAN_POINT ( 'NONE',  ( 72.96153509227066536, 61.08495594734687018, -3.864208391313482149 ) ) ;
#33476=ORIENTED_EDGE ( 'NONE', *, *, #31706, .T. ) ;
#33478=ORIENTED_EDGE ( 'NONE', *, *, #29022, .F. ) ;
#33479=CARTESIAN_POINT ( 'NONE',  ( 80.34542504610527658, 62.25824679691979924, -3.331801170923413213 ) ) ;
#33481=CARTESIAN_POINT ( 'NONE',  ( 81.83449460947085186, 63.17368474096252129, -2.819252638153957768 ) ) ;
#33483=CARTESIAN_POINT ( 'NONE',  ( 80.37564778476929916, 62.54931541869399325, 3.458772244351172809 ) ) ;
#33487=EDGE_LOOP ( 'NONE', ( #7695, #18136, #1545, #34851 ) ) ;
#33505=ADVANCED_FACE ( 'NONE', ( #26130 ), #38660, .T. ) ;
#33507=CARTESIAN_POINT ( 'NONE',  ( 68.16305384742138074, 58.02271910793402299, 3.969942683317755350 ) ) ;
#33523=CARTESIAN_POINT ( 'NONE',  ( 80.69037048981478222, 62.35571368504050582, -3.252077313700841188 ) ) ;
#33525=CARTESIAN_POINT ( 'NONE',  ( 78.81125837042770854, 65.77339625846090598, 2.277920705665355872 ) ) ;
#33529=CARTESIAN_POINT ( 'NONE',  ( 74.68367562674023930, 60.27297886100710400, -3.815996826674382447 ) ) ;
#33541=DIRECTION ( 'NONE',  ( -1.000000000000000000, 0.000000000000000000, 0.000000000000000000 ) ) ;
#33543=CARTESIAN_POINT ( 'NONE',  ( 80.90131254178920983, 64.57540998625900386, 3.341858160559718183 ) ) ;
#33551=CARTESIAN_POINT ( 'NONE',  ( -67.16566696070617581, 37.18524951245925081, -8.491446490664150915 ) ) ;
#33560=CARTESIAN_POINT ( 'NONE',  ( 81.23287006775859709, 61.35999619221078660, -1.467306180864046183 ) ) ;
#33565=DIRECTION ( 'NONE',  ( -0.000000000000000000, -0.000000000000000000, -1.000000000000000000 ) ) ;
#33569=CARTESIAN_POINT ( 'NONE',  ( 78.82816376705464734, 65.99584493362826265, -1.862141363775770220 ) ) ;
#33570=CARTESIAN_POINT ( 'NONE',  ( -58.91620474891573167, 27.52990360452328389, -4.138963871842760156 ) ) ;
#33577=CARTESIAN_POINT ( 'NONE',  ( 81.69611827519042890, 64.99316753419185488, -2.512558077908312537 ) ) ;
#33584=CARTESIAN_POINT ( 'NONE',  ( 74.27115401224453706, 62.67359094190466351, 3.404024988867591084 ) ) ;
#33593=CARTESIAN_POINT ( 'NONE',  ( 81.83803008603292994, 64.28563725689731712, 2.776691787112188337 ) ) ;
#33612=CARTESIAN_POINT ( 'NONE',  ( 67.04731915158012612, 57.88926793091046363, -3.996990690923978296 ) ) ;
#33614=VERTEX_POINT ( 'NONE', #30214 ) ;
#33617=CARTESIAN_POINT ( 'NONE',  ( 67.64868974113205979, 58.60604628695281804, 3.975234571633589731 ) ) ;
#33625=CARTESIAN_POINT ( 'NONE',  ( 81.87444285025600266, 65.47866087958055914, -1.319711737400975915 ) ) ;
#33626=CARTESIAN_POINT ( 'NONE',  ( 79.58225024864498209, 65.28851876552752742, 3.146509185145913712 ) ) ;
#33628=VERTEX_POINT ( 'NONE', #2030 ) ;
#33629=CARTESIAN_POINT ( 'NONE',  ( 79.04999676712192525, 61.38304106620122980, -3.266768353517003565 ) ) ;
#33632=CARTESIAN_POINT ( 'NONE',  ( 81.15569957775159082, 61.29889919928260156, -1.113695828830626455 ) ) ;
#33633=CARTESIAN_POINT ( 'NONE',  ( 78.61725963159938146, 63.00713372587872385, 3.804514705604319591 ) ) ;
#33639=CARTESIAN_POINT ( 'NONE',  ( 81.30214557805317099, 65.90511036421355584, 1.555014038482367633 ) ) ;
#33654=CARTESIAN_POINT ( 'NONE',  ( -11.81496944966682960, -21.25669541281728669, 4.000000000000000000 ) ) ;
#33662=CARTESIAN_POINT ( 'NONE',  ( 66.58549141467136678, 57.79032289594774596, 3.999530551061463157 ) ) ;
#33663=CARTESIAN_POINT ( 'NONE',  ( 68.99357861020946814, 59.34113723602050783, -3.933428174212677320 ) ) ;
#33677=CARTESIAN_POINT ( 'NONE',  ( 79.18319737856853635, 64.63648950223996792, -3.475409704257727217 ) ) ;
#33680=CARTESIAN_POINT ( 'NONE',  ( 80.40506551886717546, 65.76252680069852374, -2.626729253126910191 ) ) ;
#33681=CARTESIAN_POINT ( 'NONE',  ( 80.48897389181450990, 62.29924170813984574, 3.301258712451522026 ) ) ;
#33691=LINE ( 'NONE', #11420, #21505 ) ;
#33703=CARTESIAN_POINT ( 'NONE',  ( 67.82906190410768943, 58.02404379074640417, 3.985511447369935123 ) ) ;
#33705=EDGE_CURVE ( 'NONE', #2062, #16748, #31432, .T. ) ;
#33707=DIRECTION ( 'NONE',  ( -1.000000000000000000, 0.000000000000000000, 0.000000000000000000 ) ) ;
#33717=CARTESIAN_POINT ( 'NONE',  ( 78.81125837042770854, 65.77339625846090598, -2.277920705665355428 ) ) ;
#33719=CARTESIAN_POINT ( 'NONE',  ( 79.23506694815802121, 65.34107492257680860, 3.003915454719612743 ) ) ;
#33723=VERTEX_POINT ( 'NONE', #12286 ) ;
#33724=CARTESIAN_POINT ( 'NONE',  ( 73.98866219012947454, 61.81968298976576648, -3.762445401688966573 ) ) ;
#33730=CARTESIAN_POINT ( 'NONE',  ( 81.35706873939174955, 65.93413826765582542, 1.000000000000000000 ) ) ;
#33737=CARTESIAN_POINT ( 'NONE',  ( 81.53538963104975323, 62.13961868399318433, 2.518708746844631197 ) ) ;
#33759=CARTESIAN_POINT ( 'NONE',  ( 81.32346312764153140, 61.65804850752792987, -2.069468987430089779 ) ) ;
#33769=ORIENTED_EDGE ( 'NONE', *, *, #34903, .F. ) ;
#33773=CARTESIAN_POINT ( 'NONE',  ( 78.81037980241194418, 65.98117473861063331, -1.881209715725460141 ) ) ;
#33778=CARTESIAN_POINT ( 'NONE',  ( 80.99701317011651724, 65.74337749817941301, -2.326649614738085514 ) ) ;
#33780=ADVANCED_FACE ( 'NONE', ( #29755, #38612 ), #23383, .T. ) ;
#33784=CARTESIAN_POINT ( 'NONE',  ( 73.85752424338471656, 60.59307193704751882, 3.935025356177997757 ) ) ;
#33789=CARTESIAN_POINT ( 'NONE',  ( -63.99293516169444729, 35.89893413629672381, 7.506047544094568202 ) ) ;
#33790=CARTESIAN_POINT ( 'NONE',  ( 79.66325760479746521, 66.16013226748967213, 2.011780557866075458 ) ) ;
#33794=CARTESIAN_POINT ( 'NONE',  ( -64.08758708074093136, 38.76906266698303227, 3.000000000000000000 ) ) ;
#33805=CARTESIAN_POINT ( 'NONE',  ( -75.45330471031414277, 33.71485196875532608, -12.49999999999999645 ) ) ;
#33810=CARTESIAN_POINT ( 'NONE',  ( -2.954197855305039422, -12.43481156997016157, 1.000000000000000000 ) ) ;
#33817=CARTESIAN_POINT ( 'NONE',  ( 67.37456247186543123, 58.43133532855971879, 3.984420468527628767 ) ) ;
#33822=CARTESIAN_POINT ( 'NONE',  ( -58.99872204295123623, 28.54795728317104064, -6.891578894883706674 ) ) ;
#33825=CARTESIAN_POINT ( 'NONE',  ( 80.70729934198669753, 66.20774049649585891, -1.233992409460997086 ) ) ;
#33826=CARTESIAN_POINT ( 'NONE',  ( 78.79648636889820068, 65.96905942459900984, 1.896863055073862103 ) ) ;
#33827=AXIS2_PLACEMENT_3D ( 'NONE', #25804, #29691, #17120 ) ;
#33828=AXIS2_PLACEMENT_3D ( 'NONE', #35714, #20050, #27643 ) ;
#33831=CARTESIAN_POINT ( 'NONE',  ( 77.57912958173203322, 64.32824690378613752, -3.266768353516996903 ) ) ;
#33834=CARTESIAN_POINT ( 'NONE',  ( 78.83208086995163910, 66.11806168415770912, -1.392093260604380545 ) ) ;
#33836=CARTESIAN_POINT ( 'NONE',  ( 77.86640729734749300, 62.36914183036536485, 3.839379600940521442 ) ) ;
#33840=AXIS2_PLACEMENT_3D ( 'NONE', #23766, #36540, #32854 ) ;
#33841=CARTESIAN_POINT ( 'NONE',  ( 80.64785791202346843, 66.17610879001711055, 1.553473047276234587 ) ) ;
#33852=CARTESIAN_POINT ( 'NONE',  ( 81.14431910071698439, 61.29472151471745178, 1.169926324511519455 ) ) ;
#33868=CARTESIAN_POINT ( 'NONE',  ( 69.33847993643759366, 58.44820081139205570, -3.962610901733986335 ) ) ;
#33875=CARTESIAN_POINT ( 'NONE',  ( 69.89919258653301881, 58.73135405362895511, 3.965028736237032891 ) ) ;
#33885=CARTESIAN_POINT ( 'NONE',  ( 79.50676573472793507, 64.15826028415024496, -3.676305632669317536 ) ) ;
#33887=CARTESIAN_POINT ( 'NONE',  ( 80.14906791408208164, 65.90796394341647613, -2.445541897054225977 ) ) ;
#33888=CARTESIAN_POINT ( 'NONE',  ( 78.87241222613832292, 65.34207468649373141, 2.902290250791179194 ) ) ;
#33912=CARTESIAN_POINT ( 'NONE',  ( 67.51064039993573829, 57.98508837280776618, 3.992553130659727056 ) ) ;
#33924=( BOUNDED_CURVE ( )  B_SPLINE_CURVE ( 3, ( #18043, #39458, #39666, #2444 ),
 .UNSPECIFIED., .F., .T. ) 
 B_SPLINE_CURVE_WITH_KNOTS ( ( 4, 4 ),
 ( 0.6656944266037789770, 1.570796326794896558 ),
 .UNSPECIFIED. ) 
 CURVE ( )  GEOMETRIC_REPRESENTATION_ITEM ( )  RATIONAL_B_SPLINE_CURVE ( ( 1.000000000000000000, 0.9328897322841716022, 0.9328897322841716022, 1.000000000000000000 ) ) 
 REPRESENTATION_ITEM ( '' )  );
#33932=CARTESIAN_POINT ( 'NONE',  ( 79.58170130377179419, 64.56493525204570005, -3.531602295408449610 ) ) ;
#33934=CARTESIAN_POINT ( 'NONE',  ( 80.06960825067233145, 63.75365790317244574, 3.697630003121160414 ) ) ;
#33935=LINE ( 'NONE', #12065, #39406 ) ;
#33937=CARTESIAN_POINT ( 'NONE',  ( 74.11268706641025972, 61.54722250361106717, -3.856662941142631418 ) ) ;
#33952=CARTESIAN_POINT ( 'NONE',  ( 81.01997673013200085, 63.86331202395269457, 3.456914256421384835 ) ) ;
#33959=DIRECTION ( 'NONE',  ( 0.000000000000000000, 0.000000000000000000, 1.000000000000000000 ) ) ;
#33963=CARTESIAN_POINT ( 'NONE',  ( -62.85318495816822093, 36.92099889189239548, 4.451173097142760327 ) ) ;
#33970=CARTESIAN_POINT ( 'NONE',  ( 79.60946285158563285, 65.60230831631015747, -2.836177733672711643 ) ) ;
#33979=VERTEX_POINT ( 'NONE', #27080 ) ;
#33981=CARTESIAN_POINT ( 'NONE',  ( 80.36137575039693104, 63.90592395025429795, -3.640670270625565585 ) ) ;
#33989=CARTESIAN_POINT ( 'NONE',  ( 81.48599817137666435, 65.27445208842044622, -2.474249079299299048 ) ) ;
#33994=CARTESIAN_POINT ( 'NONE',  ( 72.66268786488812736, 61.76016136843576021, 3.552420216958366517 ) ) ;
#33997=ORIENTED_EDGE ( 'NONE', *, *, #26909, .F. ) ;
#34004=CARTESIAN_POINT ( 'NONE',  ( 79.11601629524611212, 66.18432715369991115, 1.588372325568262688 ) ) ;
#34015=CIRCLE ( 'NONE', #31359, 10.99999999999998224 ) ;
#34017=DIRECTION ( 'NONE',  ( 0.000000000000000000, -1.000000000000000000, 0.000000000000000000 ) ) ;
#34021=EDGE_CURVE ( 'NONE', #27835, #15467, #21901, .T. ) ;
#34022=ORIENTED_EDGE ( 'NONE', *, *, #25634, .T. ) ;
#34026=CARTESIAN_POINT ( 'NONE',  ( 66.86920591220189181, 57.92326096844472261, -3.999524142429984330 ) ) ;
#34037=CARTESIAN_POINT ( 'NONE',  ( 82.53033050081239708, 64.25366301186836893, -1.000000000000000000 ) ) ;
#34039=CARTESIAN_POINT ( 'NONE',  ( 81.06760980982291187, 61.95377044681377043, 2.747716423863114876 ) ) ;
#34040=DIRECTION ( 'NONE',  ( -0.4690749385695657803, -0.8831583674551003460, 0.000000000000000000 ) ) ;
#34042=CARTESIAN_POINT ( 'NONE',  ( 76.89779646338293162, 61.47851784853094870, -3.801074476324162177 ) ) ;
#34047=CARTESIAN_POINT ( 'NONE',  ( 79.37811825733845694, 65.99825290327332539, -2.263370276487070232 ) ) ;
#34048=CARTESIAN_POINT ( 'NONE',  ( 78.55649010480104266, 62.41317512920507937, 3.780406938340867384 ) ) ;
#34053=CARTESIAN_POINT ( 'NONE',  ( 79.28422506984799156, 66.27750502035060265, 1.322881339814630408 ) ) ;
#34060=CARTESIAN_POINT ( 'NONE',  ( -64.78745217040227544, 34.77601383833187043, 6.355070236019812135 ) ) ;
#34064=DIRECTION ( 'NONE',  ( -0.000000000000000000, -0.000000000000000000, -1.000000000000000000 ) ) ;
#34070=FACE_OUTER_BOUND ( 'NONE', #26766, .T. ) ;
#34083=CARTESIAN_POINT ( 'NONE',  ( 69.57837460818548436, 59.54477471642375974, -3.931953536312648989 ) ) ;
#34095=CARTESIAN_POINT ( 'NONE',  ( 79.80332398823145468, 63.27387486779120707, -3.741985197832890186 ) ) ;
#34098=CARTESIAN_POINT ( 'NONE',  ( 81.04721337197098308, 65.04274187704037047, -3.019849704269078394 ) ) ;
#34099=VERTEX_POINT ( 'NONE', #875 ) ;
#34126=ORIENTED_EDGE ( 'NONE', *, *, #30499, .F. ) ;
#34128=CARTESIAN_POINT ( 'NONE',  ( 67.44728384595320847, 58.15801736331750504, 3.998402061830689025 ) ) ;
#34140=VECTOR ( 'NONE', #17503, 1000.000000000000000 ) ;
#34141=ORIENTED_EDGE ( 'NONE', *, *, #2780, .F. ) ;
#34146=CARTESIAN_POINT ( 'NONE',  ( 79.88758398535436811, 64.02175723273457209, -3.702313260098205383 ) ) ;
#34148=CARTESIAN_POINT ( 'NONE',  ( 80.97211960314545820, 61.55694294823971546, 2.294512580621449693 ) ) ;
#34150=ORIENTED_EDGE ( 'NONE', *, *, #18659, .F. ) ;
#34151=CARTESIAN_POINT ( 'NONE',  ( 73.79885669521775071, 60.72590704978823339, -3.935025356184053802 ) ) ;
#34160=ADVANCED_FACE ( 'NONE', ( #27884 ), #7683, .T. ) ;
#34166=CARTESIAN_POINT ( 'NONE',  ( 81.42847900441165621, 61.86412877313431125, 2.316472630215899109 ) ) ;
#34168=CARTESIAN_POINT ( 'NONE',  ( -74.92283640148282586, 18.87330372387140187, -12.49999999999999645 ) ) ;
#34170=CARTESIAN_POINT ( 'NONE',  ( -64.08758708074093136, 36.14363715547680300, -3.800414904976364028 ) ) ;
#34172=VECTOR ( 'NONE', #26799, 1000.000000000000114 ) ;
#34181=ORIENTED_EDGE ( 'NONE', *, *, #15379, .F. ) ;
#34182=CARTESIAN_POINT ( 'NONE',  ( 80.64987221081615587, 64.05646366546658044, -3.549391953833852753 ) ) ;
#34189=ORIENTED_EDGE ( 'NONE', *, *, #8071, .F. ) ;
#34191=CARTESIAN_POINT ( 'NONE',  ( 80.99721608130789718, 62.45573281339171956, -3.163072811751558522 ) ) ;
#34192=CARTESIAN_POINT ( 'NONE',  ( -58.44033895488188790, 28.22358054771053304, -5.330345403092615619 ) ) ;
#34196=CARTESIAN_POINT ( 'NONE',  ( 79.78161832376089535, 66.22496747522383487, -1.859759604987000658 ) ) ;
#34204=CARTESIAN_POINT ( 'NONE',  ( 73.62310697524999625, 61.12246817794784448, 3.899931323576833808 ) ) ;
#34212=CARTESIAN_POINT ( 'NONE',  ( -54.81017820351302561, 31.50178459264590103, -1.053924518346901706 ) ) ;
#34213=CARTESIAN_POINT ( 'NONE',  ( 79.31479573854763032, 66.13045663638733629, 1.878604182848667037 ) ) ;
#34243=CARTESIAN_POINT ( 'NONE',  ( 81.73112818161179405, 61.68666564161350863, -1.174937739208586907 ) ) ;
#34245=CARTESIAN_POINT ( 'NONE',  ( 80.72665634072043872, 62.99526239489092205, 3.473545878414587396 ) ) ;
#34248=CARTESIAN_POINT ( 'NONE',  ( 76.72366484839760403, 61.84716987400894084, -3.872369636032548357 ) ) ;
#34252=CARTESIAN_POINT ( 'NONE',  ( 81.46310422712103616, 61.87916883045149063, -2.296576099416859140 ) ) ;
#34253=CARTESIAN_POINT ( 'NONE',  ( 78.10617727715707304, 63.31486359019603327, 3.780406938340841183 ) ) ;
#34258=CARTESIAN_POINT ( 'NONE',  ( -58.11978350796148618, 31.63118870160872120, 4.423684907992433857 ) ) ;
#34260=CARTESIAN_POINT ( 'NONE',  ( 82.37993866337130555, 63.11845131094302985, 1.936735430445675421 ) ) ;
#34261=CARTESIAN_POINT ( 'NONE',  ( -64.08758708074093136, 41.64119180419724842, 2.960472586359419900 ) ) ;
#34265=CARTESIAN_POINT ( 'NONE',  ( -62.89138254649398618, 35.56687702170635390, -5.951199099626548694 ) ) ;
#34266=CARTESIAN_POINT ( 'NONE',  ( -64.35089310738592872, 36.57692748661052207, 5.628006413927832519 ) ) ;
#34270=CYLINDRICAL_SURFACE ( 'NONE', #14499, 7.999999999999986677 ) ;
#34271=CARTESIAN_POINT ( 'NONE',  ( -63.58520484588294153, 35.72026407271188475, -6.999999999999999112 ) ) ;
#34276=CARTESIAN_POINT ( 'NONE',  ( 74.75251888580193338, 59.31330218054827697, -3.344918171298342457 ) ) ;
#34282=CARTESIAN_POINT ( 'NONE',  ( -62.99925096543692860, 37.98736139491209940, -4.069933184286554706 ) ) ;
#34288=CARTESIAN_POINT ( 'NONE',  ( 70.80012018114213390, 59.83342440824694819, -3.954977122261608802 ) ) ;
#34295=ADVANCED_FACE ( 'NONE', ( #7431 ), #16889, .F. ) ;
#34303=CARTESIAN_POINT ( 'NONE',  ( 78.85457743492895588, 65.01671056748381261, -3.151254463354985269 ) ) ;
#34305=CARTESIAN_POINT ( 'NONE',  ( 81.80968396272736243, 62.04343910699808617, -2.011780557866150509 ) ) ;
#34306=CARTESIAN_POINT ( 'NONE',  ( 79.89038670178254620, 63.31421865134938542, 3.734652355492745546 ) ) ;
#34321=CARTESIAN_POINT ( 'NONE',  ( -73.07498068578524908, 39.58105274722134226, -46.17089178453873188 ) ) ;
#34323=DIRECTION ( 'NONE',  ( 1.000000000000000000, 0.000000000000000000, 0.000000000000000000 ) ) ;
#34330=EDGE_LOOP ( 'NONE', ( #5087, #37670, #32005, #27030 ) ) ;
#34331=CARTESIAN_POINT ( 'NONE',  ( 66.94886299149460740, 58.16124406473343811, 3.993952884371009926 ) ) ;
#34343=CARTESIAN_POINT ( 'NONE',  ( 25.11437021580303863, 164.7550792202006562, 1.000000000000000000 ) ) ;
#34349=CARTESIAN_POINT ( 'NONE',  ( 80.85043593073625345, 61.68942038033311093, -2.615973384261002010 ) ) ;
#34351=CARTESIAN_POINT ( 'NONE',  ( 79.28293246176357911, 65.06528690105534452, 3.252077313700850070 ) ) ;
#34366=CARTESIAN_POINT ( 'NONE',  ( 81.51669253445732011, 62.40826230823216036, 2.731335034814801777 ) ) ;
#34370=CARTESIAN_POINT ( 'NONE',  ( -64.78473723156626818, 34.77447677474216903, -6.350763366688283007 ) ) ;
#34376=CARTESIAN_POINT ( 'NONE',  ( -62.89148181836048934, 37.17958841060684705, 4.327622075141189129 ) ) ;
#34381=CARTESIAN_POINT ( 'NONE',  ( 78.91475304129780000, 66.06124928554447706, -1.777114115212672596 ) ) ;
#34382=CARTESIAN_POINT ( 'NONE',  ( -63.58520484588292732, 35.72026407271187765, 6.999999999999999112 ) ) ;
#34385=AXIS2_PLACEMENT_3D ( 'NONE', #4596, #39978, #4789 ) ;
#34392=ORIENTED_EDGE ( 'NONE', *, *, #39409, .F. ) ;
#34394=EDGE_LOOP ( 'NONE', ( #5501, #38201, #16719, #26687, #34189, #9271 ) ) ;
#34395=CARTESIAN_POINT ( 'NONE',  ( 79.79114114151838066, 64.70569453017795070, -3.482375488376185046 ) ) ;
#34401=CARTESIAN_POINT ( 'NONE',  ( 80.64500926360288702, 65.89167229754902166, -2.340562087103693845 ) ) ;
#34406=LINE ( 'NONE', #15427, #15595 ) ;
#34407=CARTESIAN_POINT ( 'NONE',  ( 74.36844136632052482, 60.98005461696732254, 3.924711207976818717 ) ) ;
#34414=CARTESIAN_POINT ( 'NONE',  ( 79.60170308687705187, 66.12598108333452274, 2.076176908533791554 ) ) ;
#34418=AXIS2_PLACEMENT_3D ( 'NONE', #12649, #39889, #28094 ) ;
#34429=CARTESIAN_POINT ( 'NONE',  ( 66.43484696874310202, 57.75462747860463963, -4.000000000000005329 ) ) ;
#34432=CARTESIAN_POINT ( 'NONE',  ( -56.24615026952712782, 30.21122693717881802, 1.618048866027589572 ) ) ;
#34435=DIRECTION ( 'NONE',  ( 1.000000000000000000, 0.000000000000000000, 0.000000000000000000 ) ) ;
#34442=CARTESIAN_POINT ( 'NONE',  ( 82.07069543531865463, 65.18928443706812459, -1.480606629406893804 ) ) ;
#34443=CARTESIAN_POINT ( 'NONE',  ( 81.10109024085375040, 61.27893947540407993, 1.252362053669522801 ) ) ;
#34446=CARTESIAN_POINT ( 'NONE',  ( 77.57451768555480953, 61.52186891572922178, -3.722835383490939787 ) ) ;
#34451=CARTESIAN_POINT ( 'NONE',  ( 81.15131294690949915, 61.29729393613784083, -1.130345937366652898 ) ) ;
#34453=CARTESIAN_POINT ( 'NONE',  ( 77.57912958173200479, 64.32824690378610910, 3.266768353517001788 ) ) ;
#34454=VERTEX_POINT ( 'NONE', #16840 ) ;
#34458=CARTESIAN_POINT ( 'NONE',  ( 82.26467961623025360, 63.75423115438312749, 2.259066313177354512 ) ) ;
#34465=CARTESIAN_POINT ( 'NONE',  ( -63.23359472962078343, 35.57513467056965339, 6.582177359050705334 ) ) ;
#34474=CYLINDRICAL_SURFACE ( 'NONE', #10788, 3.000000000000002665 ) ;
#34481=DIRECTION ( 'NONE',  ( -1.000000000000000000, 0.000000000000000000, 0.000000000000000000 ) ) ;
#34482=CARTESIAN_POINT ( 'NONE',  ( 70.63497465855112978, 60.23961165191135336, -3.862811858476220550 ) ) ;
#34484=ORIENTED_EDGE ( 'NONE', *, *, #34843, .T. ) ;
#34485=AXIS2_PLACEMENT_3D ( 'NONE', #8829, #39935, #5763 ) ;
#34493=ORIENTED_EDGE ( 'NONE', *, *, #36300, .F. ) ;
#34497=ORIENTED_EDGE ( 'NONE', *, *, #19642, .T. ) ;
#34498=CARTESIAN_POINT ( 'NONE',  ( 79.66447349905094200, 63.54298318056227401, -3.741985197832887966 ) ) ;
#34501=CARTESIAN_POINT ( 'NONE',  ( 80.10847647497631385, 65.88576991956392703, -2.484976468875493172 ) ) ;
#34502=CARTESIAN_POINT ( 'NONE',  ( 78.88927015299483969, 65.04551736973371590, 3.140153738741057410 ) ) ;
#34505=CARTESIAN_POINT ( 'NONE',  ( 79.68852728668518637, 66.33522678087791746, 1.000000000000000000 ) ) ;
#34526=CIRCLE ( 'NONE', #32510, 7.999999999999986677 ) ;
#34533=CARTESIAN_POINT ( 'NONE',  ( 67.00300875778714271, 58.01168839481970707, 3.999354069328931782 ) ) ;
#34540=ORIENTED_EDGE ( 'NONE', *, *, #18659, .T. ) ;
#34550=CARTESIAN_POINT ( 'NONE',  ( 78.99045122244679362, 65.44959329978490814, -2.843122152733564167 ) ) ;
#34554=CARTESIAN_POINT ( 'NONE',  ( 78.67256861866690087, 65.85712333569000521, 2.031354376635688741 ) ) ;
#34560=CARTESIAN_POINT ( 'NONE',  ( -59.01732008375349636, 27.93907603120367966, 6.194723111030699059 ) ) ;
#34563=CARTESIAN_POINT ( 'NONE',  ( -54.83702497256466302, 31.47896333382912104, 1.097604620046560564 ) ) ;
#34572=CARTESIAN_POINT ( 'NONE',  ( 81.43870310587519157, 62.97649354279256784, 3.113722587674266684 ) ) ;
#34574=DIRECTION ( 'NONE',  ( -0.4690749385695657803, -0.8831583674551003460, 0.000000000000000000 ) ) ;
#34588=CARTESIAN_POINT ( 'NONE',  ( 78.66413930541318678, 66.03995068206980079, -1.171933751919276956 ) ) ;
#34592=ORIENTED_EDGE ( 'NONE', *, *, #40516, .T. ) ;
#34597=EDGE_LOOP ( 'NONE', ( #34540, #24017, #12774, #6921 ) ) ;
#34598=CARTESIAN_POINT ( 'NONE',  ( 79.01164091803717326, 65.74483092438761389, -2.494286432550484989 ) ) ;
#34603=CARTESIAN_POINT ( 'NONE',  ( 79.46293960946091772, 66.21290357410880745, -1.708467252431211003 ) ) ;
#34608=CARTESIAN_POINT ( 'NONE',  ( -63.99293516169446150, 35.89893413629672381, 7.506047544094577084 ) ) ;
#34612=CARTESIAN_POINT ( 'NONE',  ( 73.17398396214588274, 60.59975200455691891, 3.944160774623525434 ) ) ;
#34614=ORIENTED_EDGE ( 'NONE', *, *, #8241, .T. ) ;
#34622=CARTESIAN_POINT ( 'NONE',  ( 81.85373309064779335, 62.29294994509999128, 2.264354540981406316 ) ) ;
#34626=DIRECTION ( 'NONE',  ( 0.000000000000000000, -0.1369933068956149802, -0.9905719730871674900 ) ) ;
#34632=CARTESIAN_POINT ( 'NONE',  ( -64.08758708074093136, 38.13199975834722721, -3.043809435734133650 ) ) ;
#34638=CIRCLE ( 'NONE', #3086, 117.6618724293813898 ) ;
#34640=CARTESIAN_POINT ( 'NONE',  ( 66.42495344877994512, 57.78257748056734755, -4.000000000000014211 ) ) ;
#34648=ORIENTED_EDGE ( 'NONE', *, *, #14086, .F. ) ;
#34652=B_SPLINE_CURVE_WITH_KNOTS ( 'NONE', 3,
 ( #16702, #7252, #20207, #39137, #29681, #32987, #19815, #32391, #4185, #38737, #20010, #4582, #1493, #14026 ),
 .UNSPECIFIED., .F., .F.,
 ( 4, 2, 2, 2, 2, 2, 4 ),
 ( 0.000000000000000000, 0.001249862075310702141, 0.001874793112966059282, 0.002499724150621416424, 0.003124655188276773566, 0.003749586225932131141, 0.004999448301242839787 ),
 .UNSPECIFIED. ) ;
#34653=CARTESIAN_POINT ( 'NONE',  ( 81.82660409393641032, 65.45354236959398975, -1.617049763656951411 ) ) ;
#34654=CARTESIAN_POINT ( 'NONE',  ( 78.63380675089919691, 66.01840951946610403, 1.252362053669530795 ) ) ;
#34657=CARTESIAN_POINT ( 'NONE',  ( 77.97077402951184411, 60.66921691151929963, -3.160174624583422354 ) ) ;
#34661=CARTESIAN_POINT ( 'NONE',  ( 81.32870865761988455, 61.49729006283355659, -1.754135932968038825 ) ) ;
#34663=CARTESIAN_POINT ( 'NONE',  ( 77.77823160594134322, 63.95155898497984026, 3.535928464255528869 ) ) ;
#34667=CARTESIAN_POINT ( 'NONE',  ( 81.91393161461820682, 61.93681595580213184, 1.358135763685229591 ) ) ;
#34684=DIRECTION ( 'NONE',  ( -0.000000000000000000, -0.000000000000000000, -1.000000000000000000 ) ) ;
#34688=CARTESIAN_POINT ( 'NONE',  ( -64.08758708074093136, 37.05642372031412890, -4.717683440820351848 ) ) ;
#34693=CARTESIAN_POINT ( 'NONE',  ( 67.95937142815736820, 58.56762263466062279, -3.988335407916666409 ) ) ;
#34708=CARTESIAN_POINT ( 'NONE',  ( 78.71580656266537801, 64.90148335848421368, -3.195657361810693597 ) ) ;
#34712=CARTESIAN_POINT ( 'NONE',  ( 78.68741431065086545, 66.05648362737333912, -1.057717897339662372 ) ) ;
#34713=CARTESIAN_POINT ( 'NONE',  ( 78.80159527267854003, 65.27891740916035701, 2.934133054905261773 ) ) ;
#34718=ORIENTED_EDGE ( 'NONE', *, *, #14222, .T. ) ;
#34740=CARTESIAN_POINT ( 'NONE',  ( 67.15438370417800229, 58.05139456359000150, 3.999036733496184048 ) ) ;
#34757=CARTESIAN_POINT ( 'NONE',  ( 79.64740672574774294, 64.24900652125727163, -3.657510014241809326 ) ) ;
#34761=CARTESIAN_POINT ( 'NONE',  ( 80.41811942164733296, 62.87504864752338563, 3.537885823842629396 ) ) ;
#34765=CARTESIAN_POINT ( 'NONE',  ( -58.65342201553193746, 29.17550083397324912, 5.453968810494163044 ) ) ;
#34775=CARTESIAN_POINT ( 'NONE',  ( 81.25681022244552310, 61.36874951788873034, 1.439474762807428920 ) ) ;
#34780=TOROIDAL_SURFACE ( 'NONE', #16975, 98.38357402481355507, 3.000000000000000000 ) ;
#34786=DIRECTION ( 'NONE',  ( -0.000000000000000000, -0.000000000000000000, -1.000000000000000000 ) ) ;
#34792=CARTESIAN_POINT ( 'NONE',  ( 81.11573943753921867, 62.50280337846361789, -3.122598816540624433 ) ) ;
#34801=CARTESIAN_POINT ( 'NONE',  ( 78.88238753611517495, 65.83802744495456238, -2.215902410107950526 ) ) ;
#34802=EDGE_CURVE ( 'NONE', #38060, #4188, #13935, .T. ) ;
#34810=CARTESIAN_POINT ( 'NONE',  ( 78.68916368339945677, 66.05772639262713142, -1.037317649801933639 ) ) ;
#34812=CARTESIAN_POINT ( 'NONE',  ( -59.01729896555999488, 27.93936864455021762, -6.195187712944653313 ) ) ;
#34816=CARTESIAN_POINT ( 'NONE',  ( 71.13429564674895289, 59.00621471515203353, 3.925556587156296739 ) ) ;
#34824=CARTESIAN_POINT ( 'NONE',  ( -59.00110696496997775, 28.68040728033255249, -6.999999999999999112 ) ) ;
#34826=CARTESIAN_POINT ( 'NONE',  ( 81.62235710223406215, 64.17388774702372700, 3.017922835037552431 ) ) ;
#34842=CARTESIAN_POINT ( 'NONE',  ( 66.54830849220104483, 57.89461212714910943, -3.999444518117950764 ) ) ;
#34843=EDGE_CURVE ( 'NONE', #25652, #1802, #15141, .T. ) ;
#34846=ORIENTED_EDGE ( 'NONE', *, *, #5494, .T. ) ;
#34851=ORIENTED_EDGE ( 'NONE', *, *, #33189, .F. ) ;
#34856=CARTESIAN_POINT ( 'NONE',  ( 82.47906632153704720, 63.16918237499279343, -1.623788564014418068 ) ) ;
#34857=CARTESIAN_POINT ( 'NONE',  ( 78.99368969759480308, 65.72941799158938636, 2.506402126386323648 ) ) ;
#34861=CARTESIAN_POINT ( 'NONE',  ( 76.45598340902211021, 62.40619074383518949, -3.848392762312481175 ) ) ;
#34865=CARTESIAN_POINT ( 'NONE',  ( 81.32112198246268520, 62.31825444738111486, -2.836177733672716972 ) ) ;
#34866=CARTESIAN_POINT ( 'NONE',  ( 77.57451768555486638, 61.52186891572913652, 3.722835383490897598 ) ) ;
#34869=CARTESIAN_POINT ( 'NONE',  ( -58.99290877059915772, 28.70988844028545373, 6.739549407909634304 ) ) ;
#34870=CARTESIAN_POINT ( 'NONE',  ( 82.10888692569093905, 64.42619117010492857, 2.360008641314786715 ) ) ;
#34872=DIRECTION ( 'NONE',  ( 0.7864880931482275406, 0.000000000000000000, 0.6176054398530382850 ) ) ;
#34876=CARTESIAN_POINT ( 'NONE',  ( -62.78278205347341867, 35.70412497698344367, 5.569918731383189048 ) ) ;
#34884=CARTESIAN_POINT ( 'NONE',  ( 80.71264223670345928, 61.13836533427188158, -1.655461010748698669 ) ) ;
#34889=CARTESIAN_POINT ( 'NONE',  ( -64.08758708074093136, 36.87876644325631759, -4.900609702795900802 ) ) ;
#34896=CARTESIAN_POINT ( 'NONE',  ( 68.06744372826909739, 58.27867795456629807, -3.994255761866621235 ) ) ;
#34903=EDGE_CURVE ( 'NONE', #2062, #9255, #39036, .T. ) ;
#34907=LINE ( 'NONE', #16140, #1132 ) ;
#34908=CARTESIAN_POINT ( 'NONE',  ( 78.66413930541318678, 66.03995068206980079, 1.171933751919278732 ) ) ;
#34909=ORIENTED_EDGE ( 'NONE', *, *, #30743, .F. ) ;
#34912=VERTEX_POINT ( 'NONE', #10440 ) ;
#34913=CARTESIAN_POINT ( 'NONE',  ( 79.10818533696262023, 64.58014521944367914, -3.489618106120226049 ) ) ;
#34916=CARTESIAN_POINT ( 'NONE',  ( 81.65270467917648034, 63.44102909743352825, -3.019969592843240846 ) ) ;
#34917=CARTESIAN_POINT ( 'NONE',  ( 80.10726245975679660, 62.76215410473258771, 3.584461231902855705 ) ) ;
#34922=ORIENTED_EDGE ( 'NONE', *, *, #11645, .F. ) ;
#34940=CARTESIAN_POINT ( 'NONE',  ( 66.72344311391505300, 57.86780257000127392, 3.999628797551961767 ) ) ;
#34941=DIRECTION ( 'NONE',  ( -0.000000000000000000, 0.000000000000000000, 1.000000000000000000 ) ) ;
#34947=DIRECTION ( 'NONE',  ( 0.000000000000000000, 0.000000000000000000, 1.000000000000000000 ) ) ;
#34954=CARTESIAN_POINT ( 'NONE',  ( 78.67256861866690087, 65.85712333569000521, -2.031354376635688297 ) ) ;
#34956=CARTESIAN_POINT ( 'NONE',  ( 80.72421460287552009, 62.36539998118918504, 3.243225924683090344 ) ) ;
#34975=CYLINDRICAL_SURFACE ( 'NONE', #33297, 6.329987104167475565 ) ;
#34976=CARTESIAN_POINT ( 'NONE',  ( 78.67529526371438919, 66.04787469174290493, 1.130345937366638465 ) ) ;
#34983=CARTESIAN_POINT ( 'NONE',  ( -63.58520484588292732, 35.72026407271188475, 6.999999999999987566 ) ) ;
#34985=DIRECTION ( 'NONE',  ( 0.000000000000000000, 0.000000000000000000, 1.000000000000000000 ) ) ;
#34991=CARTESIAN_POINT ( 'NONE',  ( 78.76190985582823600, 66.07042273533498644, -1.483717294826052635 ) ) ;
#35003=CARTESIAN_POINT ( 'NONE',  ( 81.10500554505480864, 61.42844135377572456, -1.938154327158297940 ) ) ;
#35007=CARTESIAN_POINT ( 'NONE',  ( 81.70897365440940519, 61.83459377731552564, -1.744953761006742265 ) ) ;
#35009=( BOUNDED_SURFACE ( )  B_SPLINE_SURFACE ( 3, 2, ( 
 ( #24949, #18542, #19170 ),
 ( #15672, #2945, #15462 ),
 ( #40568, #3357, #25353 ),
 ( #28021, #6622, #37483 ),
 ( #26116, #9279, #34432 ),
 ( #3550, #38649, #13543 ),
 ( #28219, #6211, #18756 ),
 ( #31331, #25145, #9481 ),
 ( #12578, #16819, #26711 ),
 ( #14533, #27107, #10643 ),
 ( #5085, #32696, #8356 ),
 ( #35785, #23802, #17411 ),
 ( #39245, #17016, #26904 ),
 ( #32493, #8148, #10843 ),
 ( #24004, #30196, #7763 ),
 ( #36179, #1809, #1217 ),
 ( #14334, #23221, #7960 ),
 ( #26511, #36579, #39657 ),
 ( #11439, #29995, #14135 ),
 ( #20117, #23613, #36379 ),
 ( #11036, #4496, #4295 ),
 ( #20509, #33093, #4876 ) ),
 .UNSPECIFIED., .F., .F., .T. ) 
 B_SPLINE_SURFACE_WITH_KNOTS ( ( 4, 2, 2, 2, 2, 2, 2, 2, 2, 2, 4 ),
 ( 3, 3 ),
 ( 0.02037793668903936650, 0.02161998616042463614, 0.02224101089611726922, 0.02286203563180990578, 0.02410408510319517195, 0.02534613457458044158, 0.02658818404596571122, 0.02720920878165834431, 0.02783023351735097739, 0.02907228298873624703, 0.03031433246012151667 ),
 ( 0.000000000000000000, 0.8973666424348171189 ),
 .UNSPECIFIED. ) 
 GEOMETRIC_REPRESENTATION_ITEM ( )  RATIONAL_B_SPLINE_SURFACE ( (
 ( 1.000000000000000000, 0.7371673956414459550, 0.9460492146741605879),
 ( 1.000000000000000000, 0.7430206879744455373, 0.9472507007640531551),
 ( 1.000000000000000000, 0.7496157519951666126, 0.9486044478916609846),
 ( 1.000000000000000000, 0.7607417901526166704, 0.9508882531966559304),
 ( 1.000000000000000000, 0.7646561537746499049, 0.9516917417591763684),
 ( 1.000000000000000000, 0.7729170770629312237, 0.9533874343465059686),
 ( 1.000000000000000000, 0.7772865941316164928, 0.9542843507619009902),
 ( 1.000000000000000000, 0.7908687655009780659, 0.9570723184632274894),
 ( 1.000000000000000000, 0.8005515303433323737, 0.9590598677957974383),
 ( 1.000000000000000000, 0.8209981033988819066, 0.9632568686825830895),
 ( 1.000000000000000000, 0.8318680535256515185, 0.9654881076387360483),
 ( 1.000000000000000000, 0.8536763389692737514, 0.9699646227543736732),
 ( 1.000000000000000000, 0.8646174610552631590, 0.9722104709448051718),
 ( 1.000000000000000000, 0.8804437197805391468, 0.9754590750861457105),
 ( 1.000000000000000000, 0.8856184224478880207, 0.9765212693044487136),
 ( 1.000000000000000000, 0.8956081928670621695, 0.9785718366632991660),
 ( 1.000000000000000000, 0.9004099586942047040, 0.9795574793614618692),
 ( 1.000000000000000000, 0.9136990522410565196, 0.9822852879408843219),
 ( 1.000000000000000000, 0.9211930079257203419, 0.9838235476076078179),
 ( 1.000000000000000000, 0.9316451890867147867, 0.9859690325004727418),
 ( 1.000000000000000000, 0.9343530544005290706, 0.9865248671184547735),
 ( 1.000000000000000000, 0.9340560540550033597, 0.9864639028331361192) ) ) 
 REPRESENTATION_ITEM ( '' )  SURFACE ( )  );
#35010=CARTESIAN_POINT ( 'NONE',  ( -59.00042985273041296, 28.09738993419675879, -6.357743741181010932 ) ) ;
#35012=CARTESIAN_POINT ( 'NONE',  ( -54.79610818216033152, 31.51396769785350926, -1.000000000000000000 ) ) ;
#35014=CARTESIAN_POINT ( 'NONE',  ( 70.73355890789336797, 59.99733340013641936, 3.925556587156273647 ) ) ;
#35023=CARTESIAN_POINT ( 'NONE',  ( 81.41826528540525487, 63.68099735520212334, 3.235508711566408291 ) ) ;
#35034=CIRCLE ( 'NONE', #13282, 80.68529983683480111 ) ;
#35036=CARTESIAN_POINT ( 'NONE',  ( -63.99293516169446150, 35.89893413629672381, -46.17089178453873188 ) ) ;
#35042=CARTESIAN_POINT ( 'NONE',  ( 66.70872257673579497, 57.90880667275003901, -3.999713739233791809 ) ) ;
#35054=CARTESIAN_POINT ( 'NONE',  ( 79.66449323073855737, 66.32230831612966426, -1.250177805244664375 ) ) ;
#35055=CARTESIAN_POINT ( 'NONE',  ( 80.62495340926818699, 62.95361341830508906, 3.497296750721714531 ) ) ;
#35058=CARTESIAN_POINT ( 'NONE',  ( 74.65712387123647886, 61.84722771748617731, -3.833662259905225689 ) ) ;
#35060=CARTESIAN_POINT ( 'NONE',  ( -80.78329181448161478, 33.71485196875532608, -9.800414904976365804 ) ) ;
#35062=CARTESIAN_POINT ( 'NONE',  ( 79.83674225097148280, 65.44563770485289922, -3.036434590848173354 ) ) ;
#35063=CARTESIAN_POINT ( 'NONE',  ( 77.00710955723607753, 62.69977232050452898, 3.829716617887278129 ) ) ;
#35070=CARTESIAN_POINT ( 'NONE',  ( 81.63785901438880899, 61.64013749223438055, 1.421876342974067953 ) ) ;
#35075=CARTESIAN_POINT ( 'NONE',  ( -64.66796849410251014, 36.23110552202055601, 6.165526157072423352 ) ) ;
#35077=DIRECTION ( 'NONE',  ( -1.000000000000000000, 0.000000000000000000, 0.000000000000000000 ) ) ;
#35078=DIRECTION ( 'NONE',  ( -0.000000000000000000, -0.000000000000000000, -1.000000000000000000 ) ) ;
#35083=CARTESIAN_POINT ( 'NONE',  ( 72.82849231964733860, 58.84329089963347315, -3.620304665786997944 ) ) ;
#35091=VERTEX_POINT ( 'NONE', #36571 ) ;
#35093=CARTESIAN_POINT ( 'NONE',  ( 67.89958468297673733, 58.72729936788584837, -3.969942683317639887 ) ) ;
#35096=CARTESIAN_POINT ( 'NONE',  ( -64.08758708074093136, 36.14363715547680300, 3.800414904976363140 ) ) ;
#35102=CARTESIAN_POINT ( 'NONE',  ( 79.28289924135637534, 65.69038102574751292, 2.688322534164183875 ) ) ;
#35106=CARTESIAN_POINT ( 'NONE',  ( 79.32744125533960755, 63.05206431288016944, -3.774260586041107590 ) ) ;
#35109=CARTESIAN_POINT ( 'NONE',  ( 81.44087877708807355, 61.54565157041660939, -1.662073781712719578 ) ) ;
#35110=CARTESIAN_POINT ( 'NONE',  ( 78.82422632494606773, 64.37263203041347026, 3.536670452273166454 ) ) ;
#35113=CARTESIAN_POINT ( 'NONE',  ( 80.70729934198679700, 66.20774049649591575, 1.233992409460102690 ) ) ;
#35114=CARTESIAN_POINT ( 'NONE',  ( -64.08758708074093136, 42.49506848485115285, 2.672780004071997784 ) ) ;
#35134=CARTESIAN_POINT ( 'NONE',  ( -69.08758708074093136, -65.19654454972992141, -3.800414904976364028 ) ) ;
#35138=ADVANCED_FACE ( 'NONE', ( #21554 ), #35254, .T. ) ;
#35139=LINE ( 'NONE', #5380, #31507 ) ;
#35141=CARTESIAN_POINT ( 'NONE',  ( 66.55417948260128469, 57.87814544581552667, 3.999688274315071013 ) ) ;
#35143=CARTESIAN_POINT ( 'NONE',  ( -64.08758708074093136, 38.55592700272002560, 3.000000000000461409 ) ) ;
#35154=CARTESIAN_POINT ( 'NONE',  ( 80.14986013843031287, 63.43437088187636874, -3.706996517075248576 ) ) ;
#35156=LINE ( 'NONE', #2268, #3659 ) ;
#35157=CARTESIAN_POINT ( 'NONE',  ( 78.52976371562813540, 65.87711177338800894, 1.796258654642608255 ) ) ;
#35174=CARTESIAN_POINT ( 'NONE',  ( 80.64987221081617008, 64.05646366546658044, 3.549391953833848312 ) ) ;
#35186=CARTESIAN_POINT ( 'NONE',  ( 68.72765198451649837, 58.29585788764496357, 3.976359261632545827 ) ) ;
#35190=AXIS2_PLACEMENT_3D ( 'NONE', #2869, #34574, #17855 ) ;
#35193=CARTESIAN_POINT ( 'NONE',  ( 79.99568124201523744, 64.83088095446822763, -3.420541042474577242 ) ) ;
#35203=CARTESIAN_POINT ( 'NONE',  ( 80.53350286136132752, 63.24990014040474051, -3.607546830629782875 ) ) ;
#35205=EDGE_CURVE ( 'NONE', #36353, #16830, #27960, .T. ) ;
#35213=CARTESIAN_POINT ( 'NONE',  ( -64.08758708074093136, 44.07167558249655315, -1.395429732795050226 ) ) ;
#35214=CARTESIAN_POINT ( 'NONE',  ( 69.52987064631375347, 59.66723168662304033, 3.901551322707137004 ) ) ;
#35224=CARTESIAN_POINT ( 'NONE',  ( 80.57438652550355584, 65.15318659309524207, 3.125353918848692292 ) ) ;
#35243=CARTESIAN_POINT ( 'NONE',  ( 66.56005047484954673, 57.86167872611329699, -3.999845987730312746 ) ) ;
#35248=( BOUNDED_SURFACE ( )  B_SPLINE_SURFACE ( 3, 2, ( 
 ( #17424, #29607, #39466 ),
 ( #24441, #12498, #6128 ),
 ( #15377, #5715, #15589 ),
 ( #37805, #37602, #3276 ) ),
 .UNSPECIFIED., .F., .F., .F. ) 
 B_SPLINE_SURFACE_WITH_KNOTS ( ( 4, 4 ),
 ( 3, 3 ),
 ( 4.712388980384689674, 4.860526820865776365 ),
 ( 0.000000000000000000, 1.000000000000000000 ),
 .UNSPECIFIED. ) 
 GEOMETRIC_REPRESENTATION_ITEM ( )  RATIONAL_B_SPLINE_SURFACE ( (
 ( 1.000000000000000000, 0.7071067811865473507, 1.000000000000000000),
 ( 1.000000000000000000, 0.7005474459265798037, 1.000000000000000000),
 ( 1.000000000000000000, 0.6938961412926945016, 1.000000000000000000),
 ( 1.000000000000000000, 0.6872206705711640939, 1.000000000000000000) ) ) 
 REPRESENTATION_ITEM ( '' )  SURFACE ( )  );
#35254=TOROIDAL_SURFACE ( 'NONE', #30628, 5.681288188914805026, 1.000000000000000000 ) ;
#35255=CARTESIAN_POINT ( 'NONE',  ( 82.35700292606934170, 63.80179554273352238, -2.078018481493677516 ) ) ;
#35259=CARTESIAN_POINT ( 'NONE',  ( 75.12771622566773999, 62.30414178837923345, -3.756674307852014394 ) ) ;
#35264=CARTESIAN_POINT ( 'NONE',  ( 77.39092423430432177, 61.90746491491122327, 3.829716617890443153 ) ) ;
#35271=CARTESIAN_POINT ( 'NONE',  ( 81.39647959751771111, 65.22731470771827844, 2.622983904469076588 ) ) ;
#35291=CARTESIAN_POINT ( 'NONE',  ( 67.98336428835678191, 58.50351186300884621, -3.992939643064463695 ) ) ;
#35304=CARTESIAN_POINT ( 'NONE',  ( 81.21900516562017458, 61.35514353465740101, 1.483717294825997790 ) ) ;
#35306=CARTESIAN_POINT ( 'NONE',  ( 81.16957891225059996, 61.30398062001309256, 1.000000000000000000 ) ) ;
#35308=CARTESIAN_POINT ( 'NONE',  ( 77.90798433017856439, 65.01733068894688472, -2.764360460937554720 ) ) ;
#35311=MECHANICAL_DESIGN_GEOMETRIC_PRESENTATION_REPRESENTATION('',(#35967),#32015);
#35313=CARTESIAN_POINT ( 'NONE',  ( 81.69769846483475817, 62.77423530097588156, -2.811330881955112382 ) ) ;
#35314=CARTESIAN_POINT ( 'NONE',  ( 79.95886636011078963, 62.14075979114826254, 3.401284978681017090 ) ) ;
#35316=ADVANCED_FACE ( 'NONE', ( #3047 ), #22973, .T. ) ;
#35318=DIRECTION ( 'NONE',  ( -0.000000000000000000, -0.000000000000000000, -1.000000000000000000 ) ) ;
#35319=CARTESIAN_POINT ( 'NONE',  ( 79.68852728668518637, 66.33522678087791746, 1.065376284871803803 ) ) ;
#35320=DIRECTION ( 'NONE',  ( -0.000000000000000000, -0.000000000000000000, -1.000000000000000000 ) ) ;
#35323=CARTESIAN_POINT ( 'NONE',  ( -64.42495406928412649, 36.58927325464082259, -5.700117363499904499 ) ) ;
#35342=EDGE_LOOP ( 'NONE', ( #31787, #18562, #27408, #19324 ) ) ;
#35343=CARTESIAN_POINT ( 'NONE',  ( 66.68223030933245354, 57.98259542220473861, 3.998057522776775841 ) ) ;
#35355=CARTESIAN_POINT ( 'NONE',  ( 78.73521632358543343, 65.70333808056810199, -2.340042473998858785 ) ) ;
#35357=CARTESIAN_POINT ( 'NONE',  ( 80.96289755590217396, 61.39497013797971192, 2.048264032867408879 ) ) ;
#35367=AXIS2_PLACEMENT_3D ( 'NONE', #8697, #15495, #30962 ) ;
#35372=ORIENTED_EDGE ( 'NONE', *, *, #19889, .F. ) ;
#35378=CARTESIAN_POINT ( 'NONE',  ( 81.14353007428552189, 63.18723978346950076, 3.330128783915581092 ) ) ;
#35388=CARTESIAN_POINT ( 'NONE',  ( 69.25747553239096987, 58.65839085985714974, 3.984982412582168010 ) ) ;
#35391=CARTESIAN_POINT ( 'NONE',  ( -64.08758708074094557, 43.44355869293354999, -1.729337825382090132 ) ) ;
#35394=CARTESIAN_POINT ( 'NONE',  ( 79.02829278184947270, 65.95432764922180979, -2.098997056523009164 ) ) ;
#35403=CARTESIAN_POINT ( 'NONE',  ( 79.23506694815775120, 65.34107492257662386, -3.003915454719717992 ) ) ;
#35417=CARTESIAN_POINT ( 'NONE',  ( 69.80049859759003539, 58.98221833774336176, 3.985452289341161691 ) ) ;
#35421=ORIENTED_EDGE ( 'NONE', *, *, #9157, .F. ) ;
#35425=CARTESIAN_POINT ( 'NONE',  ( 81.32842084066379584, 61.39880091617793312, 1.358900964592128391 ) ) ;
#35427=ORIENTED_EDGE ( 'NONE', *, *, #12021, .T. ) ;
#35428=CIRCLE ( 'NONE', #11040, 80.68529983683480111 ) ;
#35433=LINE ( 'NONE', #29439, #20666 ) ;
#35436=CARTESIAN_POINT ( 'NONE',  ( -63.08379346057677139, 18.80112958435941906, -46.17089178453873188 ) ) ;
#35448=CARTESIAN_POINT ( 'NONE',  ( 0.000000000000000000, 0.000000000000000000, 0.000000000000000000 ) ) ;
#35450=CARTESIAN_POINT ( 'NONE',  ( -55.72565997008025818, 31.19966888624891865, -3.920894724096664508 ) ) ;
#35454=CARTESIAN_POINT ( 'NONE',  ( 81.71086237227936522, 61.67650090218637615, -1.250621450094242304 ) ) ;
#35458=CARTESIAN_POINT ( 'NONE',  ( 75.94307401167466764, 60.53934701228696014, -3.685888554891455282 ) ) ;
#35462=CARTESIAN_POINT ( 'NONE',  ( 76.45598340902213863, 62.40619074383512555, 3.848392762312490945 ) ) ;
#35468=CARTESIAN_POINT ( 'NONE',  ( 79.18750747900355691, 66.22443723336836285, 1.498428902123875694 ) ) ;
#35475=CARTESIAN_POINT ( 'NONE',  ( 66.60662334906898252, 57.77574420286332213, 3.999150726296102132 ) ) ;
#35488=CARTESIAN_POINT ( 'NONE',  ( 67.53434038244741089, 57.92037869207645429, -3.987264345885670913 ) ) ;
#35493=AXIS2_PLACEMENT_3D ( 'NONE', #12191, #25168, #22302 ) ;
#35501=CARTESIAN_POINT ( 'NONE',  ( 78.99338515863716736, 65.92867347524024524, 2.125034277891690415 ) ) ;
#35502=CARTESIAN_POINT ( 'NONE',  ( -63.67242066106361165, 44.20199017310434897, 2.029227019513839103 ) ) ;
#35505=CARTESIAN_POINT ( 'NONE',  ( 77.70122879141796091, 65.35873351754847249, -2.061059937946295495 ) ) ;
#35508=CARTESIAN_POINT ( 'NONE',  ( 81.53035370526046677, 63.02147265739189663, -3.059106349689736160 ) ) ;
#35509=CARTESIAN_POINT ( 'NONE',  ( 79.63188232868596117, 63.19436791590091218, 3.756013696796379087 ) ) ;
#35513=CARTESIAN_POINT ( 'NONE',  ( 80.68997016403565681, 66.19852044017257242, 1.342843868341103697 ) ) ;
#35517=FACE_OUTER_BOUND ( 'NONE', #13949, .T. ) ;
#35518=EDGE_LOOP ( 'NONE', ( #12539, #38713, #27136, #37844, #11603, #35731, #82 ) ) ;
#35539=CARTESIAN_POINT ( 'NONE',  ( 66.56592146697632018, 57.84521198437244038, 3.999917672785076483 ) ) ;
#35541=EDGE_CURVE ( 'NONE', #14204, #21757, #11515, .T. ) ;
#35554=CARTESIAN_POINT ( 'NONE',  ( 78.63837616148840937, 65.82632162494834915, -2.064111563736707566 ) ) ;
#35556=B_SPLINE_CURVE_WITH_KNOTS ( 'NONE', 3,
 ( #5507, #4895, #17425, #21367 ),
 .UNSPECIFIED., .F., .F.,
 ( 4, 4 ),
 ( 2.602085213965210642E-18, 0.0006739815419856351204 ),
 .UNSPECIFIED. ) ;
#35557=CARTESIAN_POINT ( 'NONE',  ( 78.69934701664540455, 65.67047266146715856, 2.368006059520778805 ) ) ;
#35565=CARTESIAN_POINT ( 'NONE',  ( 78.56547728078845694, 65.96989904497856116, -1.378793396233028323 ) ) ;
#35573=CARTESIAN_POINT ( 'NONE',  ( 81.24750358194776823, 61.36520210808431841, 1.450104216466337581 ) ) ;
#35576=LINE ( 'NONE', #29379, #24699 ) ;
#35583=CARTESIAN_POINT ( 'NONE',  ( -63.08758708074093136, 38.76906266698302517, -3.000000000000000000 ) ) ;
#35584=CARTESIAN_POINT ( 'NONE',  ( 68.97355662219305827, 59.39279559060015146, 3.921432738910643589 ) ) ;
#35589=CARTESIAN_POINT ( 'NONE',  ( 78.73750597996149736, 66.05139304066524630, -1.520709669156475430 ) ) ;
#35599=CARTESIAN_POINT ( 'NONE',  ( 78.96452808758077424, 65.70328965153812817, -2.526545245021140307 ) ) ;
#35604=ORIENTED_EDGE ( 'NONE', *, *, #10903, .T. ) ;
#35606=DIRECTION ( 'NONE',  ( -1.000000000000000000, 0.000000000000000000, 0.000000000000000000 ) ) ;
#35607=CARTESIAN_POINT ( 'NONE',  ( -59.00613449831566726, 28.05080808729636743, -6.322111786795005628 ) ) ;
#35610=CARTESIAN_POINT ( 'NONE',  ( 70.83363217041421933, 59.75074159095914439, 3.963404584535427322 ) ) ;
#35620=CARTESIAN_POINT ( 'NONE',  ( 81.69418451911097634, 62.49370361017244591, 2.611089443243005181 ) ) ;
#35642=CARTESIAN_POINT ( 'NONE',  ( 66.27376694609004915, 57.73522568913436004, -4.000000000000000000 ) ) ;
#35644=EDGE_LOOP ( 'NONE', ( #17328, #22082, #24277, #31426 ) ) ;
#35647=CARTESIAN_POINT ( 'NONE',  ( -57.95974551600830438, 28.52258727176714004, -2.765331207962145932 ) ) ;
#35651=CARTESIAN_POINT ( 'NONE',  ( 79.63539728012710839, 66.30663591242939958, -1.358135763685573760 ) ) ;
#35655=CARTESIAN_POINT ( 'NONE',  ( 76.23342353645792002, 61.41352271612331037, -3.867068906741287115 ) ) ;
#35659=CARTESIAN_POINT ( 'NONE',  ( 75.68803578311079150, 63.95394130778559116, 2.805892758485419414 ) ) ;
#35667=CARTESIAN_POINT ( 'NONE',  ( 80.99701317011684409, 65.74337749817958354, 2.326649614737514860 ) ) ;
#35684=EDGE_CURVE ( 'NONE', #18734, #13498, #18133, .T. ) ;
#35687=DIRECTION ( 'NONE',  ( -1.000000000000000000, 0.000000000000000000, 0.000000000000000000 ) ) ;
#35688=CARTESIAN_POINT ( 'NONE',  ( 67.42350544106223253, 58.22289815522609047, -3.997566301760141272 ) ) ;
#35692=CARTESIAN_POINT ( 'NONE',  ( -64.08758708074094557, 36.44316031593028526, 3.600279212593497480 ) ) ;
#35693=CARTESIAN_POINT ( 'NONE',  ( 78.69038500580363404, 66.05859403932464602, 1.000000000000000000 ) ) ;
#35700=CARTESIAN_POINT ( 'NONE',  ( 81.26055678261324999, 61.79680472324191243, 2.407735119910396016 ) ) ;
#35701=CARTESIAN_POINT ( 'NONE',  ( -63.57031559648750374, 43.64086948594911064, 2.909459873249482076 ) ) ;
#35702=VERTEX_POINT ( 'NONE', #16108 ) ;
#35703=CARTESIAN_POINT ( 'NONE',  ( 79.57145864546818359, 62.55878779196849848, -3.641957811749160445 ) ) ;
#35706=CARTESIAN_POINT ( 'NONE',  ( 80.65926296283754482, 64.83599339274806539, -3.316380171282755196 ) ) ;
#35708=CARTESIAN_POINT ( 'NONE',  ( 80.51696178947716476, 61.27878891920005344, 2.305838555345019802 ) ) ;
#35711=CARTESIAN_POINT ( 'NONE',  ( 80.71704827558885142, 66.21292280724348700, 1.118100487915077546 ) ) ;
#35714=CARTESIAN_POINT ( 'NONE',  ( -55.15112219448760555, 31.23515184556838165, 9.800414904976365804 ) ) ;
#35731=ORIENTED_EDGE ( 'NONE', *, *, #40430, .T. ) ;
#35734=CARTESIAN_POINT ( 'NONE',  ( 66.87313677512783272, 57.91234881663538658, 3.999382933222194847 ) ) ;
#35735=CARTESIAN_POINT ( 'NONE',  ( 72.04157359233609270, 60.08177168861285367, -3.962431611490357053 ) ) ;
#35737=AXIS2_PLACEMENT_3D ( 'NONE', #37327, #17970, #40405 ) ;
#35747=ORIENTED_EDGE ( 'NONE', *, *, #33230, .F. ) ;
#35748=CARTESIAN_POINT ( 'NONE',  ( 80.67643653137164961, 61.85813826494483436, -2.902290250791175197 ) ) ;
#35750=CARTESIAN_POINT ( 'NONE',  ( 78.75315097705565393, 65.71977079011902845, 2.326060681237297256 ) ) ;
#35769=CARTESIAN_POINT ( 'NONE',  ( 81.24448906778437163, 62.55865020921709885, 3.071811904357649947 ) ) ;
#35781=CARTESIAN_POINT ( 'NONE',  ( 78.83705574937599181, 66.00318003113706311, -1.852607187800925148 ) ) ;
#35785=CARTESIAN_POINT ( 'NONE',  ( -58.49128007771433602, 30.53048970692593400, 5.009453334674668135 ) ) ;
#35795=CARTESIAN_POINT ( 'NONE',  ( 80.10672643282856598, 63.77302114994530768, -3.692178340560190453 ) ) ;
#35796=DIRECTION ( 'NONE',  ( -0.000000000000000000, 0.000000000000000000, -1.000000000000000000 ) ) ;
#35797=CARTESIAN_POINT ( 'NONE',  ( 79.92294945466714751, 64.42298636752006757, 3.607546830629786427 ) ) ;
#35817=CARTESIAN_POINT ( 'NONE',  ( 78.82533416220519484, 66.11379887182081916, 1.400336002811356950 ) ) ;
#35840=CARTESIAN_POINT ( 'NONE',  ( 66.27376694609004915, 57.73522568913436004, -4.000000000000000000 ) ) ;
#35848=CARTESIAN_POINT ( 'NONE',  ( 81.23565735523285980, 65.86993722804045603, -1.793694987646317074 ) ) ;
#35849=VECTOR ( 'NONE', #22608, 1000.000000000000000 ) ;
#35856=CARTESIAN_POINT ( 'NONE',  ( 74.85245598970902847, 62.88263772385703732, 3.424891502433892843 ) ) ;
#35866=CARTESIAN_POINT ( 'NONE',  ( 82.17930952126353361, 63.71034004053225175, 2.400449347018089430 ) ) ;
#35886=CARTESIAN_POINT ( 'NONE',  ( 67.45521008556633547, 58.13638817365040978, -3.998402061830689025 ) ) ;
#35899=CARTESIAN_POINT ( 'NONE',  ( 81.20616577872307573, 61.45478060783981533, 1.852607187800907385 ) ) ;
#35902=CARTESIAN_POINT ( 'NONE',  ( 78.94057287092958575, 63.80484286357250312, -3.729426069516720954 ) ) ;
#35905=CARTESIAN_POINT ( 'NONE',  ( 80.14223387231542972, 65.61881967979002184, -2.852119850606566143 ) ) ;
#35906=CARTESIAN_POINT ( 'NONE',  ( 78.28284693538141426, 65.31437991193503478, 2.608847861177645111 ) ) ;
#35912=CARTESIAN_POINT ( 'NONE',  ( 81.58705100058477910, 65.69127060146946917, 1.444831904608907092 ) ) ;
#35913=DIRECTION ( 'NONE',  ( -0.000000000000000000, -0.000000000000000000, -1.000000000000000000 ) ) ;
#35915=CARTESIAN_POINT ( 'NONE',  ( -62.81463675898083210, 36.67811266762163314, -4.600311178732271244 ) ) ;
#35932=CARTESIAN_POINT ( 'NONE',  ( 66.42396409678352143, 57.78537248076371213, 4.000000000000012434 ) ) ;
#35933=CARTESIAN_POINT ( 'NONE',  ( 73.22742653720867168, 60.47695785811286839, -3.944160774617319287 ) ) ;
#35945=CARTESIAN_POINT ( 'NONE',  ( 80.80786883982545987, 61.35646782832053248, -2.148686496494742304 ) ) ;
#35947=CARTESIAN_POINT ( 'NONE',  ( 80.26059561567569745, 63.13455243780983750, 3.653685850874063501 ) ) ;
#35951=EDGE_CURVE ( 'NONE', #4319, #21175, #23410, .T. ) ;
#35962=CARTESIAN_POINT ( 'NONE',  ( 78.76190985582825022, 66.07042273533500065, 1.483717294826051081 ) ) ;
#35967=STYLED_ITEM('',(#40745),#39670);
#35971=CARTESIAN_POINT ( 'NONE',  ( -64.28431955412808918, 34.79066690201138812, 5.195917981389134965 ) ) ;
#35975=CARTESIAN_POINT ( 'NONE',  ( 67.40765644887963504, 58.26613713413648554, 3.996173465816879489 ) ) ;
#35979=CARTESIAN_POINT ( 'NONE',  ( 81.02087009143656360, 62.46468763289096415, -3.155412080370040950 ) ) ;
#35990=CARTESIAN_POINT ( 'NONE',  ( 80.30571993285261101, 63.50758298881786601, -3.683925914261567236 ) ) ;
#35993=CARTESIAN_POINT ( 'NONE',  ( 80.96353394671049841, 62.18107606247197339, 2.978180346930981770 ) ) ;
#36012=CARTESIAN_POINT ( 'NONE',  ( 81.29907532208984833, 61.38588276545821998, 1.392093260605081317 ) ) ;
#36023=DIRECTION ( 'NONE',  ( -0.000000000000000000, 1.000000000000000000, -0.000000000000000000 ) ) ;
#36037=CARTESIAN_POINT ( 'NONE',  ( 66.27376694609004915, 57.73522568913436004, -4.000000000000000000 ) ) ;
#36049=CARTESIAN_POINT ( 'NONE',  ( 82.50803812506887880, 63.51743744066179431, -1.680016503630877178 ) ) ;
#36056=CARTESIAN_POINT ( 'NONE',  ( 74.52260502535293085, 62.13706486897681458, 3.724166978290282426 ) ) ;
#36058=DIRECTION ( 'NONE',  ( -1.000000000000000000, 0.000000000000000000, 0.000000000000000000 ) ) ;
#36064=CARTESIAN_POINT ( 'NONE',  ( 81.59006957456236364, 61.61658442860581175, 1.498428902123875028 ) ) ;
#36072=DIRECTION ( 'NONE',  ( -1.000000000000000000, 0.000000000000000000, 0.000000000000000000 ) ) ;
#36086=CARTESIAN_POINT ( 'NONE',  ( 67.06698855917106528, 57.83491659372258908, -3.993952884371010814 ) ) ;
#36090=ORIENTED_EDGE ( 'NONE', *, *, #17230, .F. ) ;
#36096=CARTESIAN_POINT ( 'NONE',  ( -59.00110696496997775, 28.68040728033253473, 6.999999999999999112 ) ) ;
#36099=CARTESIAN_POINT ( 'NONE',  ( 81.47505553675507883, 61.46950381087523141, -1.000000000000000000 ) ) ;
#36100=CARTESIAN_POINT ( 'NONE',  ( 79.87286157980665280, 64.75688458792350843, 3.459421039841300338 ) ) ;
#36103=EDGE_LOOP ( 'NONE', ( #18616, #2852, #32496, #36090, #29349, #2610, #14376, #13841, #35604, #32445, #34484, #17518 ) ) ;
#36104=CARTESIAN_POINT ( 'NONE',  ( 79.32401137462355223, 60.77278567581102209, -2.512892981323172847 ) ) ;
#36107=CARTESIAN_POINT ( 'NONE',  ( 81.29907532209045939, 61.38588276545838340, -1.392093260604376326 ) ) ;
#36108=CARTESIAN_POINT ( 'NONE',  ( 78.30161670990426614, 64.30707665991987199, 3.470679136763274553 ) ) ;
#36110=CARTESIAN_POINT ( 'NONE',  ( 81.79239483946132339, 65.43557760269897017, 1.755995906647956240 ) ) ;
#36114=CARTESIAN_POINT ( 'NONE',  ( -62.74554520265134272, 35.90271204080874412, -5.263896983009520802 ) ) ;
#36118=AXIS2_PLACEMENT_3D ( 'NONE', #31410, #28102, #40657 ) ;
#36130=CARTESIAN_POINT ( 'NONE',  ( 66.27376694608996388, 57.73522568913447373, 4.000000000000000000 ) ) ;
#36131=CARTESIAN_POINT ( 'NONE',  ( 71.82805326594559858, 60.58951223549524201, -3.882941974849172695 ) ) ;
#36138=FACE_OUTER_BOUND ( 'NONE', #233, .T. ) ;
#36145=CARTESIAN_POINT ( 'NONE',  ( 80.79830692519209379, 61.67796721187826847, -2.640205493567933992 ) ) ;
#36147=CARTESIAN_POINT ( 'NONE',  ( 80.87649832867062116, 61.25867624111137388, 1.827177995460258941 ) ) ;
#36161=CARTESIAN_POINT ( 'NONE',  ( 80.95462345035979013, 63.09697225074527438, 3.406228740995796311 ) ) ;
#36171=CARTESIAN_POINT ( 'NONE',  ( 67.78936902810559673, 58.13140593263176470, 3.993918888840294557 ) ) ;
#36175=ADVANCED_FACE ( 'NONE', ( #13458 ), #20753, .T. ) ;
#36176=CARTESIAN_POINT ( 'NONE',  ( 80.13254067770888867, 64.54635310605580401, -3.552238747020024512 ) ) ;
#36179=CARTESIAN_POINT ( 'NONE',  ( -58.75407610588014506, 29.59432899155028807, 5.651746018159727214 ) ) ;
#36184=FACE_OUTER_BOUND ( 'NONE', #17449, .T. ) ;
#36185=CARTESIAN_POINT ( 'NONE',  ( 81.09055442218975429, 61.42501475223627949, -1.950029235564217478 ) ) ;
#36187=CARTESIAN_POINT ( 'NONE',  ( 80.93548213101078659, 62.17232332437959030, 2.988136994358705056 ) ) ;
#36202=DIRECTION ( 'NONE',  ( -0.5991095979999732091, 0.2428960078352054019, 0.7629346098860835257 ) ) ;
#36204=CARTESIAN_POINT ( 'NONE',  ( 81.56787793378551044, 61.92707632880442503, 2.226826180281122447 ) ) ;
#36230=B_SPLINE_CURVE_WITH_KNOTS ( 'NONE', 3,
 ( #20389, #14416, #1893, #17093, #1286, #29666, #17290, #13823, #14608, #11519, #26984, #39530, #24086, #23496 ),
 .UNSPECIFIED., .F., .F.,
 ( 4, 2, 2, 2, 2, 2, 4 ),
 ( 0.000000000000000000, 0.0007708628662404179172, 0.001156294299360619612, 0.001541725732480821306, 0.001927157165601023001, 0.002312588598721224912, 0.003083451464961651720 ),
 .UNSPECIFIED. ) ;
#36234=CARTESIAN_POINT ( 'NONE',  ( -57.73493806181993904, 28.75062263012298303, -2.538950603207570378 ) ) ;
#36240=CARTESIAN_POINT ( 'NONE',  ( 82.21693166776705652, 64.09145645796273527, -2.325514254129002367 ) ) ;
#36247=CARTESIAN_POINT ( 'NONE',  ( 74.79578028543750179, 61.54621940999656715, 3.896954863271602232 ) ) ;
#36252=CARTESIAN_POINT ( 'NONE',  ( -1.432293644835494373, -27.47664038617742577, 4.000000000000000000 ) ) ;
#36255=CARTESIAN_POINT ( 'NONE',  ( 81.70897365440946203, 61.83459377731555406, 1.744953761006670989 ) ) ;
#36265=AXIS2_PLACEMENT_3D ( 'NONE', #26956, #11692, #5340 ) ;
#36272=VERTEX_POINT ( 'NONE', #5006 ) ;
#36276=CARTESIAN_POINT ( 'NONE',  ( 67.66003928550829016, 58.48093499090138891, -3.988165415173012374 ) ) ;
#36287=CARTESIAN_POINT ( 'NONE',  ( 79.68852728668518637, 66.33522678087791746, -1.000000000000000000 ) ) ;
#36288=CARTESIAN_POINT ( 'NONE',  ( 81.17684021745370160, 61.76890268566523901, 2.450942308261411018 ) ) ;
#36292=CARTESIAN_POINT ( 'NONE',  ( 78.15185181088403965, 63.91595853815784523, -3.616565173810658784 ) ) ;
#36295=CARTESIAN_POINT ( 'NONE',  ( 81.16204935228429918, 61.30122352005675168, -1.083735637652199602 ) ) ;
#36297=CARTESIAN_POINT ( 'NONE',  ( 79.81867444595899030, 61.24600406626226601, 2.764360460937574260 ) ) ;
#36298=EDGE_LOOP ( 'NONE', ( #13602, #27805, #22554, #23683, #21457, #22076, #3463, #22629, #29649, #31735, #37393, #6422 ) ) ;
#36300=EDGE_CURVE ( 'NONE', #18734, #33979, #3726, .T. ) ;
#36303=CARTESIAN_POINT ( 'NONE',  ( 82.53887461166632988, 63.53329618120201161, 1.555014038482367633 ) ) ;
#36327=CARTESIAN_POINT ( 'NONE',  ( 66.27376694608996388, 57.73522568913447373, 4.000000000000000000 ) ) ;
#36328=CARTESIAN_POINT ( 'NONE',  ( 73.78163614357571021, 59.18917187859454998, -3.552420216828422461 ) ) ;
#36330=ORIENTED_EDGE ( 'NONE', *, *, #16410, .T. ) ;
#36332=CARTESIAN_POINT ( 'NONE',  ( -60.66839582778040807, 24.84364830758653397, 8.800414904976364028 ) ) ;
#36337=CYLINDRICAL_SURFACE ( 'NONE', #27116, 2.500000000000002220 ) ;
#36343=CARTESIAN_POINT ( 'NONE',  ( 78.88927015299483969, 65.04551736973371590, -3.140153738741058298 ) ) ;
#36345=CARTESIAN_POINT ( 'NONE',  ( 79.40660192983034449, 64.44177602733365973, 3.564905221331805762 ) ) ;
#36353=VERTEX_POINT ( 'NONE', #37699 ) ;
#36362=CARTESIAN_POINT ( 'NONE',  ( 80.94524665917968775, 63.44345826879091277, 3.487490852634240301 ) ) ;
#36369=CARTESIAN_POINT ( 'NONE',  ( 67.92345958529671179, 58.66354838738842403, 3.978477839347868361 ) ) ;
#36374=CARTESIAN_POINT ( 'NONE',  ( 79.72815809223409644, 65.03555043453916085, -3.332694751021849200 ) ) ;
#36375=CARTESIAN_POINT ( 'NONE',  ( -62.86576508122317364, 38.67912974266874926, 7.000000000000000000 ) ) ;
#36377=DIRECTION ( 'NONE',  ( -0.000000000000000000, -0.000000000000000000, -1.000000000000000000 ) ) ;
#36379=CARTESIAN_POINT ( 'NONE',  ( -59.61240458878657478, 26.78407864000505612, 6.268956829791734187 ) ) ;
#36383=CARTESIAN_POINT ( 'NONE',  ( 80.77881921633029094, 62.12902493665696824, -3.041370705153006782 ) ) ;
#36385=CARTESIAN_POINT ( 'NONE',  ( 80.57397677244617284, 62.93365480201040896, 3.508091314521097903 ) ) ;
#36390=CARTESIAN_POINT ( 'NONE',  ( 75.14412900705532650, 60.78131343986104440, -3.865308561588337799 ) ) ;
#36405=CARTESIAN_POINT ( 'NONE',  ( 81.06025503659105880, 64.27053461117903055, 3.341858160559717739 ) ) ;
#36410=CARTESIAN_POINT ( 'NONE',  ( -63.70768058868311812, 44.39675795731059793, -1.000000000000000000 ) ) ;
#36419=CIRCLE ( 'NONE', #40431, 2.999999999999998668 ) ;
#36426=DIRECTION ( 'NONE',  ( 0.000000000000000000, 0.000000000000000000, 1.000000000000000000 ) ) ;
#36431=ORIENTED_EDGE ( 'NONE', *, *, #3264, .T. ) ;
#36439=CARTESIAN_POINT ( 'NONE',  ( 81.07719038108439236, 65.78599662769312317, -2.192618372227129520 ) ) ;
#36446=CARTESIAN_POINT ( 'NONE',  ( 75.12771622566773999, 62.30414178837923345, 3.756674307852014394 ) ) ;
#36453=CARTESIAN_POINT ( 'NONE',  ( -64.95171866297671670, 36.28765213650432031, 6.629387290673630417 ) ) ;
#36454=CARTESIAN_POINT ( 'NONE',  ( 81.36794360107712976, 64.82106189941464436, 2.952528780688829624 ) ) ;
#36457=AXIS2_PLACEMENT_3D ( 'NONE', #33654, #15301, #37326 ) ;
#36473=CARTESIAN_POINT ( 'NONE',  ( 66.73816075044196339, 57.82680446425992926, -3.998864354716218816 ) ) ;
#36483=AXIS2_PLACEMENT_3D ( 'NONE', #24365, #36928, #15095 ) ;
#36489=CARTESIAN_POINT ( 'NONE',  ( 82.58199242721477162, 63.55547749749366915, -1.287552078898777541 ) ) ;
#36492=CARTESIAN_POINT ( 'NONE',  ( 81.17805228937325523, 61.98952396227124950, 2.700485128497479792 ) ) ;
#36495=CARTESIAN_POINT ( 'NONE',  ( 78.33250027093576762, 62.86460196216434326, -3.816136337383043475 ) ) ;
#36498=CARTESIAN_POINT ( 'NONE',  ( 81.43301797337205983, 62.09285590259236898, -2.578835243349320461 ) ) ;
#36499=CARTESIAN_POINT ( 'NONE',  ( 79.06939945841558881, 62.09164075111542758, 3.616565173810706746 ) ) ;
#36502=CARTESIAN_POINT ( 'NONE',  ( 78.69012442119817763, 66.05840891509440382, 1.017094602978567242 ) ) ;
#36528=CARTESIAN_POINT ( 'NONE',  ( 66.57374945270225908, 57.82325632336715415, 3.999874661881728688 ) ) ;
#36529=CARTESIAN_POINT ( 'NONE',  ( 72.85835069609119330, 61.31913755009141909, -3.785151435630688788 ) ) ;
#36536=DIRECTION ( 'NONE',  ( -0.9267318687906771491, 0.3757233601570964532, 0.000000000000000000 ) ) ;
#36540=DIRECTION ( 'NONE',  ( -0.000000000000000000, 0.000000000000000000, 1.000000000000000000 ) ) ;
#36543=CARTESIAN_POINT ( 'NONE',  ( 80.61353453797053703, 61.63497835834534300, -2.716276829189519404 ) ) ;
#36545=CARTESIAN_POINT ( 'NONE',  ( 78.38646849266343963, 65.84297019793960715, 1.584170212883424300 ) ) ;
#36548=DIRECTION ( 'NONE',  ( -0.8831583674550994578, 0.4690749385695672791, 0.000000000000000000 ) ) ;
#36567=CARTESIAN_POINT ( 'NONE',  ( 68.07944445521805221, 58.24657026194513776, 3.992939643064506328 ) ) ;
#36571=CARTESIAN_POINT ( 'NONE',  ( 81.16957891225059996, 61.30398062001309256, -1.000000000000000000 ) ) ;
#36579=CARTESIAN_POINT ( 'NONE',  ( -58.64967482348268391, 27.97946873212458030, 5.671478272894446171 ) ) ;
#36588=CARTESIAN_POINT ( 'NONE',  ( 78.64443580140851964, 65.97314938607593149, -1.660510093083306105 ) ) ;
#36590=CARTESIAN_POINT ( 'NONE',  ( 80.69932603693817441, 62.65430898200613541, 3.392181771880192098 ) ) ;
#36594=CARTESIAN_POINT ( 'NONE',  ( 73.28665133690081745, 61.87344754340890063, -3.624554307483654814 ) ) ;
#36607=CARTESIAN_POINT ( 'NONE',  ( 81.47197553453356988, 61.72158698297663193, 1.969816429103234290 ) ) ;
#36622=CARTESIAN_POINT ( 'NONE',  ( 80.80706632665068412, 63.75484916101672894, -3.549391953833849644 ) ) ;
#36627=CIRCLE ( 'NONE', #39920, 5.329987104167474676 ) ;
#36633=EDGE_CURVE ( 'NONE', #17865, #31330, #6353, .T. ) ;
#36634=ORIENTED_EDGE ( 'NONE', *, *, #386, .F. ) ;
#36636=CARTESIAN_POINT ( 'NONE',  ( 81.15397050155254988, 61.44050475792813160, -1.896863055073852111 ) ) ;
#36637=FACE_OUTER_BOUND ( 'NONE', #17168, .T. ) ;
#36641=ORIENTED_EDGE ( 'NONE', *, *, #4069, .F. ) ;
#36643=CARTESIAN_POINT ( 'NONE',  ( 78.95874065903551298, 66.19121013986814717, -1.203271478923241933 ) ) ;
#36649=CARTESIAN_POINT ( 'NONE',  ( 75.72894860151858154, 61.00966332974834927, 3.846775394605490561 ) ) ;
#36655=CARTESIAN_POINT ( 'NONE',  ( -67.80647484265466574, 37.44505118619654382, 9.800414904977209574 ) ) ;
#36656=CARTESIAN_POINT ( 'NONE',  ( 81.38476203741942072, 61.42515712988158327, 1.285939662725141597 ) ) ;
#36662=CARTESIAN_POINT ( 'NONE',  ( -75.45330471031414277, 33.71485196875532608, 9.800414904976365804 ) ) ;
#36667=DIRECTION ( 'NONE',  ( -1.000000000000000000, 0.000000000000000000, 0.000000000000000000 ) ) ;
#36672=CARTESIAN_POINT ( 'NONE',  ( 67.02270721038308920, 57.95726884087558517, -3.999016414675010900 ) ) ;
#36679=CARTESIAN_POINT ( 'NONE',  ( 73.32807694493881456, 62.33902570990260017, 3.356114863723819397 ) ) ;
#36689=CARTESIAN_POINT ( 'NONE',  ( 82.56222392620334460, 63.90769089702597228, -1.153249692834613427 ) ) ;
#36690=CARTESIAN_POINT ( 'NONE',  ( 78.96442931663766274, 65.90663607296401949, 2.147349935851028846 ) ) ;
#36693=CARTESIAN_POINT ( 'NONE',  ( 78.95981124517786043, 62.31610944509169769, -3.691425412862293420 ) ) ;
#36696=CARTESIAN_POINT ( 'NONE',  ( 81.36421798834938102, 61.51166984027132401, -1.726519205788531242 ) ) ;
#36697=CARTESIAN_POINT ( 'NONE',  ( 79.79883522896109582, 62.08831372790999126, 3.424416364708440241 ) ) ;
#36700=CARTESIAN_POINT ( 'NONE',  ( 78.69027363540493525, 66.05851491966868139, 1.011532654301222633 ) ) ;
#36710=FACE_OUTER_BOUND ( 'NONE', #32720, .T. ) ;
#36711=DIRECTION ( 'NONE',  ( -1.000000000000000000, 0.000000000000000000, 0.000000000000000000 ) ) ;
#36719=DIRECTION ( 'NONE',  ( 0.000000000000000000, 0.000000000000000000, 1.000000000000000000 ) ) ;
#36727=CARTESIAN_POINT ( 'NONE',  ( 66.27376694608996388, 57.73522568913447373, 4.000000000000000000 ) ) ;
#36728=CARTESIAN_POINT ( 'NONE',  ( 69.09457860630368486, 59.08023000801873081, -3.976370928559271878 ) ) ;
#36742=CARTESIAN_POINT ( 'NONE',  ( 78.65807594933866653, 65.42150623161261080, -2.716276829189491426 ) ) ;
#36744=CARTESIAN_POINT ( 'NONE',  ( 79.14825301983924533, 66.20254961713403929, -1.551099981298400099 ) ) ;
#36745=CARTESIAN_POINT ( 'NONE',  ( 79.65304550238739978, 63.88563316389422653, 3.730195463674649936 ) ) ;
#36748=EDGE_CURVE ( 'NONE', #9255, #8555, #1311, .T. ) ;
#36758=CARTESIAN_POINT ( 'NONE',  ( -68.98442902999595105, 21.93515443114010210, -9.800414904976365804 ) ) ;
#36772=CARTESIAN_POINT ( 'NONE',  ( 67.74957807481123950, 58.23899230517488235, 3.997461085607396214 ) ) ;
#36785=CIRCLE ( 'NONE', #35493, 1.000000000000000000 ) ;
#36786=ORIENTED_EDGE ( 'NONE', *, *, #3623, .F. ) ;
#36787=CARTESIAN_POINT ( 'NONE',  ( 78.69071029820845808, 65.87362605733925136, -2.012706562768929786 ) ) ;
#36789=CARTESIAN_POINT ( 'NONE',  ( 79.79930721375697544, 64.34646279424478621, 3.632888195267895970 ) ) ;
#36794=CARTESIAN_POINT ( 'NONE',  ( 73.74018914705078487, 60.85874216252894087, -3.935025356190109402 ) ) ;
#36799=CARTESIAN_POINT ( 'NONE',  ( 78.69038500580381879, 66.05859403932473128, 1.000000000000000000 ) ) ;
#36809=CARTESIAN_POINT ( 'NONE',  ( 78.68070521837705655, 66.05171761244719164, 1.104694797982982646 ) ) ;
#36812=VERTEX_POINT ( 'NONE', #30490 ) ;
#36818=CARTESIAN_POINT ( 'NONE',  ( -67.80647484265035985, 37.44505118619480299, -9.800414904974669383 ) ) ;
#36821=ORIENTED_EDGE ( 'NONE', *, *, #21307, .F. ) ;
#36828=CARTESIAN_POINT ( 'NONE',  ( 79.76270496343316552, 65.40180735727545880, -3.071811904357681478 ) ) ;
#36839=CARTESIAN_POINT ( 'NONE',  ( 80.15412116699830847, 64.17350884197745131, -3.654032574946330936 ) ) ;
#36844=CARTESIAN_POINT ( 'NONE',  ( 81.97757951650689279, 62.12693032551443650, -1.780213741554919071 ) ) ;
#36852=CARTESIAN_POINT ( 'NONE',  ( 74.30428547378053850, 61.12304205247700395, 3.924711207976832927 ) ) ;
#36859=CARTESIAN_POINT ( 'NONE',  ( 80.51660522894113114, 65.82269567859336235, 2.502189764415794659 ) ) ;
#36863=EDGE_CURVE ( 'NONE', #33979, #28588, #1103, .T. ) ;
#36869=ADVANCED_FACE ( 'NONE', ( #16007 ), #34975, .T. ) ;
#36876=CIRCLE ( 'NONE', #26369, 2.999999999999998668 ) ;
#36880=DIRECTION ( 'NONE',  ( -1.000000000000000000, 5.204170427930426016E-15, 0.000000000000000000 ) ) ;
#36882=EDGE_LOOP ( 'NONE', ( #10515, #34497, #3917, #18831, #20150 ) ) ;
#36895=CARTESIAN_POINT ( 'NONE',  ( 81.34501148009302085, 65.92776879248947353, -1.287552078898777541 ) ) ;
#36896=CARTESIAN_POINT ( 'NONE',  ( 79.95371652093496095, 64.44169929929478258, 3.600689860192761493 ) ) ;
#36899=CARTESIAN_POINT ( 'NONE',  ( 77.99575034756949776, 63.53025565730433044, -3.710351296122899711 ) ) ;
#36903=CARTESIAN_POINT ( 'NONE',  ( 81.51669253446031860, 62.40826230823314091, -2.731335034813053841 ) ) ;
#36904=CARTESIAN_POINT ( 'NONE',  ( 77.93772202372291247, 64.31926776197541074, 3.361664161258280270 ) ) ;
#36908=CARTESIAN_POINT ( 'NONE',  ( 82.56043351944062181, 63.54438683934786525, 1.421283058690022916 ) ) ;
#36928=DIRECTION ( 'NONE',  ( -0.000000000000000000, -0.000000000000000000, 1.000000000000000000 ) ) ;
#36933=CARTESIAN_POINT ( 'NONE',  ( 69.62738871241069205, 59.42086865771531023, -3.954846139149833739 ) ) ;
#36950=CARTESIAN_POINT ( 'NONE',  ( 78.96152850399714396, 65.10675657659959370, -3.115013800517339781 ) ) ;
#36952=CARTESIAN_POINT ( 'NONE',  ( 81.16644189562721579, 61.30283181452514185, -1.054034669008006908 ) ) ;
#36953=CARTESIAN_POINT ( 'NONE',  ( 80.07543224467224263, 63.05907417235837187, 3.676305632669317536 ) ) ;
#36971=TOROIDAL_SURFACE ( 'NONE', #10654, 80.68529983683480111, 3.000000000000000000 ) ;
#36976=CARTESIAN_POINT ( 'NONE',  ( 67.21949607617069944, 57.87245792367627928, 3.992323350375291291 ) ) ;
#36989=CARTESIAN_POINT ( 'NONE',  ( 80.86726794284579967, 61.90233618827342355, -2.830664096605172819 ) ) ;
#36990=B_SPLINE_CURVE_WITH_KNOTS ( 'NONE', 3,
 ( #30662, #21799, #37020, #34376, #33963, #27348 ),
 .UNSPECIFIED., .F., .F.,
 ( 4, 2, 4 ),
 ( 7.235985768044570246E-16, 0.0008525552902386053511, 0.001705110580476487106 ),
 .UNSPECIFIED. ) ;
#36993=CARTESIAN_POINT ( 'NONE',  ( 78.74908976354480217, 65.92676629176590097, 1.950029235564084029 ) ) ;
#36998=CARTESIAN_POINT ( 'NONE',  ( 73.68135292868622344, 60.99150118422435440, -3.923277237825057551 ) ) ;
#37009=CARTESIAN_POINT ( 'NONE',  ( 81.34308989085656094, 63.28542802927127298, 3.228380831072418466 ) ) ;
#37020=CARTESIAN_POINT ( 'NONE',  ( -62.96427906878896152, 37.71115934643970036, 4.137654479799069307 ) ) ;
#37025=CARTESIAN_POINT ( 'NONE',  ( 78.90480995596030311, 66.05426212177786738, -1.786209778413372362 ) ) ;
#37030=ORIENTED_EDGE ( 'NONE', *, *, #15251, .F. ) ;
#37036=CARTESIAN_POINT ( 'NONE',  ( 81.11661571137584303, 61.75122346557050435, -2.482170738714639668 ) ) ;
#37037=CARTESIAN_POINT ( 'NONE',  ( -59.64698295252583193, 26.74637988513382325, -7.056669117542212710 ) ) ;
#37044=CARTESIAN_POINT ( 'NONE',  ( 82.12703758395426235, 64.04502942998703929, -2.474249079299298604 ) ) ;
#37050=CARTESIAN_POINT ( 'NONE',  ( 72.75889805100318597, 61.54370698478812329, 3.677837812371882897 ) ) ;
#37056=CARTESIAN_POINT ( 'NONE',  ( -64.55204904897829010, 36.12561474966002351, 8.218049716822161344 ) ) ;
#37057=CARTESIAN_POINT ( 'NONE',  ( 81.35720881915661096, 61.41209416231797036, 1.323744132979554511 ) ) ;
#37061=CARTESIAN_POINT ( 'NONE',  ( -81.07947155388369254, 30.81399289130168384, -12.49999999999999645 ) ) ;
#37074=CARTESIAN_POINT ( 'NONE',  ( 66.89278707744533392, 57.85779714042387667, -3.998112125421894980 ) ) ;
#37091=CARTESIAN_POINT ( 'NONE',  ( 82.55792188592127445, 63.20960171500892955, -1.133121492189030244 ) ) ;
#37092=CARTESIAN_POINT ( 'NONE',  ( 79.62856576210180037, 64.96968976106111882, 3.364061116559610820 ) ) ;
#37097=CARTESIAN_POINT ( 'NONE',  ( 75.74534653887742763, 63.84344576921726144, -2.970791854430509193 ) ) ;
#37101=CARTESIAN_POINT ( 'NONE',  ( 80.00444560210259226, 65.54189868874054525, -2.943961322783052559 ) ) ;
#37102=CARTESIAN_POINT ( 'NONE',  ( 77.32551012344487162, 64.79183443757982275, 2.725046208697037287 ) ) ;
#37106=CARTESIAN_POINT ( 'NONE',  ( 82.39441792515161467, 64.18328374515915868, 1.882325606868446854 ) ) ;
#37113=CARTESIAN_POINT ( 'NONE',  ( -62.96789184025029584, 35.54107112332057028, 6.131023528871422101 ) ) ;
#37132=CARTESIAN_POINT ( 'NONE',  ( 70.57032280423491954, 60.39816359117256184, -3.808711916423200616 ) ) ;
#37149=CARTESIAN_POINT ( 'NONE',  ( 78.46701299008461206, 65.82614401021746176, -1.855758959884432402 ) ) ;
#37150=CARTESIAN_POINT ( 'NONE',  ( 81.77617677873419666, 62.02699640077094045, -2.046910133536480991 ) ) ;
#37151=CARTESIAN_POINT ( 'NONE',  ( 80.79577214038279465, 61.23497056275884631, 1.884339924308601644 ) ) ;
#37163=DIRECTION ( 'NONE',  ( -0.000000000000000000, 0.000000000000000000, 1.000000000000000000 ) ) ;
#37175=ORIENTED_EDGE ( 'NONE', *, *, #3392, .T. ) ;
#37176=CARTESIAN_POINT ( 'NONE',  ( 67.11883677231543288, 58.14904800069622581, 3.997022163556061436 ) ) ;
#37192=CARTESIAN_POINT ( 'NONE',  ( 78.58771539371637971, 65.98568759316003707, -1.340350474428867678 ) ) ;
#37194=CARTESIAN_POINT ( 'NONE',  ( 78.91366476310541600, 65.65666373793331445, 2.561782662428539581 ) ) ;
#37196=ORIENTED_EDGE ( 'NONE', *, *, #24072, .T. ) ;
#37198=CARTESIAN_POINT ( 'NONE',  ( 73.64914076101801754, 62.55656703988326939, -3.294766324886513775 ) ) ;
#37211=CARTESIAN_POINT ( 'NONE',  ( 79.29849762269611801, 65.95036606079995067, 2.316472630215894224 ) ) ;
#37222=CARTESIAN_POINT ( 'NONE',  ( -68.71186372058384961, 37.81212149306785619, -8.800414904976365804 ) ) ;
#37227=ORIENTED_EDGE ( 'NONE', *, *, #4212, .T. ) ;
#37228=CARTESIAN_POINT ( 'NONE',  ( 81.34759249528946157, 61.83023590116508217, -2.361823859647550261 ) ) ;
#37230=CARTESIAN_POINT ( 'NONE',  ( 35.94200923520244828, 151.3264224549853907, -4.000000000000000000 ) ) ;
#37240=CARTESIAN_POINT ( 'NONE',  ( 79.49612969957790654, 65.22981380272332785, -3.178394274514608320 ) ) ;
#37248=CARTESIAN_POINT ( 'NONE',  ( 81.60288604192454898, 64.55353989381943336, -2.864610283900680621 ) ) ;
#37255=CARTESIAN_POINT ( 'NONE',  ( 73.43932658456094487, 59.98824119151031198, 3.894134109119617104 ) ) ;
#37262=CARTESIAN_POINT ( 'NONE',  ( 78.68665600826857087, 66.05594492867547274, 1.065084354002954425 ) ) ;
#37264=DIRECTION ( 'NONE',  ( -1.000000000000000000, 0.000000000000000000, 0.000000000000000000 ) ) ;
#37284=CARTESIAN_POINT ( 'NONE',  ( 67.00793363329040631, 57.99808316372624972, -3.999354069328931782 ) ) ;
#37285=ADVANCED_FACE ( 'NONE', ( #12093 ), #14993, .F. ) ;
#37295=CARTESIAN_POINT ( 'NONE',  ( 82.52664026313777867, 63.88931701666344765, -1.444831904610020645 ) ) ;
#37296=CARTESIAN_POINT ( 'NONE',  ( 78.71191388991731230, 66.03048852543453506, 1.560659576774504398 ) ) ;
#37299=CARTESIAN_POINT ( 'NONE',  ( 77.00710955723606332, 62.69977232050459293, -3.829716617887276353 ) ) ;
#37303=CARTESIAN_POINT ( 'NONE',  ( 80.21610222778852517, 65.32174013293554538, -3.113722587672208331 ) ) ;
#37304=CARTESIAN_POINT ( 'NONE',  ( 79.04999676712186840, 61.38304106620129375, 3.266768353517085721 ) ) ;
#37308=CARTESIAN_POINT ( 'NONE',  ( -58.49108653198740626, 30.52987238301787443, 5.010559264471326379 ) ) ;
#37309=CARTESIAN_POINT ( 'NONE',  ( 81.45638069295017658, 61.46019730367517298, 1.134074597586613109 ) ) ;
#37310=CARTESIAN_POINT ( 'NONE',  ( -64.08758708074094557, 42.98467135106749737, 2.320054399416036084 ) ) ;
#37315=CARTESIAN_POINT ( 'NONE',  ( -64.12639773666754195, 35.29406715003009509, 4.430479139283200141 ) ) ;
#37317=ADVANCED_FACE ( 'NONE', ( #18479 ), #37979, .T. ) ;
#37320=CARTESIAN_POINT ( 'NONE',  ( 79.42168399090624575, 60.69064003064117685, 2.270986553420443421 ) ) ;
#37321=EDGE_CURVE ( 'NONE', #3549, #16760, #11601, .T. ) ;
#37326=DIRECTION ( 'NONE',  ( -1.000000000000000000, 0.000000000000000000, 0.000000000000000000 ) ) ;
#37327=CARTESIAN_POINT ( 'NONE',  ( -68.98442902999595105, 21.93515443114010210, 9.800414904976365804 ) ) ;
#37331=CARTESIAN_POINT ( 'NONE',  ( -64.08758708074091714, 38.27681294191128103, -4.090925416971892936 ) ) ;
#37338=CARTESIAN_POINT ( 'NONE',  ( 69.01369661159887414, 59.28919897632942337, -3.943722715026729109 ) ) ;
#37345=VERTEX_POINT ( 'NONE', #31271 ) ;
#37350=CARTESIAN_POINT ( 'NONE',  ( 79.63188232868596117, 63.19436791590091218, -3.756013696796379531 ) ) ;
#37352=CARTESIAN_POINT ( 'NONE',  ( 81.68586513309662678, 63.81782706255989268, -3.019849704269077506 ) ) ;
#37353=CARTESIAN_POINT ( 'NONE',  ( 79.80332398823145468, 63.27387486779120707, 3.741985197832889742 ) ) ;
#37355=CARTESIAN_POINT ( 'NONE',  ( -64.08758708074093136, 38.27681294190824701, 4.090925416972713613 ) ) ;
#37363=CARTESIAN_POINT ( 'NONE',  ( -74.03402466285142225, 19.33157623370700406, 8.800414904976364028 ) ) ;
#37378=EDGE_CURVE ( 'NONE', #20345, #15467, #28582, .T. ) ;
#37379=CIRCLE ( 'NONE', #40024, 1.000000000000000888 ) ;
#37381=ORIENTED_EDGE ( 'NONE', *, *, #10372, .F. ) ;
#37383=CARTESIAN_POINT ( 'NONE',  ( 67.52644525400921793, 57.94193659033309274, 3.989212576213369221 ) ) ;
#37393=ORIENTED_EDGE ( 'NONE', *, *, #34021, .T. ) ;
#37397=CARTESIAN_POINT ( 'NONE',  ( 80.95177907874115419, 61.22464621339461388, -1.448968528258131716 ) ) ;
#37398=CARTESIAN_POINT ( 'NONE',  ( 80.54480326438822146, 62.60292565479354465, 3.426353657592656976 ) ) ;
#37401=CARTESIAN_POINT ( 'NONE',  ( -58.05693936349092610, 29.90851024391614388, 4.510341912063071668 ) ) ;
#37405=CARTESIAN_POINT ( 'NONE',  ( -55.02840665537740961, 31.32676418781088401, 1.332930532353302278 ) ) ;
#37412=CARTESIAN_POINT ( 'NONE',  ( 81.36421798834848573, 61.51166984027109663, 1.726519205789175171 ) ) ;
#37416=CARTESIAN_POINT ( 'NONE',  ( -64.71588209753996068, 34.74121984326603041, -6.231007222294328685 ) ) ;
#37429=CARTESIAN_POINT ( 'NONE',  ( 79.58096101840204994, 65.58481148403340910, -2.850064543546721119 ) ) ;
#37437=CARTESIAN_POINT ( 'NONE',  ( 80.65725571609037559, 62.96675706018874052, -3.489836119548947568 ) ) ;
#37440=ADVANCED_FACE ( 'NONE', ( #16603 ), #3784, .T. ) ;
#37444=CARTESIAN_POINT ( 'NONE',  ( 81.76431320972366734, 64.63772642544184066, -2.665107514501070085 ) ) ;
#37452=CARTESIAN_POINT ( 'NONE',  ( 74.49653936242856389, 60.69398666642196360, 3.911020515999844793 ) ) ;
#37461=CARTESIAN_POINT ( 'NONE',  ( 81.10335266982619373, 65.07249684831462844, 2.967158453528945028 ) ) ;
#37479=CARTESIAN_POINT ( 'NONE',  ( 66.57570644833764106, 57.81776741001107922, -3.999845987728086083 ) ) ;
#37483=CARTESIAN_POINT ( 'NONE',  ( -56.11355572853776863, 30.33753280151826104, 1.575778306538802465 ) ) ;
#37486=CARTESIAN_POINT ( 'NONE',  ( -68.98442902999595105, 21.93515443114010210, -46.17089178453873188 ) ) ;
#37491=CARTESIAN_POINT ( 'NONE',  ( 82.33093480182111534, 62.53300266214100134, -1.299258709309398352 ) ) ;
#37492=CARTESIAN_POINT ( 'NONE',  ( 80.99158576241019603, 62.18982880056436358, 2.968223699503258484 ) ) ;
#37495=CARTESIAN_POINT ( 'NONE',  ( 76.90305707343897268, 64.27659990673319612, -3.054665556626403600 ) ) ;
#37499=EDGE_CURVE ( 'NONE', #34454, #6217, #2456, .T. ) ;
#37501=CARTESIAN_POINT ( 'NONE',  ( 79.10630237408686583, 66.00617110148429845, -2.043563575549270706 ) ) ;
#37502=CARTESIAN_POINT ( 'NONE',  ( 76.90305707343897268, 64.27659990673319612, 3.054665556626398271 ) ) ;
#37508=CARTESIAN_POINT ( 'NONE',  ( 82.35700292606965434, 63.80179554273364317, 2.078018481492982517 ) ) ;
#37514=CARTESIAN_POINT ( 'NONE',  ( -63.15778550246167811, 35.55392038829433687, 6.471101796986872934 ) ) ;
#37517=FACE_OUTER_BOUND ( 'NONE', #17457, .T. ) ;
#37522=CARTESIAN_POINT ( 'NONE',  ( 79.11842553801511713, 60.58988033035119969, -2.372312511143319647 ) ) ;
#37533=CARTESIAN_POINT ( 'NONE',  ( 69.25747553239096987, 58.65839085985714974, -3.984982412582168010 ) ) ;
#37548=CARTESIAN_POINT ( 'NONE',  ( 79.95886636011078963, 62.14075979114825543, -3.401284978681017535 ) ) ;
#37551=CARTESIAN_POINT ( 'NONE',  ( 80.35914242818640219, 65.73759417665644378, -2.670779692148392392 ) ) ;
#37552=CARTESIAN_POINT ( 'NONE',  ( 78.56734957671525876, 65.55328818492539256, 2.456741006817813933 ) ) ;
#37555=CARTESIAN_POINT ( 'NONE',  ( 82.53033050081238287, 64.25366301186838314, 1.000000000000000000 ) ) ;
#37562=LINE ( 'NONE', #2613, #22835 ) ;
#37563=ORIENTED_EDGE ( 'NONE', *, *, #29288, .F. ) ;
#37564=CARTESIAN_POINT ( 'NONE',  ( -72.95330471031414277, 33.71485196875532608, 8.800414904976364028 ) ) ;
#37567=FACE_OUTER_BOUND ( 'NONE', #3629, .T. ) ;
#37568=DIRECTION ( 'NONE',  ( 0.000000000000000000, 0.000000000000000000, -1.000000000000000000 ) ) ;
#37575=CARTESIAN_POINT ( 'NONE',  ( -2.954197855305039422, -12.43481156997016157, 4.000000000000000000 ) ) ;
#37578=CARTESIAN_POINT ( 'NONE',  ( 67.48690106321139126, 58.04989387035797677, 3.996173465816880377 ) ) ;
#37593=CARTESIAN_POINT ( 'NONE',  ( 78.52594532581821341, 65.94185624388910583, -1.429680343939077281 ) ) ;
#37595=CARTESIAN_POINT ( 'NONE',  ( 80.94504091708289195, 61.55080574620870948, 2.311104455577556394 ) ) ;
#37597=ORIENTED_EDGE ( 'NONE', *, *, #14333, .T. ) ;
#37602=CARTESIAN_POINT ( 'NONE',  ( -64.08758708074093136, 38.27681294191129524, -4.090925416971890272 ) ) ;
#37611=CARTESIAN_POINT ( 'NONE',  ( 80.13372729537762496, 65.27601544180656390, 3.162824939346259523 ) ) ;
#37625=CARTESIAN_POINT ( 'NONE',  ( 81.14373266700285114, 62.24431303712577090, -2.911438267503734689 ) ) ;
#37635=CARTESIAN_POINT ( 'NONE',  ( 80.74944977059911366, 62.67191958473371471, -3.380189700376618589 ) ) ;
#37641=ADVANCED_FACE ( 'NONE', ( #27657 ), #367, .T. ) ;
#37648=CARTESIAN_POINT ( 'NONE',  ( 73.79885669521775071, 60.72590704978823339, 3.935025356184053802 ) ) ;
#37654=CARTESIAN_POINT ( 'NONE',  ( -58.88301977763249795, 29.11298994408642571, -6.074305062359572460 ) ) ;
#37656=CARTESIAN_POINT ( 'NONE',  ( -55.16612787639762416, 31.23053227951969646, -1.484562114140327793 ) ) ;
#37657=CARTESIAN_POINT ( 'NONE',  ( 81.53193199008826753, 61.58838919619023500, 1.571309534768038141 ) ) ;
#37661=CARTESIAN_POINT ( 'NONE',  ( -63.08758708074093136, 38.13199975834322686, 3.043809435734686986 ) ) ;
#37662=ORIENTED_EDGE ( 'NONE', *, *, #7134, .T. ) ;
#37670=ORIENTED_EDGE ( 'NONE', *, *, #32608, .T. ) ;
#37674=CARTESIAN_POINT ( 'NONE',  ( 66.56983546066652480, 57.83423415266778278, -3.999917672784519596 ) ) ;
#37687=CARTESIAN_POINT ( 'NONE',  ( 82.46885687451847957, 64.22182207139027810, -1.617049763656951411 ) ) ;
#37688=CARTESIAN_POINT ( 'NONE',  ( 81.18585152890854317, 61.61024096112966220, 2.156541836018581293 ) ) ;
#37692=CARTESIAN_POINT ( 'NONE',  ( 76.82516749139865908, 64.42394039557471785, -2.889099817377081880 ) ) ;
#37696=CARTESIAN_POINT ( 'NONE',  ( 78.80232334588868071, 66.09893194982532805, -1.428845309148525589 ) ) ;
#37697=CARTESIAN_POINT ( 'NONE',  ( 77.06776432268850385, 63.96223838934589168, 3.363831406679905101 ) ) ;
#37699=CARTESIAN_POINT ( 'NONE',  ( -59.93345510331042902, 24.73247967741478703, 9.800414904976365804 ) ) ;
#37702=CARTESIAN_POINT ( 'NONE',  ( 82.31416527841567188, 64.14174473599682358, 2.134985007309428973 ) ) ;
#37708=CARTESIAN_POINT ( 'NONE',  ( -62.87442376950010470, 35.57781650258885975, 5.904453864323423673 ) ) ;
#37715=CARTESIAN_POINT ( 'NONE',  ( 81.06637268519124007, 61.26626587534826740, -1.317877730053106378 ) ) ;
#37728=CARTESIAN_POINT ( 'NONE',  ( 68.11537257328342321, 58.15040817571434673, -3.985705108533861729 ) ) ;
#37733=DIRECTION ( 'NONE',  ( 0.000000000000000000, 0.000000000000000000, 1.000000000000000000 ) ) ;
#37738=ORIENTED_EDGE ( 'NONE', *, *, #35684, .F. ) ;
#37747=CARTESIAN_POINT ( 'NONE',  ( 79.47890774847340367, 63.12292952392867562, -3.765547211956735030 ) ) ;
#37750=CARTESIAN_POINT ( 'NONE',  ( 80.60418185334548014, 65.53338749785481809, -2.819252638153959101 ) ) ;
#37751=CARTESIAN_POINT ( 'NONE',  ( 78.65807594933866653, 65.42150623161261080, 2.716276829189492314 ) ) ;
#37752=CARTESIAN_POINT ( 'NONE',  ( 81.96779975749585390, 61.96402392828839822, 1.000000000000000000 ) ) ;
#37770=DIRECTION ( 'NONE',  ( 0.000000000000000000, 0.000000000000000000, 1.000000000000000000 ) ) ;
#37779=CARTESIAN_POINT ( 'NONE',  ( 67.47898117768387749, 58.07151159967423126, 3.997009152755514272 ) ) ;
#37787=DIRECTION ( 'NONE',  ( 0.4582725098355734938, -0.8888117386314180468, 0.000000000000000000 ) ) ;
#37797=CARTESIAN_POINT ( 'NONE',  ( 80.29143557890645866, 63.14717164025322660, -3.649417990092601372 ) ) ;
#37800=CARTESIAN_POINT ( 'NONE',  ( 80.18433095895142060, 63.45046554133028138, 3.702313260098204495 ) ) ;
#37805=CARTESIAN_POINT ( 'NONE',  ( -63.03213158086148837, 38.26878225442762016, -4.032857076800600460 ) ) ;
#37807=CARTESIAN_POINT ( 'NONE',  ( -54.80986203264403400, 31.50205531805574211, 1.053352963064339898 ) ) ;
#37811=ORIENTED_EDGE ( 'NONE', *, *, #37499, .T. ) ;
#37813=CARTESIAN_POINT ( 'NONE',  ( -67.16566696069978093, 37.18524951245930055, 8.491446490665028435 ) ) ;
#37816=CARTESIAN_POINT ( 'NONE',  ( 78.67345636894508232, 66.04656848779337963, 1.137963815189256600 ) ) ;
#37820=CARTESIAN_POINT ( 'NONE',  ( -64.28450485721612040, 34.79050374529649758, -5.196496127070091120 ) ) ;
#37823=ORIENTED_EDGE ( 'NONE', *, *, #9436, .T. ) ;
#37837=CARTESIAN_POINT ( 'NONE',  ( 81.27646189173411528, 61.63998710316791829, -2.098997056522961646 ) ) ;
#37844=ORIENTED_EDGE ( 'NONE', *, *, #21627, .T. ) ;
#37845=ORIENTED_EDGE ( 'NONE', *, *, #39361, .F. ) ;
#37846=CARTESIAN_POINT ( 'NONE',  ( 81.09181894009961411, 61.27555711777438319, -1.268354304253237697 ) ) ;
#37852=CARTESIAN_POINT ( 'NONE',  ( 80.84167751523406764, 65.66068717198510285, -2.558871340112543358 ) ) ;
#37859=CARTESIAN_POINT ( 'NONE',  ( -63.08758708074093136, 41.04287353446839148, -4.000000000000000000 ) ) ;
#37860=CARTESIAN_POINT ( 'NONE',  ( 71.66251436080506210, 60.98061884659115606, 3.745173303738185577 ) ) ;
#37869=CARTESIAN_POINT ( 'NONE',  ( 81.74240050578451644, 63.84683571418597836, 2.967158453528944140 ) ) ;
#37878=EDGE_CURVE ( 'NONE', #7222, #38011, #34406, .T. ) ;
#37889=CARTESIAN_POINT ( 'NONE',  ( 66.54635149611212341, 57.90010100995254305, -3.999344142520906864 ) ) ;
#37890=AXIS2_PLACEMENT_3D ( 'NONE', #23876, #4958, #30077 ) ;
#37891=EDGE_LOOP ( 'NONE', ( #21619, #20361, #22639, #978, #37738 ) ) ;
#37900=CARTESIAN_POINT ( 'NONE',  ( 81.32357852907298934, 65.91643957835144363, -1.421283058691077850 ) ) ;
#37901=CARTESIAN_POINT ( 'NONE',  ( 80.17861389908809144, 63.81053541282458497, 3.679799701112133281 ) ) ;
#37905=CARTESIAN_POINT ( 'NONE',  ( 76.19453532209955426, 64.30418437363987039, -2.661196496273629641 ) ) ;
#37909=CARTESIAN_POINT ( 'NONE',  ( 79.27186652256901311, 65.93364065454107958, -2.332991218130509026 ) ) ;
#37910=CARTESIAN_POINT ( 'NONE',  ( 77.40632518803428752, 64.64540924511487674, 2.913524936156969058 ) ) ;
#37915=CARTESIAN_POINT ( 'NONE',  ( 81.96987370863080002, 65.13652322159784092, 1.905332024690495007 ) ) ;
#37923=CARTESIAN_POINT ( 'NONE',  ( -64.26379470914699255, 34.82012742686826101, 5.122105205699089225 ) ) ;
#37927=CARTESIAN_POINT ( 'NONE',  ( 81.16957891225065680, 61.30398062001311388, 1.085775560726838895 ) ) ;
#37929=CARTESIAN_POINT ( 'NONE',  ( 81.16957891225065680, 61.30398062001312809, -1.085786403289926261 ) ) ;
#37940=CARTESIAN_POINT ( 'NONE',  ( 68.10340323693496600, 58.18244674706191688, -3.988335407916729025 ) ) ;
#37951=DIRECTION ( 'NONE',  ( 0.000000000000000000, 1.000000000000000000, 0.000000000000000000 ) ) ;
#37952=CARTESIAN_POINT ( 'NONE',  ( 81.19854122754009040, 61.34870327520654598, 1.508787936435544541 ) ) ;
#37955=ORIENTED_EDGE ( 'NONE', *, *, #7895, .F. ) ;
#37956=CARTESIAN_POINT ( 'NONE',  ( 79.22522514097650514, 63.97890519848277791, -3.707164540951486398 ) ) ;
#37959=CARTESIAN_POINT ( 'NONE',  ( 81.04289631910501157, 64.65011820514618535, -3.243459512787966403 ) ) ;
#37961=CARTESIAN_POINT ( 'NONE',  ( 78.37355578220726215, 65.75145430471653185, 1.935054690158702684 ) ) ;
#37971=ADVANCED_FACE ( 'NONE', ( #9248 ), #8255, .T. ) ;
#37979=( BOUNDED_SURFACE ( )  B_SPLINE_SURFACE ( 3, 2, ( 
 ( #2252, #31066, #11678 ),
 ( #6146, #27751, #40499 ),
 ( #15398, #24255, #21797 ),
 ( #12309, #33551, #21179 ),
 ( #36818, #5736, #9218 ),
 ( #21385, #37222, #40107 ) ),
 .UNSPECIFIED., .F., .F., .F. ) 
 B_SPLINE_SURFACE_WITH_KNOTS ( ( 4, 2, 4 ),
 ( 3, 3 ),
 ( 0.6656944266037791991, 1.118245376699337879, 1.570796326794896558 ),
 ( 0.000000000000000000, 1.000000000000000000 ),
 .UNSPECIFIED. ) 
 GEOMETRIC_REPRESENTATION_ITEM ( )  RATIONAL_B_SPLINE_SURFACE ( (
 ( 1.000000000000000000, 0.5935057080259644735, 1.000000000000000000),
 ( 1.000000000000000000, 0.6082500109240246422, 1.000000000000000000),
 ( 1.000000000000000000, 0.6267038978090974100, 1.000000000000000000),
 ( 1.000000000000000000, 0.6661308060341680770, 1.000000000000000000),
 ( 1.000000000000000000, 0.6870851634079389036, 1.000000000000000000),
 ( 1.000000000000000000, 0.7071067811865475727, 1.000000000000000000) ) ) 
 REPRESENTATION_ITEM ( '' )  SURFACE ( )  );
#37992=CARTESIAN_POINT ( 'NONE',  ( 66.69105935506532035, 57.95800471661298303, 3.998864354720668146 ) ) ;
#38007=CARTESIAN_POINT ( 'NONE',  ( 79.23217405491418219, 65.02354781853190957, -3.268578535636863514 ) ) ;
#38009=CARTESIAN_POINT ( 'NONE',  ( 78.69071029820845808, 65.87362605733925136, 2.012706562768930230 ) ) ;
#38011=VERTEX_POINT ( 'NONE', #2235 ) ;
#38015=CARTESIAN_POINT ( 'NONE',  ( -65.15086340151077593, 36.36839105661640303, -8.980608347108747225 ) ) ;
#38028=CARTESIAN_POINT ( 'NONE',  ( 81.27876882982990026, 62.57402737888433109, 3.057227112800006807 ) ) ;
#38030=DIRECTION ( 'NONE',  ( -0.8888117386314182689, -0.4582725098355732163, 0.000000000000000000 ) ) ;
#38035=CARTESIAN_POINT ( 'NONE',  ( -64.84514717441435039, 36.26677316194255241, 6.475000919363831819 ) ) ;
#38046=CARTESIAN_POINT ( 'NONE',  ( 81.26055678261326420, 61.79680472324191243, -2.407735119910393351 ) ) ;
#38056=AXIS2_PLACEMENT_3D ( 'NONE', #40401, #22104, #31983 ) ;
#38057=CARTESIAN_POINT ( 'NONE',  ( 81.07324312733535976, 61.26878263851435236, -1.298998371267911400 ) ) ;
#38060=VERTEX_POINT ( 'NONE', #2858 ) ;
#38062=CARTESIAN_POINT ( 'NONE',  ( 79.18750747900352849, 66.22443723336834864, -1.498428902123936091 ) ) ;
#38069=CARTESIAN_POINT ( 'NONE',  ( 72.21306447944246543, 59.67152943164661849, 3.942504219364092233 ) ) ;
#38076=CARTESIAN_POINT ( 'NONE',  ( -57.16504416091206053, 33.41445838748276742, -4.000000000000000000 ) ) ;
#38078=CARTESIAN_POINT ( 'NONE',  ( 81.20219841815031714, 64.34456771236992267, 3.243459512806143863 ) ) ;
#38088=PLANE ( 'NONE',  #38823 ) ;
#38095=CARTESIAN_POINT ( 'NONE',  ( 66.57179245706689130, 57.82874523672322908, -3.999903336035371293 ) ) ;
#38106=CARTESIAN_POINT ( 'NONE',  ( 80.68997016403551470, 66.19852044017248716, -1.342843868341962121 ) ) ;
#38107=CARTESIAN_POINT ( 'NONE',  ( 79.57367618494546946, 64.93149010139244126, 3.380189700376624362 ) ) ;
#38111=CARTESIAN_POINT ( 'NONE',  ( 75.98741087703852770, 61.93803417815126977, -3.887901781367206322 ) ) ;
#38115=CARTESIAN_POINT ( 'NONE',  ( 81.09074532527955625, 63.51554843946187390, -3.425340496581091632 ) ) ;
#38116=CARTESIAN_POINT ( 'NONE',  ( 75.36936014427642760, 63.22485534106650817, 3.346357594022750792 ) ) ;
#38121=CARTESIAN_POINT ( 'NONE',  ( -58.67303335837859635, 29.89448198981503779, 5.423464252313282330 ) ) ;
#38122=CARTESIAN_POINT ( 'NONE',  ( 82.16223423120683833, 62.72759567084531795, 2.080779877698173408 ) ) ;
#38143=CARTESIAN_POINT ( 'NONE',  ( 67.99537475662653208, 58.47140781303536983, -3.994255761866590149 ) ) ;
#38151=VERTEX_POINT ( 'NONE', #40481 ) ;
#38154=CARTESIAN_POINT ( 'NONE',  ( 79.00945943828583040, 65.94065490460722856, 2.112861953993760089 ) ) ;
#38157=CARTESIAN_POINT ( 'NONE',  ( 79.21623058866053668, 63.63573840405092596, -3.765547211956732365 ) ) ;
#38160=CARTESIAN_POINT ( 'NONE',  ( 81.31796987085881767, 61.39415816021765693, -1.370814772365191114 ) ) ;
#38161=CARTESIAN_POINT ( 'NONE',  ( 78.49476978275076533, 65.27812458131612061, 2.797036776683046622 ) ) ;
#38162=EDGE_CURVE ( 'NONE', #13498, #2581, #24751, .T. ) ;
#38163=AXIS2_PLACEMENT_3D ( 'NONE', #14427, #14831, #8447 ) ;
#38167=CARTESIAN_POINT ( 'NONE',  ( -64.08758708074093136, 41.04287353446839148, 4.000000000000000000 ) ) ;
#38191=CARTESIAN_POINT ( 'NONE',  ( 66.54439450091902586, 57.90558988169555477, 3.999229419688612008 ) ) ;
#38200=LINE ( 'NONE', #1369, #27282 ) ;
#38201=ORIENTED_EDGE ( 'NONE', *, *, #25634, .F. ) ;
#38204=CARTESIAN_POINT ( 'NONE',  ( 80.38728350982638915, 62.86383526565660418, -3.543129918319041227 ) ) ;
#38206=CARTESIAN_POINT ( 'NONE',  ( 80.45282402617027628, 62.88786617374236698, 3.531602295408444281 ) ) ;
#38218=CARTESIAN_POINT ( 'NONE',  ( -64.85784325972055342, 34.81586596186931359, -6.466735817496061856 ) ) ;
#38226=CARTESIAN_POINT ( 'NONE',  ( 80.13405435096434815, 64.91068451853310250, 3.368075118064914886 ) ) ;
#38236=VERTEX_POINT ( 'NONE', #25875 ) ;
#38239=CARTESIAN_POINT ( 'NONE',  ( 72.25564410411975302, 59.56945073910184618, -3.929231508797897288 ) ) ;
#38243=CARTESIAN_POINT ( 'NONE',  ( 80.90982241169463407, 63.07641264110139190, -3.420541042474583460 ) ) ;
#38253=VECTOR ( 'NONE', #19137, 1000.000000000000000 ) ;
#38257=CARTESIAN_POINT ( 'NONE',  ( 78.89771339490202706, 65.85133954292349756, -2.202709653501102149 ) ) ;
#38258=DIRECTION ( 'NONE',  ( 6.733236168141593227E-15, 0.8314686954258621032, 0.5555716052200788679 ) ) ;
#38266=CARTESIAN_POINT ( 'NONE',  ( -63.70768059281056850, 44.39675795404822622, -1.227363068883322139 ) ) ;
#38267=CARTESIAN_POINT ( 'NONE',  ( 69.72614016916874391, 59.17085620800508394, 3.982895692900133344 ) ) ;
#38276=CARTESIAN_POINT ( 'NONE',  ( 80.19843342641586048, 65.64991096649582403, 2.811330881970102613 ) ) ;
#38294=EDGE_CURVE ( 'NONE', #38236, #19152, #36627, .T. ) ;
#38295=CARTESIAN_POINT ( 'NONE',  ( 66.56787846382142959, 57.83972306852010803, -3.999917672784798039 ) ) ;
#38305=CARTESIAN_POINT ( 'NONE',  ( 82.37993866337100712, 63.11845131094293038, -1.936735430446280048 ) ) ;
#38308=ORIENTED_EDGE ( 'NONE', *, *, #10508, .F. ) ;
#38309=CARTESIAN_POINT ( 'NONE',  ( 75.63732367802946044, 59.67466586216193036, -3.300071129360658162 ) ) ;
#38313=CARTESIAN_POINT ( 'NONE',  ( 76.46948511138620574, 60.90388096812812790, 3.723120700756737289 ) ) ;
#38318=CARTESIAN_POINT ( 'NONE',  ( 81.84349429120960906, 61.90138267109058745, 1.539394129974046344 ) ) ;
#38339=CARTESIAN_POINT ( 'NONE',  ( 67.75953150630846267, 58.21208410194267202, -3.997018227265522139 ) ) ;
#38354=CARTESIAN_POINT ( 'NONE',  ( 80.90982241169463407, 63.07641264110139190, 3.420541042474586568 ) ) ;
#38358=CARTESIAN_POINT ( 'NONE',  ( 78.81457101317378999, 64.04164361847183784, -3.641957811749153340 ) ) ;
#38360=CARTESIAN_POINT ( 'NONE',  ( 80.71932482181539115, 65.23126254902230414, -3.019969592843242179 ) ) ;
#38361=CARTESIAN_POINT ( 'NONE',  ( 80.31443933487476272, 61.76769068803228890, 3.015657119755351889 ) ) ;
#38364=CARTESIAN_POINT ( 'NONE',  ( 80.03496335128151884, 66.36160760684386162, 1.085061034363233201 ) ) ;
#38365=CARTESIAN_POINT ( 'NONE',  ( -63.23394756505680903, 41.82033939425821956, 3.940708880140557202 ) ) ;
#38378=DIRECTION ( 'NONE',  ( -1.000000000000000000, 0.000000000000000000, 0.000000000000000000 ) ) ;
#38387=CARTESIAN_POINT ( 'NONE',  ( 66.56200747226770886, 57.85618981312373421, 3.999874661883398463 ) ) ;
#38393=ADVANCED_FACE ( 'NONE', ( #36138 ), #7717, .T. ) ;
#38405=CARTESIAN_POINT ( 'NONE',  ( 80.12334914806359620, 63.07862483458217895, -3.671038198312435163 ) ) ;
#38406=CARTESIAN_POINT ( 'NONE',  ( 78.79414303495669003, 65.54496243571018965, 2.640205493567678641 ) ) ;
#38424=CARTESIAN_POINT ( 'NONE',  ( 81.39943925848319850, 61.85181198611488895, 2.332991218130497924 ) ) ;
#38432=DIRECTION ( 'NONE',  ( 0.000000000000000000, 1.000000000000000000, 0.000000000000000000 ) ) ;
#38433=CARTESIAN_POINT ( 'NONE',  ( 69.19640405677364470, 58.81667877646589204, 3.990151341881418290 ) ) ;
#38441=CARTESIAN_POINT ( 'NONE',  ( 79.17166177841365027, 65.86836750419898578, -2.393593008231246877 ) ) ;
#38450=CARTESIAN_POINT ( 'NONE',  ( 78.97848303377267598, 65.71588112483769351, -2.516896548562721492 ) ) ;
#38460=CARTESIAN_POINT ( 'NONE',  ( -63.70246229030799867, 44.36789000525197224, -1.452554708948875284 ) ) ;
#38461=CARTESIAN_POINT ( 'NONE',  ( 71.10141846075379135, 59.08792130574165924, 3.942344351592514062 ) ) ;
#38471=CARTESIAN_POINT ( 'NONE',  ( 81.69769846481528930, 62.77423530096622528, 2.811330881970099504 ) ) ;
#38500=CARTESIAN_POINT ( 'NONE',  ( -55.43956553351897298, 30.97124788692901376, -1.442063311134004877 ) ) ;
#38502=ORIENTED_EDGE ( 'NONE', *, *, #5494, .F. ) ;
#38505=CARTESIAN_POINT ( 'NONE',  ( 81.79239483946106759, 65.43557760269889911, -1.755995906648851523 ) ) ;
#38508=ORIENTED_EDGE ( 'NONE', *, *, #12109, .T. ) ;
#38509=CARTESIAN_POINT ( 'NONE',  ( 75.74268929893177926, 62.45338499886817374, -3.784676997166835921 ) ) ;
#38510=CARTESIAN_POINT ( 'NONE',  ( -80.92837670882107659, 2.429809908903242555, -12.50000000000000000 ) ) ;
#38513=CARTESIAN_POINT ( 'NONE',  ( 77.06614703306252068, 61.11928327932300675, 3.683100983543551088 ) ) ;
#38518=CARTESIAN_POINT ( 'NONE',  ( 78.68884106766326170, 66.05749720280910253, 1.041818241550643842 ) ) ;
#38541=CARTESIAN_POINT ( 'NONE',  ( 67.73962338513339887, 58.26590004628993569, -3.997461085607390885 ) ) ;
#38547=CARTESIAN_POINT ( 'NONE',  ( -58.99872204295123623, 28.48507918597066180, 6.834244957304007606 ) ) ;
#38549=CARTESIAN_POINT ( 'NONE',  ( -56.34850605459112671, 30.68671187671609246, 2.749655849400831187 ) ) ;
#38553=CARTESIAN_POINT ( 'NONE',  ( 80.17018276713265834, 64.56786917328069819, 3.540619799101248244 ) ) ;
#38556=CARTESIAN_POINT ( 'NONE',  ( 79.25863321418395913, 62.43675908411265141, -3.670385203786648454 ) ) ;
#38560=CARTESIAN_POINT ( 'NONE',  ( 81.58232553940138132, 62.71761900943698009, -2.892908819258012798 ) ) ;
#38561=CARTESIAN_POINT ( 'NONE',  ( 80.42502267531087057, 61.03612496587228975, 1.832491541757258258 ) ) ;
#38565=AXIS2_PLACEMENT_3D ( 'NONE', #30867, #5326, #39904 ) ;
#38568=CARTESIAN_POINT ( 'NONE',  ( 80.38645948019593845, 66.31981033314002616, 1.103079483641125069 ) ) ;
#38569=CARTESIAN_POINT ( 'NONE',  ( -63.08758708074093136, 41.04287353446839148, 4.000000000000000000 ) ) ;
#38571=CARTESIAN_POINT ( 'NONE',  ( -63.23359472962059158, 35.57513467056950418, -6.582177359051184062 ) ) ;
#38591=ORIENTED_EDGE ( 'NONE', *, *, #21900, .F. ) ;
#38593=CARTESIAN_POINT ( 'NONE',  ( 66.73521764480442187, 57.83500309307840581, 3.999076693781861813 ) ) ;
#38596=CARTESIAN_POINT ( 'NONE',  ( -64.08758708074093136, 38.34280096101142732, 3.014656224624933323 ) ) ;
#38608=CARTESIAN_POINT ( 'NONE',  ( 80.44027647058022978, 62.28541378099806280, -3.311815948186457970 ) ) ;
#38610=CARTESIAN_POINT ( 'NONE',  ( 80.59739669508314819, 62.32949743464991599, 3.275607309966489300 ) ) ;
#38612=FACE_OUTER_BOUND ( 'NONE', #35518, .T. ) ;
#38621=VERTEX_POINT ( 'NONE', #38547 ) ;
#38632=CARTESIAN_POINT ( 'NONE',  ( 79.45632949585316851, 65.80330994668891265, 2.596981798947342934 ) ) ;
#38644=CARTESIAN_POINT ( 'NONE',  ( 81.12411360294466078, 61.28734817074503383, -1.205449537698830564 ) ) ;
#38649=CARTESIAN_POINT ( 'NONE',  ( -56.22749146662677333, 30.67773648377099960, 3.904540345294678527 ) ) ;
#38655=CARTESIAN_POINT ( 'NONE',  ( 80.99344733541398966, 61.93321701578152272, -2.778975589575374272 ) ) ;
#38658=ORIENTED_EDGE ( 'NONE', *, *, #7722, .F. ) ;
#38659=ORIENTED_EDGE ( 'NONE', *, *, #12109, .F. ) ;
#38660=CYLINDRICAL_SURFACE ( 'NONE', #12761, 1.000000000000000888 ) ;
#38666=CARTESIAN_POINT ( 'NONE',  ( 70.93434718597480071, 59.50194243796293136, 3.976054184260643609 ) ) ;
#38677=CARTESIAN_POINT ( 'NONE',  ( 81.60486409337941893, 61.94451848015731343, 2.198649373794019812 ) ) ;
#38689=DIRECTION ( 'NONE',  ( 1.000000000000000000, 6.106796269766979397E-16, 0.000000000000000000 ) ) ;
#38693=VERTEX_POINT ( 'NONE', #23126 ) ;
#38698=CARTESIAN_POINT ( 'NONE',  ( -63.03213158086148837, 38.26878225442760595, -4.032857076800604901 ) ) ;
#38702=CARTESIAN_POINT ( 'NONE',  ( -64.08758708074094557, 36.44316031593082528, -3.600279212593069378 ) ) ;
#38705=CARTESIAN_POINT ( 'NONE',  ( -56.76293260130697860, 30.10808691202855414, -4.002692287617906075 ) ) ;
#38709=CARTESIAN_POINT ( 'NONE',  ( 80.87103490326487076, 66.01227193428218243, -1.936735430446280937 ) ) ;
#38713=ORIENTED_EDGE ( 'NONE', *, *, #19206, .T. ) ;
#38714=CARTESIAN_POINT ( 'NONE',  ( 75.51044298776172070, 62.93595297499962271, -3.562065002326785468 ) ) ;
#38718=CARTESIAN_POINT ( 'NONE',  ( 75.58676173236693785, 62.77776356238128130, 3.642592851537399312 ) ) ;
#38725=CARTESIAN_POINT ( 'NONE',  ( 82.09872185058188165, 62.41535711091003691, 1.944145319385261583 ) ) ;
#38737=CARTESIAN_POINT ( 'NONE',  ( -63.61759533396914179, 43.90016037724900144, -2.585133859511243859 ) ) ;
#38747=CARTESIAN_POINT ( 'NONE',  ( 67.43935760634008147, 58.17964655298460741, -3.998402061830689025 ) ) ;
#38763=CARTESIAN_POINT ( 'NONE',  ( 80.49748116766495798, 63.97695225015618803, 3.602832836245131620 ) ) ;
#38766=CARTESIAN_POINT ( 'NONE',  ( 78.58588809754505178, 64.79968573292298117, -3.228498513792966040 ) ) ;
#38769=CARTESIAN_POINT ( 'NONE',  ( 79.25461589595286682, 66.09583247779735871, -1.930361577749150515 ) ) ;
#38770=CARTESIAN_POINT ( 'NONE',  ( 80.35854813638249539, 61.23284135048810839, 2.372109611208351510 ) ) ;
#38773=EDGE_CURVE ( 'NONE', #15750, #30676, #28112, .T. ) ;
#38774=CARTESIAN_POINT ( 'NONE',  ( 78.69031774315027405, 66.05854625464691310, 1.008685033153497335 ) ) ;
#38775=CARTESIAN_POINT ( 'NONE',  ( -64.08758708074091714, 43.73155672946558781, 2.304326576497605306 ) ) ;
#38777=CARTESIAN_POINT ( 'NONE',  ( -64.30032790741503845, 34.77233229845787577, -5.249462333892792820 ) ) ;
#38791=CARTESIAN_POINT ( 'NONE',  ( -80.19065981525227471, 31.27226540113725051, -8.800414904976364028 ) ) ;
#38796=CARTESIAN_POINT ( 'NONE',  ( 66.71755507405909214, 57.88420400998732163, 3.999756211082241109 ) ) ;
#38802=VERTEX_POINT ( 'NONE', #6775 ) ;
#38811=CARTESIAN_POINT ( 'NONE',  ( 79.12445352002978893, 64.93440905817641351, -3.301258712451523358 ) ) ;
#38814=CARTESIAN_POINT ( 'NONE',  ( 78.60455099833413328, 65.79598288722411326, 2.095806625473878970 ) ) ;
#38823=AXIS2_PLACEMENT_3D ( 'NONE', #35036, #18746, #24939 ) ;
#38828=CARTESIAN_POINT ( 'NONE',  ( 79.73516162904326166, 65.38506083608318420, 3.083955809406667914 ) ) ;
#38840=CARTESIAN_POINT ( 'NONE',  ( 68.58273017919226788, 58.67848115723035107, 3.992679187475148161 ) ) ;
#38846=CARTESIAN_POINT ( 'NONE',  ( 80.92403995952693663, 62.73960429493251212, -3.332694751021839430 ) ) ;
#38859=CARTESIAN_POINT ( 'NONE',  ( 80.52560336917625250, 62.91486207252160057, -3.518158556798104630 ) ) ;
#38861=CARTESIAN_POINT ( 'NONE',  ( 81.04163241827637876, 61.94641952267326701, 2.758686562281579047 ) ) ;
#38866=CARTESIAN_POINT ( 'NONE',  ( -58.17330720045938364, 29.79550679426005644, -4.662693745304140158 ) ) ;
#38878=CARTESIAN_POINT ( 'NONE',  ( 81.64185025297332743, 61.96196063151020184, 2.170472567306916734 ) ) ;
#38888=DIRECTION ( 'NONE',  ( 0.000000000000000000, 0.000000000000000000, 1.000000000000000000 ) ) ;
#38899=CARTESIAN_POINT ( 'NONE',  ( 66.27376694609004915, 57.73522568913436004, -4.000000000000000000 ) ) ;
#38901=ADVANCED_FACE ( 'NONE', ( #36184 ), #29795, .F. ) ;
#38904=CARTESIAN_POINT ( 'NONE',  ( -1.432293644835494373, -27.47664038617742577, -1.000000000000000000 ) ) ;
#38906=CARTESIAN_POINT ( 'NONE',  ( -57.31959649706902127, 29.49889766843898187, -4.251262061546396076 ) ) ;
#38910=CARTESIAN_POINT ( 'NONE',  ( 78.98267122246090821, 66.20432814577485203, -1.134074597586744115 ) ) ;
#38916=CARTESIAN_POINT ( 'NONE',  ( 75.43741953989470517, 63.08613174173238747, 3.462570962765048055 ) ) ;
#38919=DIRECTION ( 'NONE',  ( -0.000000000000000000, 0.000000000000000000, -1.000000000000000000 ) ) ;
#38924=CARTESIAN_POINT ( 'NONE',  ( 79.21008177357740010, 66.23692415242767595, 1.465632304122485685 ) ) ;
#38929=AXIS2_PLACEMENT_3D ( 'NONE', #37230, #40510, #9025 ) ;
#38942=CARTESIAN_POINT ( 'NONE',  ( 67.64019463258649978, 58.53452770292938112, -3.982857479566666914 ) ) ;
#38955=CARTESIAN_POINT ( 'NONE',  ( 79.24015747652954644, 65.65980919716056974, 2.710038060602471877 ) ) ;
#38958=CARTESIAN_POINT ( 'NONE',  ( 78.65659160455585663, 63.63274296288032161, -3.750642650174855319 ) ) ;
#38961=CARTESIAN_POINT ( 'NONE',  ( 81.60109106392830824, 62.17032169346391157, -2.476693319882541378 ) ) ;
#38962=CARTESIAN_POINT ( 'NONE',  ( 78.19628368166274868, 65.45398019160434444, 2.372109611208335078 ) ) ;
#38964=CARTESIAN_POINT ( 'NONE',  ( 82.59411735159427792, 63.56171878218358273, 1.145133701562419226 ) ) ;
#38968=CARTESIAN_POINT ( 'NONE',  ( -64.35089310738592872, 36.57692748660996074, -5.628006413927908014 ) ) ;
#38987=CARTESIAN_POINT ( 'NONE',  ( 66.42297474478721142, 57.78816748095999145, 4.000000000000013323 ) ) ;
#38988=CARTESIAN_POINT ( 'NONE',  ( 72.70998213798715426, 61.65396340192921087, -3.619654763610430592 ) ) ;
#38989=CARTESIAN_POINT ( 'NONE',  ( -64.08758708074093136, 38.76906266698302517, 2.999999999999999112 ) ) ;
#39001=CARTESIAN_POINT ( 'NONE',  ( 78.79414303495656213, 65.54496243570987701, -2.640205493567942874 ) ) ;
#39003=CARTESIAN_POINT ( 'NONE',  ( 79.45016587565709187, 64.47252957033400378, 3.557377001560511509 ) ) ;
#39011=CARTESIAN_POINT ( 'NONE',  ( 75.43605262791740529, 63.77904386412239290, -2.884284812001602027 ) ) ;
#39017=CARTESIAN_POINT ( 'NONE',  ( 80.45774067191288736, 64.33927723362793927, 3.562450064734662636 ) ) ;
#39032=AXIS2_PLACEMENT_3D ( 'NONE', #38510, #30477, #39520 ) ;
#39033=CARTESIAN_POINT ( 'NONE',  ( 68.50220056233268906, 58.89075781393282227, 3.976359261632469444 ) ) ;
#39036=LINE ( 'NONE', #29782, #39145 ) ;
#39038=CARTESIAN_POINT ( 'NONE',  ( 79.10769140560613266, 65.82222301601623826, -2.432199249741003211 ) ) ;
#39050=CARTESIAN_POINT ( 'NONE',  ( 79.86701161339750854, 64.38869582053065699, -3.619557188109182810 ) ) ;
#39052=CARTESIAN_POINT ( 'NONE',  ( 80.35739993109717716, 63.53218113005920742, 3.674973878998263555 ) ) ;
#39072=CARTESIAN_POINT ( 'NONE',  ( 81.21919753139290776, 63.96565923609905013, 3.341858160559717295 ) ) ;
#39098=CYLINDRICAL_SURFACE ( 'NONE', #32346, 2.500000000000002220 ) ;
#39108=CARTESIAN_POINT ( 'NONE',  ( 81.53194397951688188, 65.66224036380454265, -1.718006205139864795 ) ) ;
#39117=CARTESIAN_POINT ( 'NONE',  ( 75.00613679496295561, 61.08591394029932076, 3.912919437578906035 ) ) ;
#39125=CARTESIAN_POINT ( 'NONE',  ( 80.84167751523420975, 65.66068717198515969, 2.558871340112365278 ) ) ;
#39137=CARTESIAN_POINT ( 'NONE',  ( -63.35138607920025322, 42.45142311247835920, -3.729943156278033189 ) ) ;
#39138=AXIS2_PLACEMENT_3D ( 'NONE', #2871, #8795, #28577 ) ;
#39144=CARTESIAN_POINT ( 'NONE',  ( 67.08333554474984339, 58.24655189615426565, -3.990981480864018938 ) ) ;
#39145=VECTOR ( 'NONE', #1598, 1000.000000000000000 ) ;
#39157=CARTESIAN_POINT ( 'NONE',  ( 80.51591231855054787, 63.60920045316173344, 3.640670270625566030 ) ) ;
#39160=CARTESIAN_POINT ( 'NONE',  ( 78.61725963159940989, 63.00713372587870964, -3.804514705604311153 ) ) ;
#39163=CARTESIAN_POINT ( 'NONE',  ( 79.86705713782787086, 65.75210810416335505, -2.684801069570281751 ) ) ;
#39164=CARTESIAN_POINT ( 'NONE',  ( 77.82439497328331868, 65.16220298991649429, 2.551779361026667470 ) ) ;
#39168=CARTESIAN_POINT ( 'NONE',  ( 82.26973386304365476, 64.90130211351629441, 1.165579324820864571 ) ) ;
#39173=CARTESIAN_POINT ( 'NONE',  ( -64.09407456991024787, 35.62175799955578981, -4.126536650000701023 ) ) ;
#39178=CYLINDRICAL_SURFACE ( 'NONE', #28111, 117.6618724293813898 ) ;
#39187=DIRECTION ( 'NONE',  ( 1.000000000000000000, 0.000000000000000000, 0.000000000000000000 ) ) ;
#39193=CARTESIAN_POINT ( 'NONE',  ( 66.27376694608996388, 57.73522568913447373, 4.000000000000000000 ) ) ;
#39194=CARTESIAN_POINT ( 'NONE',  ( 71.23183612236115891, 58.76351790733232860, -3.862811858476256077 ) ) ;
#39197=CARTESIAN_POINT ( 'NONE',  ( -60.14275962559869981, 24.84364830758654108, 9.154021781743367114 ) ) ;
#39204=DIRECTION ( 'NONE',  ( -0.4690749385695702212, -0.8831583674550980145, 0.000000000000000000 ) ) ;
#39209=CARTESIAN_POINT ( 'NONE',  ( 80.63281215842000904, 62.09153919268369037, -3.087291694836846290 ) ) ;
#39211=CARTESIAN_POINT ( 'NONE',  ( 80.91431153141797950, 61.21107275232134981, 1.487544896895754309 ) ) ;
#39218=LINE ( 'NONE', #11008, #5535 ) ;
#39227=CARTESIAN_POINT ( 'NONE',  ( 79.50768156050781954, 65.53910429656815495, 2.885071930847944444 ) ) ;
#39237=CARTESIAN_POINT ( 'NONE',  ( 68.09143390058649459, 58.21448531840948704, 3.990965707299598098 ) ) ;
#39242=CARTESIAN_POINT ( 'NONE',  ( 80.30248525907990143, 64.25517361537380623, -3.614389211669654323 ) ) ;
#39245=CARTESIAN_POINT ( 'NONE',  ( -58.56173084424084863, 30.28994157939056819, 5.156891857687778469 ) ) ;
#39252=CARTESIAN_POINT ( 'NONE',  ( 81.04993867939947449, 61.73413400689819497, -2.516896548562718383 ) ) ;
#39253=EDGE_CURVE ( 'NONE', #30342, #35091, #34638, .T. ) ;
#39257=CARTESIAN_POINT ( 'NONE',  ( 78.97848303377290335, 65.71588112483786404, 2.516896548562567837 ) ) ;
#39259=LINE ( 'NONE', #26916, #13801 ) ;
#39279=CARTESIAN_POINT ( 'NONE',  ( 80.00444560209926692, 65.54189868873926628, 2.943961322784983459 ) ) ;
#39284=AXIS2_PLACEMENT_3D ( 'NONE', #33277, #21119, #27280 ) ;
#39313=CARTESIAN_POINT ( 'NONE',  ( 81.80771926544778694, 61.88353390887438366, -1.601045042264586771 ) ) ;
#39316=ORIENTED_EDGE ( 'NONE', *, *, #15147, .T. ) ;
#39320=CARTESIAN_POINT ( 'NONE',  ( 75.20156067606269801, 62.14723293136128746, 3.810661578667819960 ) ) ;
#39324=CARTESIAN_POINT ( 'NONE',  ( -63.03213158086111179, 38.26878225442446535, 4.032857076801017016 ) ) ;
#39326=CARTESIAN_POINT ( 'NONE',  ( -55.62677557291493713, 30.95433239688068738, -1.979412988903662463 ) ) ;
#39330=CARTESIAN_POINT ( 'NONE',  ( 79.70081467235792161, 66.18075109116949761, 1.965143080302226952 ) ) ;
#39343=ORIENTED_EDGE ( 'NONE', *, *, #1371, .F. ) ;
#39345=CARTESIAN_POINT ( 'NONE',  ( -64.08758708074091714, 38.55573457772874946, -3.000000000000000444 ) ) ;
#39346=CARTESIAN_POINT ( 'NONE',  ( 67.52644525400921793, 57.94193659033309274, -3.989212576213370109 ) ) ;
#39360=CARTESIAN_POINT ( 'NONE',  ( 79.53763471700084153, 65.25825451995498838, 3.163072811751573177 ) ) ;
#39361=EDGE_CURVE ( 'NONE', #31581, #21319, #20225, .T. ) ;
#39365=CARTESIAN_POINT ( 'NONE',  ( 77.77823160594137164, 63.95155898497984026, -3.535928464255530645 ) ) ;
#39368=CARTESIAN_POINT ( 'NONE',  ( 81.41826528542581798, 63.68099735521261096, -3.235508711551935424 ) ) ;
#39369=CARTESIAN_POINT ( 'NONE',  ( 78.19518920554678232, 64.50268734400745529, 3.317372267376125894 ) ) ;
#39372=CARTESIAN_POINT ( 'NONE',  ( 82.04611962119309965, 65.17642557464539266, 1.633153239554254732 ) ) ;
#39376=CARTESIAN_POINT ( 'NONE',  ( -62.83712641625177753, 35.61106514070151263, -5.789832448495768169 ) ) ;
#39393=CIRCLE ( 'NONE', #2644, 82.54614097552274643 ) ;
#39395=CARTESIAN_POINT ( 'NONE',  ( 66.27376694608996388, 57.73522568913447373, 4.000000000000000000 ) ) ;
#39397=CARTESIAN_POINT ( 'NONE',  ( 73.28086911227147482, 60.35416371166882499, -3.944160774611113585 ) ) ;
#39406=VECTOR ( 'NONE', #15986, 1000.000000000000000 ) ;
#39409=EDGE_CURVE ( 'NONE', #5157, #30864, #8524, .T. ) ;
#39411=CARTESIAN_POINT ( 'NONE',  ( 79.14523234120532891, 64.60782394083948077, -3.482780605906210525 ) ) ;
#39414=CARTESIAN_POINT ( 'NONE',  ( 80.53463578537552792, 62.06606814882641743, 3.115013800517338005 ) ) ;
#39425=LINE ( 'NONE', #14712, #12285 ) ;
#39427=CARTESIAN_POINT ( 'NONE',  ( 81.14684024915200666, 61.29565758240214279, 1.145133111591830621 ) ) ;
#39437=CARTESIAN_POINT ( 'NONE',  ( 67.42350544106223253, 58.22289815522609047, 3.997566301760141272 ) ) ;
#39444=CARTESIAN_POINT ( 'NONE',  ( 80.09489858828513320, 64.52483703883090982, -3.563857694938803444 ) ) ;
#39455=CARTESIAN_POINT ( 'NONE',  ( 80.90366483818405641, 61.70104970548236167, -2.590854534519439145 ) ) ;
#39456=CARTESIAN_POINT ( 'NONE',  ( 80.30571993285305155, 63.50758298881806496, 3.683925914261492629 ) ) ;
#39458=CARTESIAN_POINT ( 'NONE',  ( -65.15086340151077593, 36.36839105661640303, 8.980608347108747225 ) ) ;
#39461=CARTESIAN_POINT ( 'NONE',  ( 76.54260510937174899, 60.74419326975380073, -3.642592851547832300 ) ) ;
#39466=CARTESIAN_POINT ( 'NONE',  ( -64.08758708074093136, 38.76906266698303227, -3.000000000000000000 ) ) ;
#39468=LINE ( 'NONE', #24026, #23220 ) ;
#39470=VERTEX_POINT ( 'NONE', #14498 ) ;
#39477=CARTESIAN_POINT ( 'NONE',  ( 81.38764266124185554, 63.30759111148522322, 3.202775791561840002 ) ) ;
#39487=EDGE_CURVE ( 'NONE', #1373, #31247, #32650, .T. ) ;
#39502=EDGE_LOOP ( 'NONE', ( #9402, #32858, #25084, #7914 ) ) ;
#39507=CARTESIAN_POINT ( 'NONE',  ( -77.95330471031414277, 33.71485196875532608, -8.800414904976364028 ) ) ;
#39509=CARTESIAN_POINT ( 'NONE',  ( -74.92283640148291113, 18.87330372387140187, 12.49999999999999645 ) ) ;
#39517=CARTESIAN_POINT ( 'NONE',  ( 82.17930952126317834, 63.71034004053205280, -2.400449347018691171 ) ) ;
#39518=CARTESIAN_POINT ( 'NONE',  ( -58.99872204295123623, 28.48507918597066180, 6.834244957304007606 ) ) ;
#39520=DIRECTION ( 'NONE',  ( 1.000000000000000000, 0.000000000000000000, 0.000000000000000000 ) ) ;
#39523=CARTESIAN_POINT ( 'NONE',  ( 74.11268706641025972, 61.54722250361106717, 3.856662941142631862 ) ) ;
#39527=EDGE_CURVE ( 'NONE', #6853, #33628, #34907, .T. ) ;
#39530=CARTESIAN_POINT ( 'NONE',  ( -63.25751591902427151, 35.57396452027732892, 6.629192056479301876 ) ) ;
#39532=CARTESIAN_POINT ( 'NONE',  ( 80.93893743487458892, 65.34845912995864126, 2.808566127056212114 ) ) ;
#39551=CARTESIAN_POINT ( 'NONE',  ( 67.18400333313441308, 57.97000644093014188, -3.997693602769901045 ) ) ;
#39565=CARTESIAN_POINT ( 'NONE',  ( 82.55792188592127445, 63.20960171500892955, -1.000000000000000000 ) ) ;
#39566=CARTESIAN_POINT ( 'NONE',  ( 81.11292571623972947, 62.23233742369612997, 2.923497156821702525 ) ) ;
#39569=CARTESIAN_POINT ( 'NONE',  ( 78.06740453511717703, 61.95427634543510464, -3.748203062644121619 ) ) ;
#39572=CARTESIAN_POINT ( 'NONE',  ( 81.38674634791389906, 61.68395714348710612, -2.028924249969755955 ) ) ;
#39573=CARTESIAN_POINT ( 'NONE',  ( 79.88607388276625443, 61.09294650314146224, 2.551779361026688342 ) ) ;
#39574=EDGE_LOOP ( 'NONE', ( #1657, #30883, #36634, #24396 ) ) ;
#39578=CARTESIAN_POINT ( 'NONE',  ( 81.27149311957296618, 65.88890312491021461, 1.680016503630072489 ) ) ;
#39595=DIRECTION ( 'NONE',  ( -0.000000000000000000, -0.000000000000000000, 1.000000000000000000 ) ) ;
#39604=CARTESIAN_POINT ( 'NONE',  ( 66.43385761674670675, 57.75742247880102553, 4.000000000000003553 ) ) ;
#39605=CARTESIAN_POINT ( 'NONE',  ( 71.32664523234116416, 58.52704510057537135, -3.775670717450666736 ) ) ;
#39614=ORIENTED_EDGE ( 'NONE', *, *, #39527, .T. ) ;
#39620=CARTESIAN_POINT ( 'NONE',  ( 78.80159527267854003, 65.27891740916034280, -2.934133054905260884 ) ) ;
#39623=CARTESIAN_POINT ( 'NONE',  ( 78.91303721271684424, 66.16570306020605585, -1.285939662725172461 ) ) ;
#39624=CARTESIAN_POINT ( 'NONE',  ( 78.99843287308405593, 65.13824187233507246, 3.101774481621351498 ) ) ;
#39643=CARTESIAN_POINT ( 'NONE',  ( -64.08758708074094557, 35.89352542652032696, 3.939681497839040425 ) ) ;
#39648=CARTESIAN_POINT ( 'NONE',  ( 67.79930094788625183, 58.10454462619039617, 3.992148460412408895 ) ) ;
#39656=CIRCLE ( 'NONE', #9421, 98.38357402481355507 ) ;
#39657=CARTESIAN_POINT ( 'NONE',  ( -59.35030935981329492, 27.06751177275602416, 5.142387704658994529 ) ) ;
#39662=CARTESIAN_POINT ( 'NONE',  ( 80.99919828920802445, 61.56308015027071434, -2.277920705665343437 ) ) ;
#39664=CARTESIAN_POINT ( 'NONE',  ( 80.99395165659490203, 61.72087377645424056, 2.545842637937928643 ) ) ;
#39666=CARTESIAN_POINT ( 'NONE',  ( -66.83699642652008777, 37.05199716444892744, 9.800414904976364028 ) ) ;
#39668=CARTESIAN_POINT ( 'NONE',  ( 73.85752424338471656, 60.59307193704751882, -3.935025356177997757 ) ) ;
#39670=MANIFOLD_SOLID_BREP ( 'Fillet13', #3249 ) ;
#39682=ORIENTED_EDGE ( 'NONE', *, *, #32881, .T. ) ;
#39684=CARTESIAN_POINT ( 'NONE',  ( 79.01071357413493956, 66.12284964548014443, 1.692865493182734271 ) ) ;
#39702=ORIENTED_EDGE ( 'NONE', *, *, #35205, .F. ) ;
#39703=CARTESIAN_POINT ( 'NONE',  ( 81.29933375999361544, 61.48586111389077757, -1.777114115212629075 ) ) ;
#39713=ORIENTED_EDGE ( 'NONE', *, *, #13339, .F. ) ;
#39716=CARTESIAN_POINT ( 'NONE',  ( 81.14230761098953337, 61.33243076862672183, -1.577285172236833288 ) ) ;
#39717=CARTESIAN_POINT ( 'NONE',  ( -58.20517375958247897, 28.49598760833108813, -5.016376253474278180 ) ) ;
#39724=CARTESIAN_POINT ( 'NONE',  ( 78.68944183191024422, 66.05792399308624852, -1.032522165606416298 ) ) ;
#39725=DIRECTION ( 'NONE',  ( 0.000000000000000000, 1.000000000000000000, 0.000000000000000000 ) ) ;
#39730=CARTESIAN_POINT ( 'NONE',  ( 73.92749824250802249, 61.95374747488791201, 3.708893976703420137 ) ) ;
#39736=CARTESIAN_POINT ( 'NONE',  ( -55.39244940828794483, 31.07786128219253996, -1.730094348643104185 ) ) ;
#39742=CARTESIAN_POINT ( 'NONE',  ( 81.87453109492318504, 63.55405699985837487, 2.808566127056211670 ) ) ;
#39760=CARTESIAN_POINT ( 'NONE',  ( 66.71755507405909214, 57.88420400998732163, -3.999756211082241109 ) ) ;
#39769=CARTESIAN_POINT ( 'NONE',  ( 75.43647511836071828, 63.77933554463422183, 2.884169428409014913 ) ) ;
#39776=CARTESIAN_POINT ( 'NONE',  ( 81.16957891225081312, 61.30398062001320625, -1.002944004955704127 ) ) ;
#39779=CARTESIAN_POINT ( 'NONE',  ( 80.36137575039691683, 63.90592395025429795, 3.640670270625567362 ) ) ;
#39782=CARTESIAN_POINT ( 'NONE',  ( 78.75717319332352417, 60.46956391627943361, -2.498359881428382057 ) ) ;
#39788=CARTESIAN_POINT ( 'NONE',  ( 81.15394892944708261, 63.54712375395006774, -3.396356880839461301 ) ) ;
#39789=CARTESIAN_POINT ( 'NONE',  ( 79.97179536941432332, 60.87748285318664898, 2.061059937946318144 ) ) ;
#39794=CARTESIAN_POINT ( 'NONE',  ( 82.36730661685074040, 64.56044919582443242, 1.633153239554254732 ) ) ;
#39796=CARTESIAN_POINT ( 'NONE',  ( -63.08758708074093136, -21.25669541281728669, 4.000000000000000000 ) ) ;
#39804=CARTESIAN_POINT ( 'NONE',  ( -63.70768058868311812, 44.39675795731059793, 1.000000000000000000 ) ) ;
#39813=ADVANCED_FACE ( 'NONE', ( #19638 ), #18811, .T. ) ;
#39817=AXIS2_PLACEMENT_3D ( 'NONE', #14661, #2143, #30541 ) ;
#39822=CARTESIAN_POINT ( 'NONE',  ( 66.58744840590414071, 57.78483400379950297, 3.999444518112384106 ) ) ;
#39823=CARTESIAN_POINT ( 'NONE',  ( 69.11491457486368972, 59.02763561571557460, -3.981537309218733167 ) ) ;
#39824=EDGE_CURVE ( 'NONE', #15453, #6853, #479, .T. ) ;
#39827=DIRECTION ( 'NONE',  ( -0.9506097019758702471, 0.3103887796125167076, -7.179182702314986818E-16 ) ) ;
#39833=CARTESIAN_POINT ( 'NONE',  ( -64.08758708074093136, 38.76906266698302517, -3.000000000000000000 ) ) ;
#39836=EDGE_CURVE ( 'NONE', #33117, #28074, #15171, .T. ) ;
#39838=CARTESIAN_POINT ( 'NONE',  ( 78.92462413491021778, 65.07527128086411494, -3.128253119413328509 ) ) ;
#39840=CARTESIAN_POINT ( 'NONE',  ( 81.74240050578430328, 63.84683571418585046, -2.967158453529146200 ) ) ;
#39841=CARTESIAN_POINT ( 'NONE',  ( 80.30026770407557990, 62.83227110018538042, 3.557377001560497742 ) ) ;
#39843=CARTESIAN_POINT ( 'NONE',  ( -66.99872204295122913, 28.48507918597134037, -9.800414904976365804 ) ) ;
#39863=CARTESIAN_POINT ( 'NONE',  ( 67.66997365410338716, 58.45410198214950981, 3.990378031984447293 ) ) ;
#39874=CARTESIAN_POINT ( 'NONE',  ( 80.98923082824005348, 61.23822351929057106, -1.409197735201532131 ) ) ;
#39876=CARTESIAN_POINT ( 'NONE',  ( 80.15465141033503471, 63.79803065853153754, 3.683925914261492185 ) ) ;
#39882=CARTESIAN_POINT ( 'NONE',  ( 74.91450450041774900, 59.74817859300107159, -3.564124015814033708 ) ) ;
#39889=DIRECTION ( 'NONE',  ( 0.000000000000000000, 1.000000000000000000, 0.000000000000000000 ) ) ;
#39897=CARTESIAN_POINT ( 'NONE',  ( 79.61430779865300167, 65.89704723538268638, 2.499697124809921345 ) ) ;
#39904=DIRECTION ( 'NONE',  ( -1.000000000000000000, 0.000000000000000000, 0.000000000000000000 ) ) ;
#39914=CARTESIAN_POINT ( 'NONE',  ( 78.67529526371438919, 66.04787469174289072, -1.130345937366645792 ) ) ;
#39920=AXIS2_PLACEMENT_3D ( 'NONE', #27712, #21141, #33707 ) ;
#39927=CARTESIAN_POINT ( 'NONE',  ( 80.56654867478538051, 63.26449302893301052, -3.600689860192758385 ) ) ;
#39928=DIRECTION ( 'NONE',  ( -1.000000000000000000, 0.000000000000000000, 0.000000000000000000 ) ) ;
#39933=CARTESIAN_POINT ( 'NONE',  ( 82.22785179944503398, 62.76084426383153669, -1.971256063808603631 ) ) ;
#39935=DIRECTION ( 'NONE',  ( -0.000000000000000000, -0.000000000000000000, -1.000000000000000000 ) ) ;
#39941=CARTESIAN_POINT ( 'NONE',  ( 75.06813672635826151, 59.39477395272206905, 3.294766324886222453 ) ) ;
#39943=CARTESIAN_POINT ( 'NONE',  ( -56.10469124525552331, 30.75883671979822509, -2.489329600088171723 ) ) ;
#39947=CARTESIAN_POINT ( 'NONE',  ( 81.76287911024846267, 64.24668757703155109, 2.864610283900509202 ) ) ;
#39968=CARTESIAN_POINT ( 'NONE',  ( 66.74992980603514070, 57.79401841677491092, -3.997717836767872512 ) ) ;
#39970=TOROIDAL_SURFACE ( 'NONE', #39284, 5.329987104167480894, 1.000000000000000000 ) ;
#39978=DIRECTION ( 'NONE',  ( 0.000000000000000000, 0.000000000000000000, 1.000000000000000000 ) ) ;
#39981=CARTESIAN_POINT ( 'NONE',  ( 81.03660848153758423, 66.10018949144991041, -1.263752851813363387 ) ) ;
#39982=CARTESIAN_POINT ( 'NONE',  ( 79.19089293128583051, 65.62284279856316971, 2.735335646780914676 ) ) ;
#39986=CARTESIAN_POINT ( 'NONE',  ( 77.65795924533195205, 64.82981391430574547, -2.842954625922224476 ) ) ;
#39989=CARTESIAN_POINT ( 'NONE',  ( 81.27686174477108239, 61.37652599617193516, -1.416821487223366871 ) ) ;
#39990=CARTESIAN_POINT ( 'NONE',  ( 79.07090634323701295, 63.55465448991838429, 3.774260586041105814 ) ) ;
#39991=ORIENTED_EDGE ( 'NONE', *, *, #36748, .F. ) ;
#39994=CARTESIAN_POINT ( 'NONE',  ( 81.82660409393668033, 65.45354236959411764, 1.617049763655828531 ) ) ;
#40006=FACE_OUTER_BOUND ( 'NONE', #9705, .T. ) ;
#40020=CARTESIAN_POINT ( 'NONE',  ( 69.80049859759003539, 58.98221833774336176, -3.985452289341161691 ) ) ;
#40024=AXIS2_PLACEMENT_3D ( 'NONE', #35060, #32569, #32366 ) ;
#40035=CARTESIAN_POINT ( 'NONE',  ( 80.76403243373638929, 61.15693784680268408, -1.612955153530313046 ) ) ;
#40037=CARTESIAN_POINT ( 'NONE',  ( 81.89445579901081373, 62.31310441928815180, -2.222430037836082839 ) ) ;
#40038=CARTESIAN_POINT ( 'NONE',  ( 79.36500080098821286, 64.41263654525117488, 3.571698303486884996 ) ) ;
#40060=ORIENTED_EDGE ( 'NONE', *, *, #39253, .T. ) ;
#40061=CARTESIAN_POINT ( 'NONE',  ( 67.70975997764571730, 58.34660981014267378, 3.996132678073276878 ) ) ;
#40065=VECTOR ( 'NONE', #22558, 1000.000000000000000 ) ;
#40079=CARTESIAN_POINT ( 'NONE',  ( 78.62745313524290225, 65.95871297147078849, -1.682919622592493614 ) ) ;
#40081=CARTESIAN_POINT ( 'NONE',  ( 80.25680044982712502, 63.48435701671617437, 3.692178340560210437 ) ) ;
#40084=CARTESIAN_POINT ( 'NONE',  ( 75.06813672635826151, 59.39477395272206905, -3.294766324886222897 ) ) ;
#40092=AXIS2_PLACEMENT_3D ( 'NONE', #18359, #1377, #13908 ) ;
#40096=CARTESIAN_POINT ( 'NONE',  ( 78.97265649164181411, 66.09949689503534387, 1.726519205789194045 ) ) ;
#40107=CARTESIAN_POINT ( 'NONE',  ( -69.08758708074093136, 36.88538962427717394, -8.800414904976365804 ) ) ;
#40113=EDGE_CURVE ( 'NONE', #4188, #31697, #34015, .T. ) ;
#40117=CARTESIAN_POINT ( 'NONE',  ( 78.77947119303418333, 66.08315628559921606, -1.459100623883114345 ) ) ;
#40126=CARTESIAN_POINT ( 'NONE',  ( 79.98933190693155382, 64.46315002137731653, -3.592474444481856821 ) ) ;
#40132=CARTESIAN_POINT ( 'NONE',  ( 82.31242756469269750, 63.41700585080309338, -2.192618372227128631 ) ) ;
#40134=CARTESIAN_POINT ( 'NONE',  ( -63.08758708074093136, 41.61202515287869375, -4.000000000000000000 ) ) ;
#40139=CARTESIAN_POINT ( 'NONE',  ( 74.03116782478153368, 60.19763641771454132, 3.876585409280477013 ) ) ;
#40145=CARTESIAN_POINT ( 'NONE',  ( -67.91293329751579222, 37.48821246049005396, 8.742028012086855426 ) ) ;
#40147=CARTESIAN_POINT ( 'NONE',  ( 79.38089166731855073, 66.16750285958215727, 1.809109834152207164 ) ) ;
#40159=CARTESIAN_POINT ( 'NONE',  ( -64.08758708074093136, 36.14363715547680300, -3.800414904976364028 ) ) ;
#40167=B_SPLINE_CURVE_WITH_KNOTS ( 'NONE', 3,
 ( #29693, #7669, #7870, #1117, #17317, #13649 ),
 .UNSPECIFIED., .F., .F.,
 ( 4, 2, 4 ),
 ( 0.0002345877247508168376, 0.0005913096522288236161, 0.0009480315797068302863 ),
 .UNSPECIFIED. ) ;
#40168=CARTESIAN_POINT ( 'NONE',  ( 66.88885785885000246, 57.86870549787170859, -3.998465113252547720 ) ) ;
#40179=CARTESIAN_POINT ( 'NONE',  ( 82.43037228308448050, 64.59322875725442259, -1.000000000000000000 ) ) ;
#40180=CARTESIAN_POINT ( 'NONE',  ( 81.15619658878986797, 61.33623061796058806, 1.560659576774481971 ) ) ;
#40183=CARTESIAN_POINT ( 'NONE',  ( 76.11285053945336188, 63.10974250081550707, -3.590981437842944324 ) ) ;
#40187=CARTESIAN_POINT ( 'NONE',  ( 81.26611686294326375, 61.37229692769314227, -1.428845309148531584 ) ) ;
#40188=CARTESIAN_POINT ( 'NONE',  ( 76.31986902294670472, 64.06746608568100498, 3.012346708716361565 ) ) ;
#40193=EDGE_LOOP ( 'NONE', ( #25829, #25851, #37563, #34181 ) ) ;
#40194=CARTESIAN_POINT ( 'NONE',  ( 81.53194397951713768, 65.66224036380459950, 1.718006205139014364 ) ) ;
#40199=CARTESIAN_POINT ( 'NONE',  ( -59.93345510331042902, 24.73247967741478703, -12.49999999999999645 ) ) ;
#40200=CARTESIAN_POINT ( 'NONE',  ( -64.38387608637887638, 34.70929407487223273, 5.501206404649374271 ) ) ;
#40218=EDGE_CURVE ( 'NONE', #28074, #3507, #20167, .T. ) ;
#40219=CARTESIAN_POINT ( 'NONE',  ( 69.77571843317402056, 59.04509999696490041, -3.985452289341159915 ) ) ;
#40222=AXIS2_PLACEMENT_3D ( 'NONE', #32911, #19550, #26334 ) ;
#40224=CARTESIAN_POINT ( 'NONE',  ( 69.92361841086972163, 58.66916198470556765, 3.954846139149858164 ) ) ;
#40233=CARTESIAN_POINT ( 'NONE',  ( 80.66846628934483476, 61.48471191768543775, -2.456741006817842798 ) ) ;
#40235=CARTESIAN_POINT ( 'NONE',  ( 81.88105255503960223, 62.58610580235431087, -2.445541897054222868 ) ) ;
#40237=CARTESIAN_POINT ( 'NONE',  ( 78.73387159939801450, 65.21990392541003700, 2.961936469198041433 ) ) ;
#40260=CARTESIAN_POINT ( 'NONE',  ( 66.98331017875999294, 58.06610265625960210, 3.998453671246410046 ) ) ;
#40276=CARTESIAN_POINT ( 'NONE',  ( 80.96252947514877008, 61.71397308826821870, -2.561782662428527146 ) ) ;
#40278=CARTESIAN_POINT ( 'NONE',  ( 80.39951605126509548, 63.19197404919997751, 3.632888195267896858 ) ) ;
#40281=CARTESIAN_POINT ( 'NONE',  ( 74.96893927862336682, 59.62365076172311262, -3.485789274173447083 ) ) ;
#40285=CARTESIAN_POINT ( 'NONE',  ( -68.71186372058383540, 37.81212149306784909, -9.800414904976365804 ) ) ;
#40286=EDGE_CURVE ( 'NONE', #9808, #23165, #5746, .T. ) ;
#40295=CARTESIAN_POINT ( 'NONE',  ( 81.19366756170084898, 63.21158026472419067, 3.307636073424109924 ) ) ;
#40299=CARTESIAN_POINT ( 'NONE',  ( -65.15514661499977933, 34.97220226750606997, 6.888442104241535802 ) ) ;
#40312=CARTESIAN_POINT ( 'NONE',  ( 79.98672868146590531, 65.19218680485843720, -3.233552917234638446 ) ) ;
#40321=CARTESIAN_POINT ( 'NONE',  ( 81.11033257497912530, 61.28231361833088897, -1.235082213173757770 ) ) ;
#40327=CARTESIAN_POINT ( 'NONE',  ( 80.57628295459058165, 65.85481838934495613, -2.430878896394279565 ) ) ;
#40330=CARTESIAN_POINT ( 'NONE',  ( -59.01947560891952804, 27.90920910948504385, 6.147301388271928957 ) ) ;
#40336=CARTESIAN_POINT ( 'NONE',  ( 74.55930941259208566, 60.55296354997373953, 3.883841728571185481 ) ) ;
#40342=CARTESIAN_POINT ( 'NONE',  ( -58.83368549508428913, 29.29773222442904412, -5.899739961855157588 ) ) ;
#40344=CARTESIAN_POINT ( 'NONE',  ( 81.86163085503910963, 62.85586669281870087, 2.670779692148243178 ) ) ;
#40362=CARTESIAN_POINT ( 'NONE',  ( 67.03747645593968230, 57.91646344912344091, -3.998003515188802037 ) ) ;
#40371=CARTESIAN_POINT ( 'NONE',  ( 79.00097698949592484, 66.21430696267364624, -1.024355359505926488 ) ) ;
#40372=CARTESIAN_POINT ( 'NONE',  ( 80.94990806105060699, 62.43782317439323037, 3.178394274514596773 ) ) ;
#40373=CIRCLE ( 'NONE', #33827, 3.000000000000002220 ) ;
#40376=CARTESIAN_POINT ( 'NONE',  ( 76.98094665547928628, 64.12925941789167439, -3.220231295875725319 ) ) ;
#40380=CARTESIAN_POINT ( 'NONE',  ( 81.51347805234148325, 61.90211215308941206, -2.263370276487066679 ) ) ;
#40381=CARTESIAN_POINT ( 'NONE',  ( 78.16578481971126280, 61.75018358139124786, 3.687756614093599783 ) ) ;
#40387=EDGE_CURVE ( 'NONE', #15332, #11154, #12290, .T. ) ;
#40390=CARTESIAN_POINT ( 'NONE',  ( 80.61888529134442649, 66.16066543623880136, 1.646077502935600734 ) ) ;
#40391=CARTESIAN_POINT ( 'NONE',  ( -64.08758708074094557, 42.86825253850305728, 2.416740211339933442 ) ) ;
#40400=CARTESIAN_POINT ( 'NONE',  ( 81.16957891225059996, 61.30398062001309256, 1.000000000000000000 ) ) ;
#40401=CARTESIAN_POINT ( 'NONE',  ( -60.75950795826495465, 23.17721540975219696, -46.17089178453873188 ) ) ;
#40405=DIRECTION ( 'NONE',  ( 1.000000000000000000, 0.000000000000000000, 0.000000000000000000 ) ) ;
#40408=CARTESIAN_POINT ( 'NONE',  ( -64.08758708074093136, 37.27332153486465671, -4.546479763848711109 ) ) ;
#40412=AXIS2_PLACEMENT_3D ( 'NONE', #17352, #36719, #39187 ) ;
#40414=CARTESIAN_POINT ( 'NONE',  ( 69.75093826875801994, 59.10798165618643907, -3.985452289341158139 ) ) ;
#40424=CARTESIAN_POINT ( 'NONE',  ( 80.51696178947716476, 61.27878891920004634, -2.305838555345020247 ) ) ;
#40426=CARTESIAN_POINT ( 'NONE',  ( 81.85373309064766545, 62.29294994509992733, -2.264354540981538211 ) ) ;
#40427=CARTESIAN_POINT ( 'NONE',  ( 79.10818533696262023, 64.58014521944369335, 3.489618106120226049 ) ) ;
#40430=EDGE_CURVE ( 'NONE', #33628, #29749, #20930, .T. ) ;
#40431=AXIS2_PLACEMENT_3D ( 'NONE', #17191, #29966, #10812 ) ;
#40452=CARTESIAN_POINT ( 'NONE',  ( 66.97838688114072170, 58.07970146089488850, 3.998003515188801149 ) ) ;
#40455=CARTESIAN_POINT ( 'NONE',  ( -58.99872204295123623, 28.48507918597134037, 12.49999999999999645 ) ) ;
#40470=CARTESIAN_POINT ( 'NONE',  ( 78.85101321104539807, 65.59805058642685083, -2.603857329607544013 ) ) ;
#40472=CARTESIAN_POINT ( 'NONE',  ( 80.32629651820978722, 63.16159226777920566, 3.644176963625957111 ) ) ;
#40478=DIRECTION ( 'NONE',  ( -0.9267318687906771491, 0.3757233601570964532, 0.000000000000000000 ) ) ;
#40481=CARTESIAN_POINT ( 'NONE',  ( -81.78329181448161478, 33.71485196875532608, -9.800414904976365804 ) ) ;
#40485=AXIS2_PLACEMENT_3D ( 'NONE', #2274, #14797, #39928 ) ;
#40488=CARTESIAN_POINT ( 'NONE',  ( 80.95544561733518663, 63.83034742112759830, 3.486376426170537002 ) ) ;
#40492=ORIENTED_EDGE ( 'NONE', *, *, #7722, .T. ) ;
#40493=CARTESIAN_POINT ( 'NONE',  ( -64.41585990636637860, 34.69667140566502894, -5.588029444252497591 ) ) ;
#40499=CARTESIAN_POINT ( 'NONE',  ( -65.62105494223132496, 35.19887319331773767, -7.481751891074711835 ) ) ;
#40507=CARTESIAN_POINT ( 'NONE',  ( 78.67345636894508232, 66.04656848779336542, -1.137963815189258598 ) ) ;
#40510=DIRECTION ( 'NONE',  ( 0.000000000000000000, 0.000000000000000000, 1.000000000000000000 ) ) ;
#40516=EDGE_CURVE ( 'NONE', #36812, #11880, #23764, .T. ) ;
#40520=CARTESIAN_POINT ( 'NONE',  ( 81.06760980982289766, 61.95377044681377043, -2.747716423863113100 ) ) ;
#40528=CARTESIAN_POINT ( 'NONE',  ( 81.94117896397179379, 62.33638752672998606, -2.166533184762309716 ) ) ;
#40535=CARTESIAN_POINT ( 'NONE',  ( 73.56486102181378328, 61.25343517167133456, 3.876585409328609177 ) ) ;
#40542=CARTESIAN_POINT ( 'NONE',  ( 80.50371486736987947, 65.47929316355259743, 2.914706979937431885 ) ) ;
#40565=CARTESIAN_POINT ( 'NONE',  ( 67.01285850879368411, 57.98447793263278527, -3.999354069328931782 ) ) ;
#40568=CARTESIAN_POINT ( 'NONE',  ( -57.41832745699786500, 33.02173582530747353, 4.020356607641593527 ) ) ;
#40571=CARTESIAN_POINT ( 'NONE',  ( -64.94969918204330384, 34.86787045525706219, 6.612452343231767671 ) ) ;
#40577=CARTESIAN_POINT ( 'NONE',  ( 81.16936534046872964, 61.30390240240431865, -1.014334479594669602 ) ) ;
#40578=CARTESIAN_POINT ( 'NONE',  ( 80.15412116699829426, 64.17350884197745131, 3.654032574946332268 ) ) ;
#40581=CARTESIAN_POINT ( 'NONE',  ( 76.03108743707694828, 63.27561679962271057, -3.498861892150602060 ) ) ;
#40588=CARTESIAN_POINT ( 'NONE',  ( 81.36347513509552698, 62.06248151587791995, -2.615128354545410705 ) ) ;
#40590=CARTESIAN_POINT ( 'NONE',  ( 78.43336062804338837, 61.18469638573561298, 3.363831406680000136 ) ) ;
#40595=CARTESIAN_POINT ( 'NONE',  ( -57.31086168400016589, 33.19661634462462274, 4.000000000000000000 ) ) ;
#40596=CARTESIAN_POINT ( 'NONE',  ( 81.32635356316056630, 65.55379304840816701, 2.259066313177355401 ) ) ;
#40597=CARTESIAN_POINT ( 'NONE',  ( -64.08758708074093136, 41.04287353446839148, 3.000000000000000000 ) ) ;
#40601=CARTESIAN_POINT ( 'NONE',  ( -62.75232748054406073, 36.25463151227798875, -4.889949273166490862 ) ) ;
#40602=CARTESIAN_POINT ( 'NONE',  ( -64.52806261857489289, 36.37942767235070818, 5.858659361856595638 ) ) ;
#40614=CARTESIAN_POINT ( 'NONE',  ( 28.61591789821288145, 47.14532032487838364, 1.000000000000000000 ) ) ;
#40621=EDGE_CURVE ( 'NONE', #29368, #18695, #29409, .T. ) ;
#40625=CARTESIAN_POINT ( 'NONE',  ( 69.52987064631375347, 59.66723168662304033, -3.901551322707137004 ) ) ;
#40633=CARTESIAN_POINT ( 'NONE',  ( -80.19065981525226050, 31.27226540113725406, -9.800414904976365804 ) ) ;
#40639=CARTESIAN_POINT ( 'NONE',  ( 80.35854813638249539, 61.23284135048811549, -2.372109611208351954 ) ) ;
#40642=CARTESIAN_POINT ( 'NONE',  ( 81.65405438441118235, 61.80769279848058062, -1.809109834152291540 ) ) ;
#40643=CARTESIAN_POINT ( 'NONE',  ( 80.72339804071911828, 61.33444547702554672, 2.197205184446166193 ) ) ;
#40646=CARTESIAN_POINT ( 'NONE',  ( 82.10909544300281482, 65.20937546977818045, 1.000000000000000000 ) ) ;
#40654=ORIENTED_EDGE ( 'NONE', *, *, #30751, .T. ) ;
#40657=DIRECTION ( 'NONE',  ( -1.000000000000000000, 0.000000000000000000, 0.000000000000000000 ) ) ;
#40671=CARTESIAN_POINT ( 'NONE',  ( 67.03747645593968230, 57.91646344912344091, 3.998003515188802037 ) ) ;
#40680=CARTESIAN_POINT ( 'NONE',  ( -81.07947155388369254, 30.81399289130168384, 12.49999999999999645 ) ) ;
#40687=CARTESIAN_POINT ( 'NONE',  ( 80.59739669508272186, 62.32949743464985204, -3.275607309966713565 ) ) ;
#40689=CARTESIAN_POINT ( 'NONE',  ( 79.55161461803720613, 64.54397228415258780, 3.537885823842634725 ) ) ;
#40698=CARTESIAN_POINT ( 'NONE',  ( -55.09636020043951987, 31.27759585575460477, 1.408872394161159836 ) ) ;
#40701=CARTESIAN_POINT ( 'NONE',  ( -63.99293516169446150, 35.89893413629674512, -7.506047544094580637 ) ) ;
#40705=CARTESIAN_POINT ( 'NONE',  ( 80.95699988731961128, 64.21667718577513995, 3.402511877379640559 ) ) ;
#40708=ORIENTED_EDGE ( 'NONE', *, *, #19865, .T. ) ;
#40713=EDGE_CURVE ( 'NONE', #19152, #12078, #6824, .T. ) ;
#40739=COLOUR_RGB('Light Blue',0.38,0.62,0.78);
#40740=FILL_AREA_STYLE_COLOUR('',#40739);
#40741=FILL_AREA_STYLE('',(#40740));
#40742=SURFACE_STYLE_FILL_AREA(#40741);
#40743=SURFACE_SIDE_STYLE('',(#40742));
#40744=SURFACE_STYLE_USAGE(.BOTH.,#40743);
#40745=PRESENTATION_STYLE_ASSIGNMENT((#40744));
ENDSEC;
END-ISO-10303-21;
